ISO-10303-21;
HEADER;
FILE_DESCRIPTION (('STEP AP214'),
    '1' );
FILE_NAME ('Security screw.step',
    '2026-10-07T19:06:49',
    ( '' ),
    ( '' ),
    'SwSTEP 2.0',
    'SolidWorks 2020',
    '' );
FILE_SCHEMA (( 'AUTOMOTIVE_DESIGN' ));
ENDSEC;

DATA;
#5=EDGE_LOOP ( 'NONE', ( #45388, #8761, #11979 ) ) ;
#31=CARTESIAN_POINT ( 'NONE',  ( -1.435212230719999926, -80.44593403531600018, -0.7398511866349000154 ) ) ;
#35=CARTESIAN_POINT ( 'NONE',  ( -0.2380956042587999977, -78.76861702419900269, -1.297642515519999984 ) ) ;
#76=EDGE_CURVE ( 'NONE', #36029, #6234, #44439, .T. ) ;
#77=CARTESIAN_POINT ( 'NONE',  ( 1.232689987415999999, -80.87906169571699877, -0.4701533967999000363 ) ) ;
#94=ORIENTED_EDGE ( 'NONE', *, *, #34546, .F. ) ;
#169=CARTESIAN_POINT ( 'NONE',  ( -0.06134698815010001388, -80.66909307349899905, -1.515015350337000077 ) ) ;
#179=CARTESIAN_POINT ( 'NONE',  ( -0.1963495408493673433, -78.38541666666668561, 1.499999999999999334 ) ) ;
#187=FACE_OUTER_BOUND ( 'NONE', #5, .T. ) ;
#188=CARTESIAN_POINT ( 'NONE',  ( -0.8465867926663999121, -80.83273884615699956, -0.9556525628790000226 ) ) ;
#205=CARTESIAN_POINT ( 'NONE',  ( -0.8668440880359000733, -77.83435542797239748, -1.013523202003999923 ) ) ;
#208=CARTESIAN_POINT ( 'NONE',  ( 0.6793464540269460450, -80.58066705791090101, 1.078661931325863188 ) ) ;
#221=LINE ( 'NONE', #4907, #38945 ) ;
#222=CARTESIAN_POINT ( 'NONE',  ( 1.058064258495000187, -81.94170750542799908, -0.7735121372284999852 ) ) ;
#228=CARTESIAN_POINT ( 'NONE',  ( -0.9898995639662998558, -79.60058255474299926, 0.8721608040441000131 ) ) ;
#246=CARTESIAN_POINT ( 'NONE',  ( 1.251671508224674323, -80.38505487870085631, -0.2410332141617578250 ) ) ;
#280=EDGE_CURVE ( 'NONE', #6234, #56598, #9324, .T. ) ;
#287=FACE_OUTER_BOUND ( 'NONE', #40391, .T. ) ;
#301=FACE_OUTER_BOUND ( 'NONE', #47142, .T. ) ;
#329=CARTESIAN_POINT ( 'NONE',  ( 0.5881506857339000582, -79.69598562025299771, 1.397505295191999952 ) ) ;
#432=CARTESIAN_POINT ( 'NONE',  ( -1.417334032777999964, -79.42654225787899236, -0.4910847579886000736 ) ) ;
#449=CARTESIAN_POINT ( 'NONE',  ( -0.3527936601020746354, -78.04753704632268807, 1.224052721373980690 ) ) ;
#455=ORIENTED_EDGE ( 'NONE', *, *, #16747, .F. ) ;
#457=CARTESIAN_POINT ( 'NONE',  ( 0.8888964087114000767, -80.66333400915199547, -1.347979478730999991 ) ) ;
#463=ADVANCED_BREP_SHAPE_REPRESENTATION ( '', ( #16630, #43526 ), #6767 ) ;
#473=CARTESIAN_POINT ( 'NONE',  ( -1.154258600661999923, -79.76363727870300124, -0.6680293646364998672 ) ) ;
#487=CARTESIAN_POINT ( 'NONE',  ( 0.2086861075963999945, -78.58438338449100513, 1.317203954600000060 ) ) ;
#508=CARTESIAN_POINT ( 'NONE',  ( -0.8958779135676999683, -82.17683127161700440, 0.9567003624791000638 ) ) ;
#514=CARTESIAN_POINT ( 'NONE',  ( -0.4820197951951999960, -79.25329419107600870, -1.228125725326999929 ) ) ;
#538=CARTESIAN_POINT ( 'NONE',  ( -0.1647286073852369803, -79.76489708643704546, -1.263362412047110306 ) ) ;
#551=CARTESIAN_POINT ( 'NONE',  ( 1.323534079420999987, -79.87453973706999477, -0.1638099207045999872 ) ) ;
#559=CARTESIAN_POINT ( 'NONE',  ( -1.250002149560441644, -82.24413779550083348, 0.09476315643046410997 ) ) ;
#572=CARTESIAN_POINT ( 'NONE',  ( 0.6680689699263999692, -78.46136003831350081, -1.250497193771000104 ) ) ;
#589=CARTESIAN_POINT ( 'NONE',  ( -0.9870767835202884921, -80.56949413944577998, -1.171048524979026340 ) ) ;
#593=CARTESIAN_POINT ( 'NONE',  ( 0.6849175148897999055, -77.80225862199890230, -1.144319635748999975 ) ) ;
#606=DIRECTION ( 'NONE',  ( 1.000000000000000000, 0.000000000000000000, 0.000000000000000000 ) ) ;
#619=CARTESIAN_POINT ( 'NONE',  ( -0.5539667471886999817, -79.44792250334801054, -1.411437496924000001 ) ) ;
#625=DIRECTION ( 'NONE',  ( -0.8320502943378438321, -0.5547001962252288143, -2.960716109815154402E-12 ) ) ;
#626=AXIS2_PLACEMENT_3D ( 'NONE', #27825, #9845, #41713 ) ;
#651=ORIENTED_EDGE ( 'NONE', *, *, #26448, .T. ) ;
#662=CARTESIAN_POINT ( 'NONE',  ( -0.7554284705563480973, -81.08333333333332860, -1.310679582531387277 ) ) ;
#667=CARTESIAN_POINT ( 'NONE',  ( 0.000000000000000000, -76.79999999999999716, 0.000000000000000000 ) ) ;
#722=CYLINDRICAL_SURFACE ( 'NONE', #626, 1.500000000000000000 ) ;
#745=CARTESIAN_POINT ( 'NONE',  ( -1.570404433027000168, -81.01062237281999501, -0.3755580415715000231 ) ) ;
#760=CARTESIAN_POINT ( 'NONE',  ( -0.3926218265389255779, -79.39583333333335702, 1.460959015002472494 ) ) ;
#765=CARTESIAN_POINT ( 'NONE',  ( -1.181111693982000110, -79.17654225787899236, -0.4092372983238000139 ) ) ;
#776=CARTESIAN_POINT ( 'NONE',  ( -0.1765672563250000049, -78.38009428516419064, -1.321892640673999919 ) ) ;
#793=CARTESIAN_POINT ( 'NONE',  ( 0.5862232456189999663, -82.13815345286899117, 1.280678996225000033 ) ) ;
#799=CARTESIAN_POINT ( 'NONE',  ( -1.199500263597274685, -81.44791666666668561, 0.9218200799623673669 ) ) ;
#835=CARTESIAN_POINT ( 'NONE',  ( -1.261445002938999860, -79.14688792748098933, -0.1968185027220000216 ) ) ;
#843=CARTESIAN_POINT ( 'NONE',  ( -8.022734517049746273E-06, -82.01564364893640402, -1.484164386985079798 ) ) ;
#855=CARTESIAN_POINT ( 'NONE',  ( 0.7281259072094999896, -77.96523380450278751, -1.216509659635999885 ) ) ;
#857=ORIENTED_EDGE ( 'NONE', *, *, #38891, .F. ) ;
#858=ADVANCED_FACE ( 'NONE', ( #52466 ), #2310, .T. ) ;
#872=CARTESIAN_POINT ( 'NONE',  ( -1.295435361468000091, -77.65342075185570536, -0.3166359884281000348 ) ) ;
#900=VERTEX_POINT ( 'NONE', #11455 ) ;
#903=CARTESIAN_POINT ( 'NONE',  ( 0.3023484132065000218, -79.99366136053998844, -1.485775080250999913 ) ) ;
#906=ADVANCED_FACE ( 'NONE', ( #47487 ), #15853, .F. ) ;
#912=B_SPLINE_CURVE_WITH_KNOTS ( 'NONE', 3,
 ( #17029, #35299, #12028, #30008, #21457, #34727, #52756, #30299, #53328, #12874, #12309, #4021, #30876, #2881, #48911, #53625, #48340, #8452 ),
 .UNSPECIFIED., .F., .F.,
 ( 4, 2, 2, 2, 2, 2, 2, 2, 4 ),
 ( 0.000000000000000000, 0.1249999999999999722, 0.2499999999999999445, 0.3749999999999998890, 0.4999999999999998890, 0.6249999999999998890, 0.7499999999999997780, 0.8749999999999998890, 1.000000000000000000 ),
 .UNSPECIFIED. ) ;
#940=CARTESIAN_POINT ( 'NONE',  ( 1.500000000000000000, -80.65000000000000568, 0.000000000000000000 ) ) ;
#944=CARTESIAN_POINT ( 'NONE',  ( -1.220882145615000081, -81.12712481262300912, 0.5000124012157000086 ) ) ;
#974=CARTESIAN_POINT ( 'NONE',  ( 0.3299670982549000042, -78.85056507792100433, 1.580613947285000043 ) ) ;
#981=EDGE_CURVE ( 'NONE', #9701, #31705, #54281, .T. ) ;
#1009=B_SPLINE_SURFACE_WITH_KNOTS ( 'NONE', 3, 3, ( 
 ( #41246, #835, #14955, #14085, #50997, #55409, #41834, #15255, #51290, #32953, #10545, #23240, #10845, #4944, #28529, #46578, #551, #18817, #18528, #36809, #36520, #32082, #54828, #32369, #27942, #45990, #5516, #23526, #1120, #37099, #55115, #14659, #10249, #56001, #57149 ),
 ( #15842, #33544, #24983, #2847, #19990, #33830, #38269, #56576, #11141, #16714, #43004, #52155, #51868, #34696, #38560, #11422, #42713, #38847, #16135, #11712, #29115, #15550, #2561, #29401, #47454, #6980, #20562, #6693, #24411, #29688, #47738, #2279, #7271, #52725, #25272 ),
 ( #28820, #56866, #16425, #6396, #39138, #29975, #48027, #7560, #46869, #25560, #42427, #3696, #473, #49758, #45323, #17566, #9008, #57712, #44731, #36442, #22871, #21698, #49462, #12836, #4875, #54177, #9298, #26993, #53887, #45028, #58307, #27287, #4580, #26407, #40593 ),
 ( #32004, #18452, #35259, #4282, #44430, #27578, #3983, #39994, #39705, #54471, #53289, #17868, #40881, #26700, #14007, #21985, #50045, #58007, #13418, #30836, #17269, #9592, #35558, #48869, #18164, #22279, #8410, #31709, #53584, #13122, #31116, #8709, #49157, #188, #22580 ) ),
 .UNSPECIFIED., .F., .F., .F.,
 ( 4, 4 ),
 ( 4, 1, 1, 1, 1, 1, 1, 1, 1, 1, 1, 1, 1, 1, 1, 1, 1, 1, 1, 1, 1, 1, 1, 1, 1, 1, 1, 1, 1, 1, 1, 1, 4 ),
 ( -0.1566102636784000024, 1.156610263678000017 ),
 ( -0.02000000000000000042, 0.01250000000000000069, 0.04499999999999999833, 0.07749999999999999944, 0.1100000000000000006, 0.1424999999999999878, 0.1749999999999999889, 0.2074999999999999900, 0.2399999999999999911, 0.2725000000000000200, 0.3049999999999999933, 0.3375000000000000222, 0.3699999999999999956, 0.4025000000000000244, 0.4349999999999999978, 0.4675000000000000266, 0.5000000000000000000, 0.5324999999999999734, 0.5649999999999999467, 0.5975000000000000311, 0.6300000000000000044, 0.6624999999999999778, 0.6949999999999999512, 0.7275000000000000355, 0.7600000000000000089, 0.7924999999999999822, 0.8249999999999999556, 0.8575000000000000400, 0.8900000000000000133, 0.9224999999999999867, 0.9549999999999999600, 0.9875000000000000444, 1.020000000000000018 ),
 .UNSPECIFIED. ) ;
#1022=CARTESIAN_POINT ( 'NONE',  ( -1.181111693982000110, -79.27654225787900089, -0.4092372983238000139 ) ) ;
#1032=CARTESIAN_POINT ( 'NONE',  ( -0.6920646488899999671, -81.51826673532400491, 1.237378641307999905 ) ) ;
#1046=CARTESIAN_POINT ( 'NONE',  ( 0.7554284705563453217, -79.33333333333334281, 1.310679582531389276 ) ) ;
#1060=CARTESIAN_POINT ( 'NONE',  ( 0.9384621721472999889, -78.57854477868900744, 0.9475573338641000154 ) ) ;
#1080=CARTESIAN_POINT ( 'NONE',  ( 0.2104032054905000115, -81.54352552975799995, -1.590243660542000059 ) ) ;
#1082=AXIS2_PLACEMENT_3D ( 'NONE', #46716, #41673, #6235 ) ;
#1090=CARTESIAN_POINT ( 'NONE',  ( -1.417334032777999964, -79.42654225787899236, -0.4910847579886000736 ) ) ;
#1096=CARTESIAN_POINT ( 'NONE',  ( 1.249999992656000147, -76.50000000027618796, -0.4999999997238000482 ) ) ;
#1120=CARTESIAN_POINT ( 'NONE',  ( 0.6343572851480000496, -80.46989121764299568, 1.173101423079000005 ) ) ;
#1128=CARTESIAN_POINT ( 'NONE',  ( 0.5515549627219517026, -82.09100159915311679, 1.204941737300085691 ) ) ;
#1161=CARTESIAN_POINT ( 'NONE',  ( 1.500000000000000000, -78.64999999999999147, 0.000000000000000000 ) ) ;
#1189=B_SPLINE_CURVE_WITH_KNOTS ( 'NONE', 3,
 ( #4361, #44223, #31494, #12630, #4058, #30626, #12911, #35936, #45113, #4665, #39201, #13202, #3772, #57216, #30910, #48944, #22062, #31197, #22957, #40968, #36237, #32377, #54552, #41256, #23533, #50420, #18826, #46292, #19408, #1128, #19117, #55417, #37107, #559, #54260 ),
 .UNSPECIFIED., .F., .F.,
 ( 4, 1, 1, 1, 1, 1, 1, 1, 1, 1, 1, 1, 1, 1, 1, 1, 1, 1, 1, 1, 1, 1, 1, 1, 1, 1, 1, 1, 1, 1, 1, 1, 4 ),
 ( 0.000000000000000000, 0.01250524777966226068, 0.04500492809905208558, 0.07750460841844190873, 0.1100042887377895434, 0.1425039690572004469, 0.1750036493766114198, 0.2075033296960223372, 0.2400030100154332546, 0.2725026903347386731, 0.3050023706541495905, 0.3375020509735605079, 0.3700017312929714808, 0.4025014116123823427, 0.4350010919316877334, 0.4675007722510986508, 0.5000004525705096237, 0.5325001328899204855, 0.5649998132093314585, 0.5974994935287424314, 0.6299991738480477110, 0.6624988541674586839, 0.6949985344868696568, 0.7274982148062805187, 0.7599978951256914916, 0.7924975754449967713, 0.8249972557644078552, 0.8574969360838187171, 0.8899966164032295790, 0.9224962967226405519, 0.9549959770419459426, 0.9874956573613570265, 1.000000000000000000 ),
 .UNSPECIFIED. ) ;
#1232=CARTESIAN_POINT ( 'NONE',  ( 1.249999993052000047, -76.30000000069199473, 0.6999999993075000093 ) ) ;
#1257=CARTESIAN_POINT ( 'NONE',  ( -0.4820197951951999960, -79.33717912789200000, -1.228125725326999929 ) ) ;
#1259=CARTESIAN_POINT ( 'NONE',  ( -1.568439782227999846, -77.51102424663160662, -0.3833649254202000090 ) ) ;
#1260=CIRCLE ( 'NONE', #4991, 0.5000000000000000000 ) ;
#1293=CARTESIAN_POINT ( 'NONE',  ( 1.310679582531385279, -80.29166666666668561, 0.7554284705563519831 ) ) ;
#1315=CARTESIAN_POINT ( 'NONE',  ( -0.6310361675857999453, -82.01439296913500243, 1.269589084679000113 ) ) ;
#1328=CARTESIAN_POINT ( 'NONE',  ( 0.000000000000000000, -75.67500000000001137, 0.000000000000000000 ) ) ;
#1329=CARTESIAN_POINT ( 'NONE',  ( 1.460959015002472494, -79.27083333333335702, 0.3926218265389233020 ) ) ;
#1361=CARTESIAN_POINT ( 'NONE',  ( -1.414458455730000175, -82.43699584127701030, -0.5383077919788999965 ) ) ;
#1367=CARTESIAN_POINT ( 'NONE',  ( 0.7554284705563452107, -80.73333333333332007, 1.310679582531388609 ) ) ;
#1368=CARTESIAN_POINT ( 'NONE',  ( 0.3256773761571999937, -79.30290681445698908, -1.278468177226000035 ) ) ;
#1448=CARTESIAN_POINT ( 'NONE',  ( 0.2725326480772000126, -78.99296158314500360, 1.305490477442999842 ) ) ;
#1542=CARTESIAN_POINT ( 'NONE',  ( -1.247892825656000015, -79.25449142225700427, -0.1947040076506000028 ) ) ;
#1559=CARTESIAN_POINT ( 'NONE',  ( 0.7505602511881427352, -77.92510946887425405, -1.030241528371574677 ) ) ;
#1588=DIRECTION ( 'NONE',  ( 0.000000000000000000, 1.000000000000000000, 1.898821519315000128E-14 ) ) ;
#1589=CYLINDRICAL_SURFACE ( 'NONE', #17101, 1.500000000000000000 ) ;
#1594=VERTEX_POINT ( 'NONE', #11378 ) ;
#1600=CARTESIAN_POINT ( 'NONE',  ( 1.388711894915000133, -81.26444455407199996, -0.6086225636969000430 ) ) ;
#1604=CARTESIAN_POINT ( 'NONE',  ( -0.7554284705563544255, -81.91666666667600794, 1.310679582531384169 ) ) ;
#1615=DIRECTION ( 'NONE',  ( 0.000000000000000000, 0.000000000000000000, -1.000000000000000000 ) ) ;
#1616=CARTESIAN_POINT ( 'NONE',  ( -0.1963495408493673433, -79.38541666666668561, 1.499999999999999334 ) ) ;
#1654=CARTESIAN_POINT ( 'NONE',  ( 1.426927307065000150, -81.12030275061700024, -0.7328213294338999928 ) ) ;
#1660=CARTESIAN_POINT ( 'NONE',  ( 0.1963495408493571848, -80.76458333333334849, 1.500000000000000666 ) ) ;
#1711=CARTESIAN_POINT ( 'NONE',  ( -0.8719406389885000497, -81.20263150142500308, -1.009106372638000071 ) ) ;
#1725=CYLINDRICAL_SURFACE ( 'NONE', #17188, 4.000000000000000000 ) ;
#1739=CARTESIAN_POINT ( 'NONE',  ( -1.256362333281000110, -77.66411968718020375, 0.2270125678640999844 ) ) ;
#1780=CARTESIAN_POINT ( 'NONE',  ( 1.500000000000000000, -80.75000000000000000, 0.000000000000000000 ) ) ;
#1790=ORIENTED_EDGE ( 'NONE', *, *, #40283, .F. ) ;
#1826=CARTESIAN_POINT ( 'NONE',  ( 1.199500263597268246, -80.20208333333334849, 0.9218200799623752495 ) ) ;
#1840=CARTESIAN_POINT ( 'NONE',  ( -1.347317391812999920, -79.03247803031800345, -0.7577098654840999092 ) ) ;
#1865=CARTESIAN_POINT ( 'NONE',  ( -0.9657971644277000278, -82.32620602178199931, -0.9195906491977999808 ) ) ;
#1879=CARTESIAN_POINT ( 'NONE',  ( -0.7554284705563544255, -80.41666666666667140, 1.310679582531384169 ) ) ;
#1899=CARTESIAN_POINT ( 'NONE',  ( -1.340601520916999911, -82.00863390478799886, 0.7083111249264000264 ) ) ;
#1905=CARTESIAN_POINT ( 'NONE',  ( -0.1963495408493605987, -78.11458333333332860, -1.500000000000000444 ) ) ;
#1921=CARTESIAN_POINT ( 'NONE',  ( -1.500000000000000000, -81.50000000000000000, 0.000000000000000000 ) ) ;
#1932=CARTESIAN_POINT ( 'NONE',  ( 0.2725326480772000126, -79.12428363588000479, 1.305490477442999842 ) ) ;
#1951=CARTESIAN_POINT ( 'NONE',  ( -0.4716608572466999827, -81.25303007584000170, 1.430537295918000051 ) ) ;
#1958=CARTESIAN_POINT ( 'NONE',  ( -0.3926218265389256890, -80.79583333333334849, 1.460959015002472050 ) ) ;
#1963=ORIENTED_EDGE ( 'NONE', *, *, #25227, .F. ) ;
#2007=CARTESIAN_POINT ( 'NONE',  ( -0.6509962010243000030, -81.54991986509199364, 1.163950211895000031 ) ) ;
#2009=CARTESIAN_POINT ( 'NONE',  ( 0.9186508726441413586, -79.17551408595964801, -1.236643120628077241 ) ) ;
#2011=VECTOR ( 'NONE', #36511, 1000.000000000000000 ) ;
#2016=EDGE_LOOP ( 'NONE', ( #45371, #52569, #19655, #5257 ) ) ;
#2026=CARTESIAN_POINT ( 'NONE',  ( -1.527286180810999872, -79.00449142225700427, -0.2382966983378000114 ) ) ;
#2030=CARTESIAN_POINT ( 'NONE',  ( 1.196963559360000096, -78.34799747919070967, -0.5880938590690999446 ) ) ;
#2042=EDGE_CURVE ( 'NONE', #30255, #39723, #43715, .T. ) ;
#2068=EDGE_CURVE ( 'NONE', #35842, #42334, #57094, .T. ) ;
#2072=B_SPLINE_CURVE_WITH_KNOTS ( 'NONE', 3,
 ( #17844, #21959, #40860, #26384 ),
 .UNSPECIFIED., .F., .F.,
 ( 4, 4 ),
 ( 0.000000000000000000, 1.000000000000000000 ),
 .UNSPECIFIED. ) ;
#2083=ORIENTED_EDGE ( 'NONE', *, *, #26596, .F. ) ;
#2100=CARTESIAN_POINT ( 'NONE',  ( -0.9641794813156493449, -78.20655186485167576, -0.8343030551515581150 ) ) ;
#2127=CARTESIAN_POINT ( 'NONE',  ( 0.2218511837006999776, -78.46518221956569050, 1.400300479361000106 ) ) ;
#2144=CARTESIAN_POINT ( 'NONE',  ( -1.184494039570261226, -78.72019068799889396, 0.4727986017936515184 ) ) ;
#2151=CARTESIAN_POINT ( 'NONE',  ( -0.7807745468539649680, -81.57766601766863346, 1.007917326718190898 ) ) ;
#2153=VECTOR ( 'NONE', #16088, 1000.000000000000114 ) ;
#2154=CARTESIAN_POINT ( 'NONE',  ( -1.200131629027000102, -80.78821469696899271, -0.3495483843597000373 ) ) ;
#2216=CARTESIAN_POINT ( 'NONE',  ( -0.2406813341972999787, -78.87622051897500342, -1.311734976874999958 ) ) ;
#2229=CARTESIAN_POINT ( 'NONE',  ( 1.250000000000000000, -76.50000000000000000, -0.5000000000000000000 ) ) ;
#2242=CARTESIAN_POINT ( 'NONE',  ( -0.1963495408493673156, -80.78541666666670551, 1.499999999999999556 ) ) ;
#2279=CARTESIAN_POINT ( 'NONE',  ( -1.308081345731999967, -80.66250310536500479, 0.2599445073669000017 ) ) ;
#2292=CARTESIAN_POINT ( 'NONE',  ( 1.500000000000000000, -77.75000000000000000, 0.000000000000000000 ) ) ;
#2310=CYLINDRICAL_SURFACE ( 'NONE', #53783, 1.500000000000000000 ) ;
#2314=FACE_OUTER_BOUND ( 'NONE', #22185, .T. ) ;
#2317=CARTESIAN_POINT ( 'NONE',  ( -0.9151233253627000241, -78.24293362662599804, -0.9701162038759999495 ) ) ;
#2323=VERTEX_POINT ( 'NONE', #36045 ) ;
#2368=CIRCLE ( 'NONE', #31531, 4.000000000000000000 ) ;
#2375=CARTESIAN_POINT ( 'NONE',  ( -1.259732728554407988, -79.32676086870174004, -0.4364646385938031337 ) ) ;
#2383=CONICAL_SURFACE ( 'NONE', #8984, 0.5999999993581000002, 0.7853981633972997312 ) ;
#2385=CARTESIAN_POINT ( 'NONE',  ( 0.3718183191318770731, -79.00162595749708316, 1.218859363413805852 ) ) ;
#2409=CARTESIAN_POINT ( 'NONE',  ( 1.500000000000000000, -79.25000000000000000, 0.000000000000000000 ) ) ;
#2411=UNCERTAINTY_MEASURE_WITH_UNIT (LENGTH_MEASURE( 1.000000000000000082E-05 ), #44948, 'distance_accuracy_value', 'NONE');
#2412=CARTESIAN_POINT ( 'NONE',  ( 1.326698500471999997, -78.75709889550499554, -0.7340390780227000755 ) ) ;
#2436=CARTESIAN_POINT ( 'NONE',  ( -0.8273849986450537708, -80.71898599761188109, -0.9695052011924152335 ) ) ;
#2439=CARTESIAN_POINT ( 'NONE',  ( -0.9820397338569999413, -80.70308451575900222, -0.7733679338621000099 ) ) ;
#2450=CARTESIAN_POINT ( 'NONE',  ( -1.250000000000000000, -77.64999999999999147, 0.000000000000000000 ) ) ;
#2467=ORIENTED_EDGE ( 'NONE', *, *, #16504, .T. ) ;
#2474=CARTESIAN_POINT ( 'NONE',  ( 0.3926218265389220807, -78.14583333333335702, -1.460959015002473382 ) ) ;
#2496=CARTESIAN_POINT ( 'NONE',  ( -0.5996107393304999089, -78.67777002545099663, 1.191235959310000148 ) ) ;
#2499=FACE_OUTER_BOUND ( 'NONE', #12871, .T. ) ;
#2504=EDGE_LOOP ( 'NONE', ( #26220, #44640, #7939, #2537, #53948 ) ) ;
#2516=CARTESIAN_POINT ( 'NONE',  ( 1.250000000000000000, -67.52659999995799467, 0.000000000000000000 ) ) ;
#2524=CARTESIAN_POINT ( 'NONE',  ( -1.310679582531389498, -78.95833333333335702, 0.7554284705563444335 ) ) ;
#2536=AXIS2_PLACEMENT_3D ( 'NONE', #50585, #23701, #41714 ) ;
#2537=ORIENTED_EDGE ( 'NONE', *, *, #24871, .T. ) ;
#2561=CARTESIAN_POINT ( 'NONE',  ( -1.185397549814999785, -80.21598949493500186, -0.6110718436566999756 ) ) ;
#2574=CARTESIAN_POINT ( 'NONE',  ( 0.1963495408493638184, -77.63541666666668561, -1.499999999999999778 ) ) ;
#2576=CARTESIAN_POINT ( 'NONE',  ( -1.500000000000000000, -78.00000000000000000, 0.000000000000000000 ) ) ;
#2590=CARTESIAN_POINT ( 'NONE',  ( -0.4104034600731000237, -81.14228670038500013, 1.244744919973999941 ) ) ;
#2597=CARTESIAN_POINT ( 'NONE',  ( 0.6980205241115000625, -79.83136847860799890, 1.456015547280999911 ) ) ;
#2613=DIRECTION ( 'NONE',  ( 0.000000000000000000, -1.000000000000000000, 0.000000000000000000 ) ) ;
#2617=ORIENTED_EDGE ( 'NONE', *, *, #9555, .F. ) ;
#2618=CARTESIAN_POINT ( 'NONE',  ( -0.5434382620641865502, -79.24014818529076365, -1.152742929317775777 ) ) ;
#2622=CARTESIAN_POINT ( 'NONE',  ( 1.500000000000000000, -80.65000000000000568, 0.000000000000000000 ) ) ;
#2623=CARTESIAN_POINT ( 'NONE',  ( 1.500000000000000000, -81.15000000000000568, 0.000000000000000000 ) ) ;
#2651=CARTESIAN_POINT ( 'NONE',  ( -0.6498089757737999239, -78.15792523368020284, 1.148178518287000127 ) ) ;
#2668=DIRECTION ( 'NONE',  ( -1.000000000000000000, 0.000000000000000000, 0.000000000000000000 ) ) ;
#2701=CARTESIAN_POINT ( 'NONE',  ( -0.3164422402712000482, -79.69022655590600834, 1.381999876370000102 ) ) ;
#2703=CARTESIAN_POINT ( 'NONE',  ( 1.391768007815999963, -77.76484642788379631, -0.6016011292324999760 ) ) ;
#2718=CARTESIAN_POINT ( 'NONE',  ( 1.309259533489598670, -78.51346957102681756, 0.2203786214735808102 ) ) ;
#2727=CARTESIAN_POINT ( 'NONE',  ( -0.9820397338569999413, -80.70308451575900222, -0.7733679338621000099 ) ) ;
#2751=ORIENTED_EDGE ( 'NONE', *, *, #16332, .T. ) ;
#2773=LINE ( 'NONE', #29614, #29892 ) ;
#2783=CARTESIAN_POINT ( 'NONE',  ( -0.3862712429687000237, -82.25000000000000000, -1.188820645369000006 ) ) ;
#2801=CARTESIAN_POINT ( 'NONE',  ( -0.3926218265389190276, -80.10416666666667140, -1.460959015002473826 ) ) ;
#2812=CARTESIAN_POINT ( 'NONE',  ( -1.500000000000000888, -78.98958333333331439, 0.1963495408493559080 ) ) ;
#2815=CARTESIAN_POINT ( 'NONE',  ( -1.500000000000000000, -80.91769483858634260, -0.3335398494528040159 ) ) ;
#2831=DIRECTION ( 'NONE',  ( 0.000000000000000000, 1.000000000000000000, 0.000000000000000000 ) ) ;
#2845=FACE_OUTER_BOUND ( 'NONE', #49797, .T. ) ;
#2847=CARTESIAN_POINT ( 'NONE',  ( -0.4872545538094000261, -79.27334965069501038, -1.241463230931000084 ) ) ;
#2860=CARTESIAN_POINT ( 'NONE',  ( 1.310679582531387943, -77.70833333333332860, -0.7554284705563468760 ) ) ;
#2862=CARTESIAN_POINT ( 'NONE',  ( 1.199500263597271577, -80.59791666666667709, -0.9218200799623702535 ) ) ;
#2871=CARTESIAN_POINT ( 'NONE',  ( -1.034297989014000052, -81.18931145362199686, 0.8050146651342000581 ) ) ;
#2881=CARTESIAN_POINT ( 'NONE',  ( -1.026216979225322623, -82.21744791666523611, 0.7875855714864156143 ) ) ;
#2892=CARTESIAN_POINT ( 'NONE',  ( -1.250000000000000000, -67.52659999995799467, 0.000000000000000000 ) ) ;
#2896=ORIENTED_EDGE ( 'NONE', *, *, #26131, .T. ) ;
#2956=B_SPLINE_SURFACE_WITH_KNOTS ( 'NONE', 3, 3, ( 
 ( #9575, #13105, #44411, #53271, #457, #49137, #27559, #44712, #22261, #27271, #12819, #745, #40276, #58287, #4858, #3964, #40866, #45308, #18143, #54454, #13990, #36139, #35239, #54156, #31400, #17850, #22855, #36428, #30817, #35838, #23145, #53866, #48850, #8394, #26390 ),
 ( #21966, #8991, #22564, #169, #13698, #31692, #33151, #36719, #24606, #14570, #32563, #46779, #27849, #24316, #51196, #1600, #37884, #55906, #19592, #42618, #37591, #14859, #19014, #10751, #28727, #18725, #50612, #6303, #23436, #42331, #1899, #19891, #10161, #14276, #15460 ),
 ( #29027, #33449, #55314, #50319, #23724, #45894, #47066, #54733, #51487, #55609, #11045, #15157, #6595, #32274, #28138, #32854, #9868, #41448, #5426, #1032, #6008, #42032, #37007, #55024, #46482, #24015, #46192, #5716, #41736, #1315, #19309, #10449, #37298, #50901, #28434 ),
 ( #31604, #22470, #27764, #40482, #45807, #77, #9192, #14484, #31897, #4763, #944, #18926, #9486, #50520, #10073, #46102, #51397, #20664, #24224, #7088, #32768, #50815, #20379, #33934, #10952, #38086, #28342, #28933, #10358, #46393, #41943, #47266, #24514, #15067, #20097 ) ),
 .UNSPECIFIED., .F., .F., .F.,
 ( 4, 4 ),
 ( 4, 1, 1, 1, 1, 1, 1, 1, 1, 1, 1, 1, 1, 1, 1, 1, 1, 1, 1, 1, 1, 1, 1, 1, 1, 1, 1, 1, 1, 1, 1, 1, 4 ),
 ( -0.05371687727927999811, 1.053716877278999986 ),
 ( -0.02000000000000000042, 0.01250000000000000069, 0.04499999999999999833, 0.07749999999999999944, 0.1100000000000000006, 0.1424999999999999878, 0.1749999999999999889, 0.2074999999999999900, 0.2399999999999999911, 0.2725000000000000200, 0.3049999999999999933, 0.3375000000000000222, 0.3699999999999999956, 0.4025000000000000244, 0.4349999999999999978, 0.4675000000000000266, 0.5000000000000000000, 0.5324999999999999734, 0.5649999999999999467, 0.5975000000000000311, 0.6300000000000000044, 0.6624999999999999778, 0.6949999999999999512, 0.7275000000000000355, 0.7600000000000000089, 0.7924999999999999822, 0.8249999999999999556, 0.8575000000000000400, 0.8900000000000000133, 0.9224999999999999867, 0.9549999999999999600, 0.9875000000000000444, 1.020000000000000018 ),
 .UNSPECIFIED. ) ;
#2981=CARTESIAN_POINT ( 'NONE',  ( -0.6438247211726000341, -80.38480328324099844, -1.263150469460000203 ) ) ;
#2984=CARTESIAN_POINT ( 'NONE',  ( -1.071041487988000140, -79.10438725917299507, -0.9340865940840999970 ) ) ;
#2986=DIRECTION ( 'NONE',  ( 0.000000000000000000, 1.000000000000000000, 0.000000000000000000 ) ) ;
#2992=CARTESIAN_POINT ( 'NONE',  ( -1.417334032777999964, -79.42654225787899236, -0.4910847579886000736 ) ) ;
#3001=EDGE_CURVE ( 'NONE', #43048, #19498, #15143, .T. ) ;
#3004=CARTESIAN_POINT ( 'NONE',  ( 0.3719284678543265388, -79.10182967317921054, 1.219176263759028878 ) ) ;
#3011=CARTESIAN_POINT ( 'NONE',  ( 0.7671735781280533129, -80.97340970725861098, 1.017801935282923287 ) ) ;
#3066=CARTESIAN_POINT ( 'NONE',  ( -0.5959590523698999887, -82.22858541388899312, -1.119253685964999967 ) ) ;
#3090=CARTESIAN_POINT ( 'NONE',  ( 0.1963495408493638184, -80.13541666666668561, -1.499999999999999778 ) ) ;
#3106=B_SPLINE_CURVE_WITH_KNOTS ( 'NONE', 3,
 ( #44072, #3621, #22204, #40215, #21627, #39632, #57639, #12762, #35183, #8337, #9223, #36660, #5656, #54678, #14513, #22795, #50549, #19535 ),
 .UNSPECIFIED., .F., .F.,
 ( 4, 2, 2, 2, 2, 2, 2, 2, 4 ),
 ( 0.000000000000000000, 0.1250000000000000833, 0.2500000000000001665, 0.3750000000000001665, 0.5000000000000002220, 0.6250000000000002220, 0.7500000000000001110, 0.8750000000000001110, 1.000000000000000000 ),
 .UNSPECIFIED. ) ;
#3155=CARTESIAN_POINT ( 'NONE',  ( -1.297058042903999953, -81.19679289562199642, -0.3101879797029999941 ) ) ;
#3171=CARTESIAN_POINT ( 'NONE',  ( -1.606812318740999945, -79.48408011494099412, 0.1592736582230999953 ) ) ;
#3221=CARTESIAN_POINT ( 'NONE',  ( -1.460959015002474937, -80.97916666666665719, 0.3926218265389144757 ) ) ;
#3226=ORIENTED_EDGE ( 'NONE', *, *, #981, .T. ) ;
#3273=CARTESIAN_POINT ( 'NONE',  ( 0.1998609718125000101, -80.37904421889498963, -1.304078681214000168 ) ) ;
#3275=CARTESIAN_POINT ( 'NONE',  ( 0.1534498121882000021, -77.96905598575500562, 1.409436946036999760 ) ) ;
#3293=CARTESIAN_POINT ( 'NONE',  ( 1.224548907347106752, -79.02232155126675650, 0.3527677417113336267 ) ) ;
#3299=CARTESIAN_POINT ( 'NONE',  ( -1.122584031195864362, -81.68897639063932559, -0.6023342644404590107 ) ) ;
#3302=CARTESIAN_POINT ( 'NONE',  ( -0.3926218265389256890, -79.29583333333334849, 1.460959015002472050 ) ) ;
#3326=EDGE_CURVE ( 'NONE', #6234, #23510, #39605, .T. ) ;
#3330=ORIENTED_EDGE ( 'NONE', *, *, #34450, .F. ) ;
#3333=CARTESIAN_POINT ( 'NONE',  ( 1.500000000000000000, -81.75000000000000000, 0.000000000000000000 ) ) ;
#3339=ORIENTED_EDGE ( 'NONE', *, *, #26131, .F. ) ;
#3377=CARTESIAN_POINT ( 'NONE',  ( -1.250000000001000089, -82.24999999999900524, 4.142826023433999917E-11 ) ) ;
#3380=B_SPLINE_SURFACE_WITH_KNOTS ( 'NONE', 3, 3, ( 
 ( #20504, #38500, #16076, #34056 ),
 ( #58251, #13067, #31065, #8953 ),
 ( #21928, #44094, #3643, #49103 ),
 ( #36102, #12500, #26937, #12782 ) ),
 .UNSPECIFIED., .F., .F., .F.,
 ( 4, 4 ),
 ( 4, 4 ),
 ( -0.1566102636784000024, 0.3603425273004000062 ),
 ( -0.0006517983049530999724, 0.01399779397395000020 ),
 .UNSPECIFIED. ) ;
#3393=DIRECTION ( 'NONE',  ( 0.000000000000000000, -1.000000000000000000, 0.000000000000000000 ) ) ;
#3415=PLANE ( 'NONE',  #11724 ) ;
#3431=CARTESIAN_POINT ( 'NONE',  ( -0.9315676299678438133, -79.69017609249064549, 0.8708394447951318673 ) ) ;
#3435=CARTESIAN_POINT ( 'NONE',  ( 0.8962411872155999770, -81.49446863590900136, 0.9875868993909000526 ) ) ;
#3438=CARTESIAN_POINT ( 'NONE',  ( 0.9186508726441414696, -79.57551408595966791, -1.236643120628077241 ) ) ;
#3448=CARTESIAN_POINT ( 'NONE',  ( 1.275615568647000098, -80.38862546449399815, 0.6187600927687999519 ) ) ;
#3449=ORIENTED_EDGE ( 'NONE', *, *, #21568, .F. ) ;
#3469=CARTESIAN_POINT ( 'NONE',  ( 1.058112158932194902, -79.44686744937848744, 0.7105453803691499370 ) ) ;
#3474=CARTESIAN_POINT ( 'NONE',  ( -1.500000000000000444, -78.38958333333333428, 0.1963495408493560745 ) ) ;
#3498=CARTESIAN_POINT ( 'NONE',  ( -0.7554284705563544255, -80.91666666666667140, 1.310679582531384169 ) ) ;
#3501=CARTESIAN_POINT ( 'NONE',  ( 1.301001062148999798, -78.50521359734798921, 0.2190019327816999928 ) ) ;
#3521=CARTESIAN_POINT ( 'NONE',  ( -0.1963495408493606265, -78.51458333333334849, -1.500000000000000222 ) ) ;
#3552=CARTESIAN_POINT ( 'NONE',  ( -0.1680659145979999936, -80.62710733580000522, 1.308557476745999981 ) ) ;
#3555=CARTESIAN_POINT ( 'NONE',  ( -1.305945605467999870, -78.66939177743699929, -0.1872743590209999809 ) ) ;
#3565=B_SPLINE_CURVE_WITH_KNOTS ( 'NONE', 3,
 ( #40388, #54844, #50432, #14390, #27385, #40082, #45127, #49851, #53976, #31809, #32388, #13216, #45421, #13515, #23261, #40688, #35648, #4963 ),
 .UNSPECIFIED., .F., .F.,
 ( 4, 2, 2, 2, 2, 2, 2, 2, 4 ),
 ( 0.000000000000000000, 0.1249999999999999722, 0.2499999999999999445, 0.3749999999999998890, 0.4999999999999998890, 0.6249999999999998890, 0.7499999999999997780, 0.8749999999999998890, 1.000000000000000000 ),
 .UNSPECIFIED. ) ;
#3581=CARTESIAN_POINT ( 'NONE',  ( 1.499999999999999778, -79.16041666666667709, 0.1963495408493654004 ) ) ;
#3611=CARTESIAN_POINT ( 'NONE',  ( 1.460959015002472494, -81.77083333333453652, 0.3926218265389233020 ) ) ;
#3621=CARTESIAN_POINT ( 'NONE',  ( -1.500000000000000888, -77.98958333333332860, 0.1963495408493559080 ) ) ;
#3636=DIRECTION ( 'NONE',  ( 0.000000000000000000, 1.000000000000000000, 0.000000000000000000 ) ) ;
#3643=CARTESIAN_POINT ( 'NONE',  ( -0.4831833036036000117, -82.26234308346199953, -1.158768654956999988 ) ) ;
#3693=FACE_OUTER_BOUND ( 'NONE', #2016, .T. ) ;
#3696=CARTESIAN_POINT ( 'NONE',  ( -1.327128730425999992, -79.71402465532199244, 0.1315503032697999675 ) ) ;
#3714=CARTESIAN_POINT ( 'NONE',  ( -1.136758720370837805, -80.78738817488307689, -0.5771817327056680824 ) ) ;
#3719=CARTESIAN_POINT ( 'NONE',  ( 0.08638142328466999476, -81.09172904305800955, 1.330832257483999914 ) ) ;
#3734=CARTESIAN_POINT ( 'NONE',  ( -1.016909733597999965, -80.04133710082599862, 0.9879038282509999824 ) ) ;
#3741=ORIENTED_EDGE ( 'NONE', *, *, #17449, .F. ) ;
#3752=DIRECTION ( 'NONE',  ( -1.000000000000000000, 0.000000000000000000, 0.000000000000000000 ) ) ;
#3757=CARTESIAN_POINT ( 'NONE',  ( 0.8974734542577849084, -80.33735043314219126, -0.9053192546341672919 ) ) ;
#3772=CARTESIAN_POINT ( 'NONE',  ( -1.149697912616226558, -81.29158079410925097, -0.6590062889063229568 ) ) ;
#3776=CARTESIAN_POINT ( 'NONE',  ( -0.1356420093736999954, -78.02636455657749082, -1.608970710047999964 ) ) ;
#3809=CARTESIAN_POINT ( 'NONE',  ( 0.000000000000000000, -82.50000000000000000, 0.000000000000000000 ) ) ;
#3823=ORIENTED_EDGE ( 'NONE', *, *, #25570, .F. ) ;
#3840=CARTESIAN_POINT ( 'NONE',  ( 0.6275421466603999798, -80.57749471241899641, 1.160498354042999836 ) ) ;
#3841=CARTESIAN_POINT ( 'NONE',  ( -0.5351185351402000245, -79.06629276448599342, 1.205899990410000067 ) ) ;
#3867=CARTESIAN_POINT ( 'NONE',  ( 0.1963495408493571848, -79.26458333333334849, 1.500000000000000666 ) ) ;
#3902=ORIENTED_EDGE ( 'NONE', *, *, #15168, .F. ) ;
#3963=ADVANCED_FACE ( 'NONE', ( #53311 ), #42106, .T. ) ;
#3964=CARTESIAN_POINT ( 'NONE',  ( 1.478892026253000092, -81.20907286634400180, -0.6481452774650000581 ) ) ;
#3983=CARTESIAN_POINT ( 'NONE',  ( 1.329937235669000017, -79.50973555599499321, -0.09921221311570001256 ) ) ;
#3999=CARTESIAN_POINT ( 'NONE',  ( 1.058402703809858236, -79.54706147304830210, 0.7107250344689944876 ) ) ;
#4003=CARTESIAN_POINT ( 'NONE',  ( -0.6509962010243000030, -81.63746790025000166, 1.163950211895000031 ) ) ;
#4012=CARTESIAN_POINT ( 'NONE',  ( 1.267480381879000140, -81.47145997305000265, -0.3336381545036999907 ) ) ;
#4017=CARTESIAN_POINT ( 'NONE',  ( -1.327188084842999993, -79.09869725658599293, 0.06657717027841000834 ) ) ;
#4021=CARTESIAN_POINT ( 'NONE',  ( -0.6565412214492993837, -82.19791666666498031, 1.137416565959658232 ) ) ;
#4040=ORIENTED_EDGE ( 'NONE', *, *, #46328, .F. ) ;
#4044=LINE ( 'NONE', #45094, #2011 ) ;
#4052=CARTESIAN_POINT ( 'NONE',  ( 0.7554284705563509839, -80.06666666666669130, -1.310679582531386167 ) ) ;
#4058=CARTESIAN_POINT ( 'NONE',  ( 0.6416220162505898994, -80.91538276820625697, -1.159482954178659320 ) ) ;
#4072=CARTESIAN_POINT ( 'NONE',  ( -1.344169958103999862, -78.81440746632799232, 0.7015335173854999606 ) ) ;
#4074=SHAPE_REPRESENTATION ( 'Security screw', ( #43526 ), #6767 ) ;
#4091=DIRECTION ( 'NONE',  ( 0.000000000000000000, 1.000000000000000000, 0.000000000000000000 ) ) ;
#4094=VECTOR ( 'NONE', #4091, 1000.000000000000000 ) ;
#4130=CARTESIAN_POINT ( 'NONE',  ( -1.211530263941000163, -79.85058255474299926, 1.067430724879000037 ) ) ;
#4132=CARTESIAN_POINT ( 'NONE',  ( -0.6498089757737999239, -78.07404029686399838, 1.148178518287000127 ) ) ;
#4192=VERTEX_POINT ( 'NONE', #41194 ) ;
#4207=DIRECTION ( 'NONE',  ( 0.000000000000000000, 1.000000000000000000, 0.000000000000000000 ) ) ;
#4213=CARTESIAN_POINT ( 'NONE',  ( -0.3862712429687000237, -82.25000000000000000, -1.188820645369000006 ) ) ;
#4271=CARTESIAN_POINT ( 'NONE',  ( 1.500000000000000000, -78.25000000000000000, 0.000000000000000000 ) ) ;
#4282=CARTESIAN_POINT ( 'NONE',  ( -0.4872545538094000261, -79.36089768585199522, -1.241463230931000084 ) ) ;
#4298=CARTESIAN_POINT ( 'NONE',  ( 0.7897348250228778399, -80.07181507767086259, 1.000737493962424507 ) ) ;
#4303=CARTESIAN_POINT ( 'NONE',  ( 1.289124607492999841, -80.94872977871700925, 0.3416633729347999804 ) ) ;
#4312=CARTESIAN_POINT ( 'NONE',  ( -0.1286311518798999853, -80.97088155641299068, -1.500807616117999954 ) ) ;
#4319=CARTESIAN_POINT ( 'NONE',  ( -0.3384184472371999930, -79.44022655590600834, 1.477976681755000188 ) ) ;
#4322=CARTESIAN_POINT ( 'NONE',  ( 0.1963495408493637351, -79.03541666666667709, -1.499999999999999778 ) ) ;
#4340=CARTESIAN_POINT ( 'NONE',  ( 0.3859110462609495196, -82.02864582858185827, -1.432732671933543811 ) ) ;
#4342=CARTESIAN_POINT ( 'NONE',  ( -0.9313275411143693283, -79.58998078605505100, 0.8705974481289671107 ) ) ;
#4361=CARTESIAN_POINT ( 'NONE',  ( -0.9820397338569999413, -80.80308451575899653, -0.7733679338621000099 ) ) ;
#4364=EDGE_CURVE ( 'NONE', #900, #32341, #55438, .T. ) ;
#4376=CARTESIAN_POINT ( 'NONE',  ( 1.360845176917000021, -78.56634434942300516, -0.6686124113221000309 ) ) ;
#4394=CARTESIAN_POINT ( 'NONE',  ( 0.000000000000000000, -77.50000000000000000, 0.000000000000000000 ) ) ;
#4400=DIRECTION ( 'NONE',  ( 0.000000000000000000, 1.000000000000000000, 0.000000000000000000 ) ) ;
#4429=CARTESIAN_POINT ( 'NONE',  ( 1.416781233620999947, -80.19787091841099880, 0.7745610770380000343 ) ) ;
#4432=CARTESIAN_POINT ( 'NONE',  ( -1.178447680628000205, -80.55308451575899653, -0.9280415206345000723 ) ) ;
#4576=EDGE_LOOP ( 'NONE', ( #27409, #54589, #29028, #21262 ) ) ;
#4577=ORIENTED_EDGE ( 'NONE', *, *, #41177, .T. ) ;
#4580=CARTESIAN_POINT ( 'NONE',  ( -1.213636094208999872, -80.75588974632400152, -0.5527192377158001158 ) ) ;
#4598=CARTESIAN_POINT ( 'NONE',  ( -1.159125165887999964, -77.73513018121029461, 0.4678983327651999868 ) ) ;
#4600=CARTESIAN_POINT ( 'NONE',  ( -0.6747260877994001316, -82.22962677363800310, -1.052256958371999840 ) ) ;
#4603=CARTESIAN_POINT ( 'NONE',  ( 1.169602984591961103, -80.53296218476353374, 0.5073077260901295293 ) ) ;
#4607=CARTESIAN_POINT ( 'NONE',  ( -0.5935892672256000147, -82.17736815163898711, 1.194249225580000129 ) ) ;
#4616=CARTESIAN_POINT ( 'NONE',  ( 0.3790021828235000112, -81.15063363487499259, 1.356521486386000230 ) ) ;
#4622=CARTESIAN_POINT ( 'NONE',  ( 1.112922243992000126, -79.73790229619299907, -1.029731144982999780 ) ) ;
#4642=CARTESIAN_POINT ( 'NONE',  ( 1.500000000000000000, -81.65000000000000568, 0.000000000000000000 ) ) ;
#4648=CARTESIAN_POINT ( 'NONE',  ( 1.500000000000000000, -77.50000000000000000, 0.000000000000000000 ) ) ;
#4665=CARTESIAN_POINT ( 'NONE',  ( -0.4149502389179186013, -81.15050653439624284, 1.258535203000175295 ) ) ;
#4680=CARTESIAN_POINT ( 'NONE',  ( -0.9728543758959999899, -78.36213479155139794, -1.031316509929999903 ) ) ;
#4698=CARTESIAN_POINT ( 'NONE',  ( 1.500000000000000000, -81.65000000000000568, 0.000000000000000000 ) ) ;
#4727=CARTESIAN_POINT ( 'NONE',  ( -1.487176594838000021, -80.83707595801799073, 0.2955346688291999868 ) ) ;
#4736=CARTESIAN_POINT ( 'NONE',  ( 0.000000000000000000, -76.15000000005198899, 0.000000000000000000 ) ) ;
#4740=CARTESIAN_POINT ( 'NONE',  ( -1.500000000000000000, -80.50000000000000000, 0.000000000000000000 ) ) ;
#4758=EDGE_CURVE ( 'NONE', #43330, #15471, #11791, .T. ) ;
#4763=CARTESIAN_POINT ( 'NONE',  ( -0.6992687060550999423, -81.07751218924100556, 1.118744323162000009 ) ) ;
#4788=ADVANCED_FACE ( 'NONE', ( #48107 ), #56878, .F. ) ;
#4812=LINE ( 'NONE', #5387, #11801 ) ;
#4828=CARTESIAN_POINT ( 'NONE',  ( 1.500000000000000000, -79.65000000000000568, 0.000000000000000000 ) ) ;
#4833=EDGE_CURVE ( 'NONE', #44267, #28437, #28775, .T. ) ;
#4849=CARTESIAN_POINT ( 'NONE',  ( 1.012234255459822041, -77.95212815520520167, 0.7735125553324427861 ) ) ;
#4858=CARTESIAN_POINT ( 'NONE',  ( 0.8222529417517999706, -81.15946024296299299, -1.389645287737000245 ) ) ;
#4875=CARTESIAN_POINT ( 'NONE',  ( 0.2020314717676000016, -80.35898875927600216, -1.318241039644999946 ) ) ;
#4888=CARTESIAN_POINT ( 'NONE',  ( -0.2406813341972999787, -78.83244650139599230, -1.311734976874999958 ) ) ;
#4907=CARTESIAN_POINT ( 'NONE',  ( 2.799999999997999645, -75.99999999999900524, 5.978114955471999489E-11 ) ) ;
#4908=CARTESIAN_POINT ( 'NONE',  ( 1.238425546590999904, -81.51848472628699938, 0.4290956794724000156 ) ) ;
#4914=CARTESIAN_POINT ( 'NONE',  ( -1.294028136707999987, -80.64244764574600310, 0.2571518259264999884 ) ) ;
#4933=CARTESIAN_POINT ( 'NONE',  ( -0.9820397338569999413, -80.70308451575900222, -0.7733679338621000099 ) ) ;
#4934=VECTOR ( 'NONE', #48228, 1000.000000000000114 ) ;
#4944=CARTESIAN_POINT ( 'NONE',  ( -0.5470841013496000604, -79.72570186692699679, -1.216254552179000026 ) ) ;
#4953=DIRECTION ( 'NONE',  ( 1.000000000000000000, 0.000000000000000000, 0.000000000000000000 ) ) ;
#4963=CARTESIAN_POINT ( 'NONE',  ( -1.500000000000000000, -79.90000000000000568, 0.000000000000000000 ) ) ;
#4983=CARTESIAN_POINT ( 'NONE',  ( -0.1963495408493606265, -81.51458333333333428, -1.500000000000000222 ) ) ;
#4985=DIRECTION ( 'NONE',  ( 0.000000000000000000, 1.000000000000000000, 0.000000000000000000 ) ) ;
#4991=AXIS2_PLACEMENT_3D ( 'NONE', #48751, #26877, #5329 ) ;
#4996=ORIENTED_EDGE ( 'NONE', *, *, #5956, .F. ) ;
#5012=CARTESIAN_POINT ( 'NONE',  ( 1.364204221418999774, -80.63862546449399815, 0.6617315995101000770 ) ) ;
#5063=CARTESIAN_POINT ( 'NONE',  ( 0.7554284705563509839, -81.16666666666668561, -1.310679582531385945 ) ) ;
#5068=VERTEX_POINT ( 'NONE', #28244 ) ;
#5128=CARTESIAN_POINT ( 'NONE',  ( -1.500000000000000222, -79.51041666666668561, -0.1963495408493622085 ) ) ;
#5158=FACE_OUTER_BOUND ( 'NONE', #50892, .T. ) ;
#5159=DIRECTION ( 'NONE',  ( 0.000000000000000000, -1.000000000000000000, 0.000000000000000000 ) ) ;
#5175=CARTESIAN_POINT ( 'NONE',  ( 0.9384621721472999889, -78.53477076110999633, 0.9475573338641000154 ) ) ;
#5196=CARTESIAN_POINT ( 'NONE',  ( 0.1847432000700000021, -81.43278215430200362, -1.396303359803000133 ) ) ;
#5203=CARTESIAN_POINT ( 'NONE',  ( -1.460959015002474937, -81.47916666666665719, 0.3926218265389144757 ) ) ;
#5206=CARTESIAN_POINT ( 'NONE',  ( -1.500000000000000222, -78.91041666666666288, -0.1963495408493622363 ) ) ;
#5255=CARTESIAN_POINT ( 'NONE',  ( -1.317826160292999926, -77.82215499870639519, 0.5319603796220000458 ) ) ;
#5257=ORIENTED_EDGE ( 'NONE', *, *, #17405, .F. ) ;
#5263=CARTESIAN_POINT ( 'NONE',  ( 0.9218200799623742503, -81.67708333333332860, -1.199500263597268912 ) ) ;
#5274=CARTESIAN_POINT ( 'NONE',  ( -1.256362333281000110, -77.62034566960160475, 0.2270125678640999844 ) ) ;
#5279=VERTEX_POINT ( 'NONE', #10759 ) ;
#5301=CARTESIAN_POINT ( 'NONE',  ( -0.3603946542032999689, -79.80096993136200467, 1.573953487139999829 ) ) ;
#5329=DIRECTION ( 'NONE',  ( 0.000000000000000000, 0.000000000000000000, 1.000000000000000000 ) ) ;
#5347=CARTESIAN_POINT ( 'NONE',  ( 1.310679582531387943, -81.20833333333331439, -0.7554284705563468760 ) ) ;
#5373=CARTESIAN_POINT ( 'NONE',  ( 1.577356090230000119, -77.75908736353699169, 0.3451975780249000314 ) ) ;
#5387=CARTESIAN_POINT ( 'NONE',  ( 3.999999999993000266, -77.30000000000720206, -8.632702228606999814E-11 ) ) ;
#5409=CARTESIAN_POINT ( 'NONE',  ( -0.3926218265389190276, -79.60416666666668561, -1.460959015002473826 ) ) ;
#5425=VERTEX_POINT ( 'NONE', #50038 ) ;
#5426=CARTESIAN_POINT ( 'NONE',  ( 0.1605656202615999839, -81.46865411194299611, 1.408644050778000034 ) ) ;
#5442=CARTESIAN_POINT ( 'NONE',  ( 0.000000000000000000, -82.50000000000000000, 0.000000000000000000 ) ) ;
#5461=CARTESIAN_POINT ( 'NONE',  ( 1.315129997485000146, -78.52893215530700388, 0.2213803045116000123 ) ) ;
#5477=CARTESIAN_POINT ( 'NONE',  ( -0.6678841138425000157, -81.44112908879199608, -1.350122867467000054 ) ) ;
#5501=ORIENTED_EDGE ( 'NONE', *, *, #25525, .T. ) ;
#5516=CARTESIAN_POINT ( 'NONE',  ( 1.313995274498999999, -80.37066597088099229, -0.2280190045613000038 ) ) ;
#5525=CARTESIAN_POINT ( 'NONE',  ( -0.4635254915625000027, -82.00000000000000000, -1.426584774443000025 ) ) ;
#5534=EDGE_CURVE ( 'NONE', #54221, #5753, #42921, .T. ) ;
#5535=CARTESIAN_POINT ( 'NONE',  ( 1.500000000000000000, -80.25000000000000000, 0.000000000000000000 ) ) ;
#5555=DIRECTION ( 'NONE',  ( 0.000000000000000000, 0.7071067811866525998, -0.7071067811864425456 ) ) ;
#5558=CARTESIAN_POINT ( 'NONE',  ( -1.460959015002473826, -81.42083333333336270, -0.3926218265389207485 ) ) ;
#5629=DIRECTION ( 'NONE',  ( 1.140590214241074934E-08, -0.7071067811865474617, -0.7071067811865474617 ) ) ;
#5636=EDGE_LOOP ( 'NONE', ( #30724, #42187, #30547, #46852 ) ) ;
#5645=CARTESIAN_POINT ( 'NONE',  ( 0.3926218265389159745, -80.25416666666666288, 1.460959015002474493 ) ) ;
#5655=CARTESIAN_POINT ( 'NONE',  ( -1.235017835984000056, -79.23795388112999660, 0.06195353447049999768 ) ) ;
#5656=CARTESIAN_POINT ( 'NONE',  ( 0.9218200799623694763, -77.82291666666667140, 1.199500263597272465 ) ) ;
#5701=CARTESIAN_POINT ( 'NONE',  ( 1.500000000000000000, -78.75000000000000000, 0.000000000000000000 ) ) ;
#5716=CARTESIAN_POINT ( 'NONE',  ( 1.002739805183000099, -81.91516772237299904, 1.002283400281000159 ) ) ;
#5731=CARTESIAN_POINT ( 'NONE',  ( 1.500000000000000000, -79.26041666666669983, 0.1963495408493652339 ) ) ;
#5748=CARTESIAN_POINT ( 'NONE',  ( 1.302799686710000016, -77.98903190391820317, 0.2851120931344000020 ) ) ;
#5753=VERTEX_POINT ( 'NONE', #41464 ) ;
#5757=VECTOR ( 'NONE', #19083, 1000.000000000000114 ) ;
#5766=CARTESIAN_POINT ( 'NONE',  ( -0.3614649557311000461, -81.95840137440799822, -1.462273585377000140 ) ) ;
#5774=CARTESIAN_POINT ( 'NONE',  ( -0.6144861720749000833, -80.74167289250799229, -1.073086222052999972 ) ) ;
#5812=EDGE_CURVE ( 'NONE', #42334, #15713, #15477, .T. ) ;
#5847=CARTESIAN_POINT ( 'NONE',  ( -1.250000000000000000, -76.50000000000000000, 0.000000000000000000 ) ) ;
#5849=CARTESIAN_POINT ( 'NONE',  ( -1.112801787005999854, -79.17487453554200272, -0.6258220204580999813 ) ) ;
#5935=DIRECTION ( 'NONE',  ( 0.000000000000000000, -1.000000000000000000, 0.000000000000000000 ) ) ;
#5948=CARTESIAN_POINT ( 'NONE',  ( -0.2944660333051000167, -79.63485486817799597, 1.286023070983999927 ) ) ;
#5950=CARTESIAN_POINT ( 'NONE',  ( -1.607511835558000035, -78.99940294806400232, -0.1512538100690999920 ) ) ;
#5956=EDGE_CURVE ( 'NONE', #39914, #22868, #25101, .T. ) ;
#5968=CARTESIAN_POINT ( 'NONE',  ( 0.4989225658573747113, -78.59297769293915792, 1.172947819115397916 ) ) ;
#5987=CARTESIAN_POINT ( 'NONE',  ( -0.7554284705563480973, -79.58333333333334281, -1.310679582531387277 ) ) ;
#5988=AXIS2_PLACEMENT_3D ( 'NONE', #52225, #15916, #35047 ) ;
#6000=CARTESIAN_POINT ( 'NONE',  ( 0.3926218265389221362, -78.04583333333334849, -1.460959015002473160 ) ) ;
#6008=CARTESIAN_POINT ( 'NONE',  ( -1.284296857402999814, -81.56787935870499950, 0.6005338976478999946 ) ) ;
#6038=CARTESIAN_POINT ( 'NONE',  ( 1.500000000000000000, -78.64999999999999147, 0.000000000000000000 ) ) ;
#6058=CARTESIAN_POINT ( 'NONE',  ( 0.7766715314972000295, -81.07327799737899454, -1.403532576748999894 ) ) ;
#6120=PLANE ( 'NONE',  #51241 ) ;
#6130=CARTESIAN_POINT ( 'NONE',  ( 0.000000000000000000, -75.67500000000001137, 0.000000000000000000 ) ) ;
#6131=CARTESIAN_POINT ( 'NONE',  ( -0.7554284705563480973, -81.58333333333332860, -1.310679582531387277 ) ) ;
#6144=CARTESIAN_POINT ( 'NONE',  ( -0.9151233253627000241, -78.19915960904749852, -0.9701162038759999495 ) ) ;
#6168=EDGE_CURVE ( 'NONE', #49068, #11615, #56213, .T. ) ;
#6208=LINE ( 'NONE', #47264, #32498 ) ;
#6211=CARTESIAN_POINT ( 'NONE',  ( 0.7276880389500910429, -78.47687705635108557, 1.046751526124253262 ) ) ;
#6234=VERTEX_POINT ( 'NONE', #18674 ) ;
#6235=DIRECTION ( 'NONE',  ( 0.000000000000000000, 0.000000000000000000, 1.000000000000000000 ) ) ;
#6240=CARTESIAN_POINT ( 'NONE',  ( -1.049525737143000015, -77.56063687001267226, -1.227116502697000122 ) ) ;
#6249=ADVANCED_FACE ( 'NONE', ( #45546 ), #19249, .T. ) ;
#6258=CARTESIAN_POINT ( 'NONE',  ( -0.2498055603741706487, -78.64068256608658203, 1.249787055701736316 ) ) ;
#6267=CARTESIAN_POINT ( 'NONE',  ( 0.2153359604882000011, -82.12775552825800673, 1.316133176457000120 ) ) ;
#6276=ORIENTED_EDGE ( 'NONE', *, *, #34608, .T. ) ;
#6303=CARTESIAN_POINT ( 'NONE',  ( 1.072377845517999972, -81.85979603464500087, 1.071889744314999948 ) ) ;
#6335=CARTESIAN_POINT ( 'NONE',  ( 0.5704417986824000808, -78.92583314235599801, -1.205475954488999912 ) ) ;
#6353=CARTESIAN_POINT ( 'NONE',  ( -0.1369841977586999937, -81.02625324414100305, -1.598267016032999921 ) ) ;
#6396=CARTESIAN_POINT ( 'NONE',  ( -0.4872545538094000261, -79.31712366827299832, -1.241463230931000084 ) ) ;
#6398=CARTESIAN_POINT ( 'NONE',  ( 0.000000000000000000, -82.25000000001401190, 0.000000000000000000 ) ) ;
#6411=CARTESIAN_POINT ( 'NONE',  ( -0.8218343019581000330, -80.70650526761399135, -1.050237832603999832 ) ) ;
#6429=CARTESIAN_POINT ( 'NONE',  ( -1.158153954042000056, -79.93059372536998808, 1.125119257983999921 ) ) ;
#6436=CARTESIAN_POINT ( 'NONE',  ( 0.8912423865758999364, -77.99487050972069824, 0.9921004264782997684 ) ) ;
#6448=EDGE_CURVE ( 'NONE', #54221, #5425, #51183, .T. ) ;
#6464=CARTESIAN_POINT ( 'NONE',  ( -0.6744830649036911430, -82.23641784909204944, -1.051876958025935949 ) ) ;
#6513=DIRECTION ( 'NONE',  ( 0.000000000000000000, 1.000000000000000000, 0.000000000000000000 ) ) ;
#6519=PRODUCT_DEFINITION_FORMATION_WITH_SPECIFIED_SOURCE ( 'ANY', '', #8796, .NOT_KNOWN. ) ;
#6522=AXIS2_PLACEMENT_3D ( 'NONE', #48710, #38969, #30094 ) ;
#6536=UNCERTAINTY_MEASURE_WITH_UNIT (LENGTH_MEASURE( 1.000000000000000082E-05 ), #21532, 'distance_accuracy_value', 'NONE');
#6545=LINE ( 'NONE', #28971, #46939 ) ;
#6555=CARTESIAN_POINT ( 'NONE',  ( -0.9821332843717349714, -78.19543708337666033, 0.8118240402714035353 ) ) ;
#6563=CARTESIAN_POINT ( 'NONE',  ( 0.7435827448538506745, -81.97520306399145795, 1.034501988448051968 ) ) ;
#6565=CARTESIAN_POINT ( 'NONE',  ( 0.8471236057751000414, -81.08589043725500289, 1.030027924806000028 ) ) ;
#6576=CARTESIAN_POINT ( 'NONE',  ( -1.250000000000000000, -77.68333333333332291, 0.000000000000000000 ) ) ;
#6595=CARTESIAN_POINT ( 'NONE',  ( -0.9269474863677999998, -81.17097837165700014, -1.072766394601999851 ) ) ;
#6611=FILL_AREA_STYLE ('',( #33465 ) ) ;
#6647=CARTESIAN_POINT ( 'NONE',  ( -0.2424364941441000121, -82.24054989383500924, 1.486642543718000198 ) ) ;
#6666=EDGE_CURVE ( 'NONE', #49070, #11684, #16180, .T. ) ;
#6693=CARTESIAN_POINT ( 'NONE',  ( 1.199918086393000127, -80.46405261184000324, 0.5820416783086000967 ) ) ;
#6705=CARTESIAN_POINT ( 'NONE',  ( -0.1832406609208000192, -81.74837035861699519, -1.320984106490000087 ) ) ;
#6725=CARTESIAN_POINT ( 'NONE',  ( -0.5539667471886999817, -79.14255081561999816, -1.411437496924000001 ) ) ;
#6730=CARTESIAN_POINT ( 'NONE',  ( -1.309352690804000074, -78.19332100324500345, -0.2533212985548999874 ) ) ;
#6749=CARTESIAN_POINT ( 'NONE',  ( -1.500000000000000000, -77.50000000000000000, 0.000000000000000000 ) ) ;
#6753=CARTESIAN_POINT ( 'NONE',  ( -0.3926218265389256890, -81.29583333333334849, 1.460959015002472050 ) ) ;
#6767=( GEOMETRIC_REPRESENTATION_CONTEXT ( 3 ) GLOBAL_UNCERTAINTY_ASSIGNED_CONTEXT ( ( #6536 ) ) GLOBAL_UNIT_ASSIGNED_CONTEXT ( ( #21532, #57543, #35683 ) ) REPRESENTATION_CONTEXT ( 'NONE', 'WORKASPACE' ) );
#6772=CARTESIAN_POINT ( 'NONE',  ( -0.9218200799623716968, -78.57291666666667140, -1.199500263597270910 ) ) ;
#6797=CARTESIAN_POINT ( 'NONE',  ( -0.7620226540494657863, -81.98338008206076211, -1.329091872049480427 ) ) ;
#6799=CARTESIAN_POINT ( 'NONE',  ( 0.8552014154741368612, -78.33376371967493412, -0.9447217733863905176 ) ) ;
#6817=CARTESIAN_POINT ( 'NONE',  ( 1.500000000000000000, -79.76041666666669983, 0.1963495408493652339 ) ) ;
#6826=CARTESIAN_POINT ( 'NONE',  ( 0.7144648680787000217, -78.21136003831350081, -1.337341431498000111 ) ) ;
#6852=CARTESIAN_POINT ( 'NONE',  ( 0.9169854298989832397, -81.33914378987525140, -0.8846736303925517575 ) ) ;
#6889=CARTESIAN_POINT ( 'NONE',  ( 0.7554284705563453217, -81.83333333333801818, 1.310679582531389276 ) ) ;
#6909=CARTESIAN_POINT ( 'NONE',  ( -0.4980389805768000167, -82.22048152020499856, -1.194395492011000037 ) ) ;
#6916=CARTESIAN_POINT ( 'NONE',  ( 0.9218200799623692543, -78.72291666666667709, 1.199500263597272687 ) ) ;
#6917=CARTESIAN_POINT ( 'NONE',  ( -1.327706488546999797, -79.27312150602399754, -0.1249263990498000187 ) ) ;
#6932=CARTESIAN_POINT ( 'NONE',  ( 0.7554284705563509839, -80.16666666666667140, -1.310679582531385945 ) ) ;
#6964=ORIENTED_EDGE ( 'NONE', *, *, #41461, .T. ) ;
#6980=CARTESIAN_POINT ( 'NONE',  ( 0.9336649615752000697, -80.36482736507799984, -0.9522845488932000224 ) ) ;
#6989=CARTESIAN_POINT ( 'NONE',  ( -1.099495439336281688, -79.29263548292873054, -0.6453601205885236558 ) ) ;
#6994=CARTESIAN_POINT ( 'NONE',  ( 1.289124607492999841, -80.90495576113799814, 0.3416633729347999804 ) ) ;
#7006=CARTESIAN_POINT ( 'NONE',  ( 1.301773871033000018, -81.00121244067099724, 0.1523335971162000091 ) ) ;
#7012=CARTESIAN_POINT ( 'NONE',  ( -1.511528582562000178, -78.98795388112999660, 0.07582444189424000780 ) ) ;
#7043=CARTESIAN_POINT ( 'NONE',  ( -0.9218200799623778030, -78.32708333333337691, 1.199500263597266914 ) ) ;
#7063=CARTESIAN_POINT ( 'NONE',  ( -1.310679582531386611, -78.54166666666667140, -0.7554284705563495406 ) ) ;
#7078=DIRECTION ( 'NONE',  ( 0.000000000000000000, -1.000000000000000000, 0.000000000000000000 ) ) ;
#7080=CARTESIAN_POINT ( 'NONE',  ( -1.181111693982000110, -79.27654225787900089, -0.4092372983238000139 ) ) ;
#7088=CARTESIAN_POINT ( 'NONE',  ( -0.6440023044164000510, -81.57363842305200308, 1.151445457756000046 ) ) ;
#7091=CARTESIAN_POINT ( 'NONE',  ( -1.254598503050118108, -78.63589187488014431, 0.2213234496388573058 ) ) ;
#7118=CARTESIAN_POINT ( 'NONE',  ( -1.016909733597999965, -80.23596541309798624, 0.9879038282509999824 ) ) ;
#7121=CARTESIAN_POINT ( 'NONE',  ( -0.7468003766476000171, -77.96329692140810153, 1.319557257415000073 ) ) ;
#7135=CARTESIAN_POINT ( 'NONE',  ( -0.2214140910157267050, -77.86150297134426523, -1.255277234743452430 ) ) ;
#7142=CARTESIAN_POINT ( 'NONE',  ( 1.197531862287877891, -81.92749861843283554, 0.4345771507895428987 ) ) ;
#7145=CARTESIAN_POINT ( 'NONE',  ( -0.9820397338569999413, -80.80308451575899653, -0.7733679338621000099 ) ) ;
#7159=B_SPLINE_CURVE_WITH_KNOTS ( 'NONE', 3,
 ( #2439, #34284, #29566, #7145 ),
 .UNSPECIFIED., .F., .F.,
 ( 4, 4 ),
 ( 0.000000000000000000, 1.000000000000000000 ),
 .UNSPECIFIED. ) ;
#7178=ORIENTED_EDGE ( 'NONE', *, *, #54890, .T. ) ;
#7190=CARTESIAN_POINT ( 'NONE',  ( -1.500000000000000000, -79.00884741929299082, -0.1667699247263852436 ) ) ;
#7202=EDGE_CURVE ( 'NONE', #22736, #2323, #57722, .T. ) ;
#7248=ORIENTED_EDGE ( 'NONE', *, *, #13867, .T. ) ;
#7257=CARTESIAN_POINT ( 'NONE',  ( 0.000000000000000000, -77.29999999999999716, 0.000000000000000000 ) ) ;
#7271=CARTESIAN_POINT ( 'NONE',  ( -1.213636094208999872, -80.71211572874599938, -0.5527192377158001158 ) ) ;
#7284=CARTESIAN_POINT ( 'NONE',  ( -0.3926218265389189721, -80.50416666666666288, -1.460959015002473604 ) ) ;
#7293=FACE_BOUND ( 'NONE', #30025, .T. ) ;
#7301=CARTESIAN_POINT ( 'NONE',  ( -0.2833792192578999947, -79.88098110198900770, 1.589625787444000071 ) ) ;
#7313=VERTEX_POINT ( 'NONE', #11284 ) ;
#7325=CARTESIAN_POINT ( 'NONE',  ( 0.9218200799623692543, -80.72291666666664867, 1.199500263597272687 ) ) ;
#7326=CARTESIAN_POINT ( 'NONE',  ( -1.199500263597274241, -81.34791666666666288, 0.9218200799623669228 ) ) ;
#7347=CARTESIAN_POINT ( 'NONE',  ( -1.500000000000000222, -78.51041666666665719, -0.1963495408493622085 ) ) ;
#7353=CARTESIAN_POINT ( 'NONE',  ( -0.9319389680074999793, -79.29901557144499691, -0.8127712196805999545 ) ) ;
#7375=CARTESIAN_POINT ( 'NONE',  ( -0.5692623238608193192, -78.23835482855749035, -1.139807222690662147 ) ) ;
#7378=B_SPLINE_CURVE_WITH_KNOTS ( 'NONE', 3,
 ( #49860, #27683, #13524, #45728, #22684, #5263, #32396, #31516, #55440, #19134, #37129, #6131, #29141, #41568, #56317, #46605, #23843, #28557 ),
 .UNSPECIFIED., .F., .F.,
 ( 4, 2, 2, 2, 2, 2, 2, 2, 4 ),
 ( 0.000000000000000000, 0.1250000000000000000, 0.2500000000000000000, 0.3750000000000000000, 0.5000000000000000000, 0.6250000000000000000, 0.7500000000000000000, 0.8750000000000000000, 1.000000000000000000 ),
 .UNSPECIFIED. ) ;
#7393=CARTESIAN_POINT ( 'NONE',  ( -0.9218200799623775810, -79.92708333333332860, 1.199500263597266247 ) ) ;
#7402=CARTESIAN_POINT ( 'NONE',  ( 1.407029943534999994, -80.03751491957400788, -0.1741439582578000189 ) ) ;
#7405=CARTESIAN_POINT ( 'NONE',  ( -0.6149910796752999786, -78.95554938902999709, 1.385894317580000035 ) ) ;
#7433=CARTESIAN_POINT ( 'NONE',  ( 1.273953344568438784, -81.40274971728671005, 0.04755539231170149983 ) ) ;
#7471=CARTESIAN_POINT ( 'NONE',  ( 1.199500263597268246, -81.80208333333625603, 0.9218200799623752495 ) ) ;
#7489=CARTESIAN_POINT ( 'NONE',  ( -0.4880156322679000125, -82.23603982111399091, -1.170357530120999856 ) ) ;
#7500=FACE_OUTER_BOUND ( 'NONE', #28764, .T. ) ;
#7536=EDGE_CURVE ( 'NONE', #49070, #30255, #43568, .T. ) ;
#7560=CARTESIAN_POINT ( 'NONE',  ( 1.137658753740000028, -79.51557416179699089, 0.6959227610743999870 ) ) ;
#7572=CARTESIAN_POINT ( 'NONE',  ( 1.246077061130999919, -80.89911715533600045, -0.4752592857455000264 ) ) ;
#7573=VECTOR ( 'NONE', #33897, 1000.000000000000000 ) ;
#7575=CARTESIAN_POINT ( 'NONE',  ( -1.199500263597270244, -80.45208333333333428, -0.9218200799623728070 ) ) ;
#7590=CARTESIAN_POINT ( 'NONE',  ( -1.024999350969000078, -80.55902028819700433, -1.157050009743000096 ) ) ;
#7615=CARTESIAN_POINT ( 'NONE',  ( 1.500000000000000000, -78.14999999999999147, 0.000000000000000000 ) ) ;
#7639=CARTESIAN_POINT ( 'NONE',  ( -1.197912192620000038, -78.20753785706131112, 0.5527856627588000338 ) ) ;
#7654=CARTESIAN_POINT ( 'NONE',  ( -1.500000000000000000, -79.00000000000000000, 0.000000000000000000 ) ) ;
#7665=AXIS2_PLACEMENT_3D ( 'NONE', #14126, #50163, #27698 ) ;
#7682=CARTESIAN_POINT ( 'NONE',  ( -1.310679582531389498, -79.95833333333335702, 0.7554284705563444335 ) ) ;
#7690=CARTESIAN_POINT ( 'NONE',  ( 1.040651332726000078, -79.98790229619299907, -0.9628624948066000222 ) ) ;
#7693=CARTESIAN_POINT ( 'NONE',  ( 1.360845176917000021, -78.26097266169459488, -0.6686124113221000309 ) ) ;
#7713=CARTESIAN_POINT ( 'NONE',  ( 0.5517547646476002043, -78.91101018058850514, -1.149559085547208426 ) ) ;
#7719=CARTESIAN_POINT ( 'NONE',  ( -0.4347137722153567307, -81.05291711652307640, 1.197434020721431125 ) ) ;
#7732=CARTESIAN_POINT ( 'NONE',  ( -1.500000000000000000, -77.89999999999999147, 0.000000000000000000 ) ) ;
#7768=SURFACE_SIDE_STYLE ('',( #52929 ) ) ;
#7856=CARTESIAN_POINT ( 'NONE',  ( -1.264053276207970367, -80.73968330173562435, 0.1648152915473942437 ) ) ;
#7861=CARTESIAN_POINT ( 'NONE',  ( -1.200131629027000102, -80.70066666181199366, -0.3495483843597000373 ) ) ;
#7870=CARTESIAN_POINT ( 'NONE',  ( -0.1119250601223000102, -80.86013818095800332, -1.305888816287000154 ) ) ;
#7875=CARTESIAN_POINT ( 'NONE',  ( 1.086271320152000008, -79.29714775010999972, -0.9110860045855999623 ) ) ;
#7916=B_SPLINE_SURFACE_WITH_KNOTS ( 'NONE', 3, 3, ( 
 ( #9809, #15098, #1259, #6240, #32506, #27794, #15399, #5373, #33392, #42561, #42272, #23666, #51430, #54679, #37828, #10103, #41972, #45838, #55254, #19833, #33095, #10985, #23381, #14803, #32796, #36661, #41391, #10390, #28376, #974, #55848, #46421, #5950, #1840, #51139 ),
 ( #23953, #18958, #36952, #19536, #37530, #29538, #2703, #20128, #47594, #16559, #7121, #20698, #47876, #48439, #48161, #6826, #7693, #30112, #43424, #30404, #38697, #16848, #24837, #11272, #38116, #25694, #2412, #39274, #7981, #52859, #7405, #25121, #43144, #43722, #2984 ),
 ( #20983, #38986, #52575, #56997, #11846, #34542, #56139, #52287, #56718, #3275, #57284, #12125, #21268, #34829, #12413, #42852, #15686, #25979, #29825, #2127, #33683, #51720, #25409, #11561, #33969, #29251, #47300, #20412, #38407, #56427, #34254, #15979, #16275, #52007, #35401 ),
 ( #35113, #30972, #53432, #26847, #48726, #13865, #17129, #31860, #22131, #57859, #4132, #44284, #9448, #54325, #44878, #22430, #8269, #12695, #35706, #49010, #12975, #44577, #3555, #8557, #35, #40141, #40444, #53146, #18012, #49901, #3841, #45178, #36004, #21557, #54029 ) ),
 .UNSPECIFIED., .F., .F., .F.,
 ( 4, 4 ),
 ( 4, 1, 1, 1, 1, 1, 1, 1, 1, 1, 1, 1, 1, 1, 1, 1, 1, 1, 1, 1, 1, 1, 1, 1, 1, 1, 1, 1, 1, 1, 1, 1, 4 ),
 ( -0.05371687727927999811, 1.053716877278999986 ),
 ( -0.02000000000000000042, 0.01250000000000000069, 0.04499999999999999833, 0.07749999999999999944, 0.1100000000000000006, 0.1424999999999999878, 0.1749999999999999889, 0.2074999999999999900, 0.2399999999999999911, 0.2725000000000000200, 0.3049999999999999933, 0.3375000000000000222, 0.3699999999999999956, 0.4025000000000000244, 0.4349999999999999978, 0.4675000000000000266, 0.5000000000000000000, 0.5324999999999999734, 0.5649999999999999467, 0.5975000000000000311, 0.6300000000000000044, 0.6624999999999999778, 0.6949999999999999512, 0.7275000000000000355, 0.7600000000000000089, 0.7924999999999999822, 0.8249999999999999556, 0.8575000000000000400, 0.8900000000000000133, 0.9224999999999999867, 0.9549999999999999600, 0.9875000000000000444, 1.020000000000000018 ),
 .UNSPECIFIED. ) ;
#7926=CARTESIAN_POINT ( 'NONE',  ( -1.295285823243000012, -78.25715048044240518, -0.2505997727336000125 ) ) ;
#7939=ORIENTED_EDGE ( 'NONE', *, *, #15168, .T. ) ;
#7975=CARTESIAN_POINT ( 'NONE',  ( -0.6747260877994001316, -82.25000000000000000, -1.052256958371999840 ) ) ;
#7978=CARTESIAN_POINT ( 'NONE',  ( -1.191059436918999959, -79.34293819223900357, -0.7689280169367000983 ) ) ;
#7981=CARTESIAN_POINT ( 'NONE',  ( 1.118108678836999825, -78.85632414226799369, 1.024097206608999944 ) ) ;
#8085=CARTESIAN_POINT ( 'NONE',  ( -1.249999992656000147, -76.50000000027618796, 0.4999999997238000482 ) ) ;
#8099=CARTESIAN_POINT ( 'NONE',  ( -0.7554284705563544255, -78.91666666666668561, 1.310679582531384169 ) ) ;
#8115=CARTESIAN_POINT ( 'NONE',  ( 1.500000000000000000, -78.26041666666669983, 0.1963495408493652339 ) ) ;
#8147=CARTESIAN_POINT ( 'NONE',  ( 0.4802634405885786162, -80.40574918970366980, -1.180242626984035370 ) ) ;
#8152=CARTESIAN_POINT ( 'NONE',  ( -1.310615285706999922, -81.69291912943299394, -0.2467057407436999972 ) ) ;
#8158=ORIENTED_EDGE ( 'NONE', *, *, #15752, .F. ) ;
#8162=CARTESIAN_POINT ( 'NONE',  ( -1.180080746428999960, -80.76608867448199192, -0.3694817012252999966 ) ) ;
#8167=CARTESIAN_POINT ( 'NONE',  ( 1.407029943534999994, -79.84288660730200604, -0.1741439582578000189 ) ) ;
#8169=AXIS2_PLACEMENT_3D ( 'NONE', #46966, #7078, #38364 ) ;
#8173=VECTOR ( 'NONE', #625, 1000.000000000000227 ) ;
#8176=ADVANCED_FACE ( 'NONE', ( #7500 ), #39078, .T. ) ;
#8237=ORIENTED_EDGE ( 'NONE', *, *, #35484, .T. ) ;
#8247=ORIENTED_EDGE ( 'NONE', *, *, #38413, .F. ) ;
#8267=CARTESIAN_POINT ( 'NONE',  ( -1.304983203281999904, -80.23020634875099688, 0.1938670925079999940 ) ) ;
#8269=CARTESIAN_POINT ( 'NONE',  ( 1.184104130434999957, -78.37171603715040646, -0.5817757459379000462 ) ) ;
#8294=ADVANCED_FACE ( 'NONE', ( #2499 ), #3380, .F. ) ;
#8309=COLOUR_RGB ( '', 0.09019608, 0.27058824, 0.51372549) ;
#8337=CARTESIAN_POINT ( 'NONE',  ( 0.1963495408493571015, -77.86458333333330017, 1.500000000000000444 ) ) ;
#8372=CIRCLE ( 'NONE', #55499, 1.000000000000000000 ) ;
#8394=CARTESIAN_POINT ( 'NONE',  ( -0.5897045597925999472, -82.08556254607600522, -1.428858609762999832 ) ) ;
#8397=ORIENTED_EDGE ( 'NONE', *, *, #20120, .T. ) ;
#8407=ORIENTED_EDGE ( 'NONE', *, *, #28500, .T. ) ;
#8410=CARTESIAN_POINT ( 'NONE',  ( 1.313995274498999999, -80.50198802361599348, -0.2280190045613000038 ) ) ;
#8431=CARTESIAN_POINT ( 'NONE',  ( -0.2777255150705856823, -79.64247121934312190, 1.244507665173133715 ) ) ;
#8433=CARTESIAN_POINT ( 'NONE',  ( 1.406250000003000045, -82.09374999999700151, -9.314605757769000352E-11 ) ) ;
#8435=CARTESIAN_POINT ( 'NONE',  ( 0.8962411872155999770, -81.53824265348700351, 0.9875868993909000526 ) ) ;
#8443=CARTESIAN_POINT ( 'NONE',  ( 1.200322591745000000, -82.09112869963200865, 0.7368979351527999988 ) ) ;
#8449=CARTESIAN_POINT ( 'NONE',  ( 0.2147767365671000017, -80.23978759434999120, -1.401402989476999927 ) ) ;
#8452=CARTESIAN_POINT ( 'NONE',  ( -1.250000000000000000, -82.25000000000000000, 8.279869130157999738E-11 ) ) ;
#8470=CARTESIAN_POINT ( 'NONE',  ( -1.136454603970731725, -80.68718303390609492, -0.5770417699229399844 ) ) ;
#8482=CARTESIAN_POINT ( 'NONE',  ( -1.500000000000000222, -79.91041666666666288, -0.1963495408493622363 ) ) ;
#8499=CARTESIAN_POINT ( 'NONE',  ( -1.310679582531389498, -80.95833333333332860, 0.7554284705563444335 ) ) ;
#8502=CARTESIAN_POINT ( 'NONE',  ( 1.184104130434999957, -78.45560097396669619, -0.5817757459379000462 ) ) ;
#8519=MECHANICAL_DESIGN_GEOMETRIC_PRESENTATION_REPRESENTATION('',(#17122),#21834);
#8524=AXIS2_PLACEMENT_3D ( 'NONE', #33256, #51298, #20569 ) ;
#8556=CARTESIAN_POINT ( 'NONE',  ( 0.7212099693301999848, -80.68823808787499274, 1.333715969168000059 ) ) ;
#8557=CARTESIAN_POINT ( 'NONE',  ( -0.9509180703096998810, -78.71900440081799388, -0.9145055679095001056 ) ) ;
#8589=AXIS2_PLACEMENT_3D ( 'NONE', #10091, #5935, #9206 ) ;
#8608=CARTESIAN_POINT ( 'NONE',  ( 1.500000000000000888, -81.23958333333332860, -0.1963495408493590444 ) ) ;
#8640=B_SPLINE_CURVE_WITH_KNOTS ( 'NONE', 3,
 ( #2292, #47750, #43304, #2860, #56014, #51595, #29127, #16438, #2574, #11436, #42142, #56882, #34421, #20287, #29417, #12008, #52450, #46880 ),
 .UNSPECIFIED., .F., .F.,
 ( 4, 2, 2, 2, 2, 2, 2, 2, 4 ),
 ( 0.000000000000000000, 0.1250000000000000000, 0.2500000000000000000, 0.3750000000000000000, 0.5000000000000000000, 0.6250000000000000000, 0.7500000000000000000, 0.8750000000000000000, 1.000000000000000000 ),
 .UNSPECIFIED. ) ;
#8665=ADVANCED_FACE ( 'NONE', ( #51597, #55727 ), #51306, .T. ) ;
#8682=CARTESIAN_POINT ( 'NONE',  ( 0.7503693421468168312, -77.82491630038197172, -1.029957698447139913 ) ) ;
#8687=ORIENTED_EDGE ( 'NONE', *, *, #7202, .F. ) ;
#8709=CARTESIAN_POINT ( 'NONE',  ( -1.308081345731999967, -80.75005114052200383, 0.2599445073669000017 ) ) ;
#8726=CARTESIAN_POINT ( 'NONE',  ( 1.046486999526615502, -79.45165172675351073, -0.7277384538878118869 ) ) ;
#8731=CARTESIAN_POINT ( 'NONE',  ( 1.316231252753000014, -81.94098224633900429, 0.2147359707272000207 ) ) ;
#8741=CARTESIAN_POINT ( 'NONE',  ( -1.372219269624000093, -82.27922771258300827, 0.3172897272240999822 ) ) ;
#8747=CARTESIAN_POINT ( 'NONE',  ( 0.3023484132065000218, -79.68828967281199027, -1.485775080250999913 ) ) ;
#8748=ORIENTED_EDGE ( 'NONE', *, *, #22352, .F. ) ;
#8751=CARTESIAN_POINT ( 'NONE',  ( -1.460959015002473826, -78.92083333333336270, -0.3926218265389207485 ) ) ;
#8761=ORIENTED_EDGE ( 'NONE', *, *, #35602, .F. ) ;
#8766=EDGE_LOOP ( 'NONE', ( #30651, #28507, #30661, #54947 ) ) ;
#8767=CARTESIAN_POINT ( 'NONE',  ( 0.8928155417757041024, -82.04817708000638277, -1.160372106499861333 ) ) ;
#8770=CARTESIAN_POINT ( 'NONE',  ( -1.236716109016945175, -79.66948819531968695, -0.3055935817348646166 ) ) ;
#8791=CARTESIAN_POINT ( 'NONE',  ( -0.9027627336519593593, -82.16588911174736154, -1.005952998842721158 ) ) ;
#8793=CARTESIAN_POINT ( 'NONE',  ( -1.466115278491000096, -78.37365292024510666, 0.6765500100044000709 ) ) ;
#8796=PRODUCT ( 'Security screw', 'Security screw', '', ( #32861 ) ) ;
#8798=CARTESIAN_POINT ( 'NONE',  ( 1.460959015002472494, -80.77083333333334281, 0.3926218265389233020 ) ) ;
#8801=CARTESIAN_POINT ( 'NONE',  ( -0.2736340887363999941, -78.96324533647100452, -1.491330460909999989 ) ) ;
#8825=CARTESIAN_POINT ( 'NONE',  ( -1.500000000000000222, -81.41041666666664867, -0.1963495408493622363 ) ) ;
#8834=SURFACE_STYLE_USAGE ( .BOTH. , #39821 ) ;
#8856=CARTESIAN_POINT ( 'NONE',  ( -1.087531843820000121, -80.29133710082599862, 1.056511543117000018 ) ) ;
#8925=ORIENTED_EDGE ( 'NONE', *, *, #39957, .T. ) ;
#8948=FACE_OUTER_BOUND ( 'NONE', #54517, .T. ) ;
#8953=CARTESIAN_POINT ( 'NONE',  ( -0.3713770062794000126, -82.25256573098799606, -1.193557338046999927 ) ) ;
#8982=CARTESIAN_POINT ( 'NONE',  ( -0.6868264915819426442, -77.72950740926451374, -1.073137721056557803 ) ) ;
#8984=AXIS2_PLACEMENT_3D ( 'NONE', #58244, #32523, #31651 ) ;
#8991=CARTESIAN_POINT ( 'NONE',  ( -1.281859202539999965, -80.58640536786400332, -0.6809617183367999704 ) ) ;
#8997=CARTESIAN_POINT ( 'NONE',  ( -0.7554284705563544255, -78.41666666666667140, 1.310679582531384169 ) ) ;
#9008=CARTESIAN_POINT ( 'NONE',  ( 1.323534079420999987, -79.96208777222700803, -0.1638099207045999872 ) ) ;
#9028=CARTESIAN_POINT ( 'NONE',  ( -0.2693486100347141088, -80.35804431655570568, -1.245426196537031682 ) ) ;
#9032=CARTESIAN_POINT ( 'NONE',  ( 0.6224761083686999319, -81.88553101715500304, -1.179448874982999884 ) ) ;
#9041=CARTESIAN_POINT ( 'NONE',  ( -0.9627379117275000064, -82.23220295934500257, 1.028099582737000084 ) ) ;
#9047=CARTESIAN_POINT ( 'NONE',  ( 0.6743760579952999823, -80.43823808787499274, 1.247107161604999792 ) ) ;
#9048=ORIENTED_EDGE ( 'NONE', *, *, #3001, .F. ) ;
#9050=CARTESIAN_POINT ( 'NONE',  ( 0.7554284705563509839, -79.06666666666667709, -1.310679582531386167 ) ) ;
#9059=ORIENTED_EDGE ( 'NONE', *, *, #3326, .T. ) ;
#9069=CARTESIAN_POINT ( 'NONE',  ( -1.229479409833385883, -80.67128155205320184, -0.3337909954253061029 ) ) ;
#9078=CARTESIAN_POINT ( 'NONE',  ( -1.310679582531386389, -79.94166666666667709, -0.7554284705563492075 ) ) ;
#9090=CARTESIAN_POINT ( 'NONE',  ( -1.466822177622293388, -82.03317782236065625, -0.2501548871699424414 ) ) ;
#9093=CARTESIAN_POINT ( 'NONE',  ( 0.1747633057891999908, -78.27442767348290431, 1.605201443249000048 ) ) ;
#9100=CARTESIAN_POINT ( 'NONE',  ( 1.505666248717000055, -79.11208320661400251, 0.1786365444185999962 ) ) ;
#9123=CARTESIAN_POINT ( 'NONE',  ( 1.310679582531388387, -81.60833333333333428, -0.7554284705563470981 ) ) ;
#9154=CARTESIAN_POINT ( 'NONE',  ( -1.508831841893000236, -79.84482349039599569, 0.1495614418054999895 ) ) ;
#9192=CARTESIAN_POINT ( 'NONE',  ( 1.275275057825000058, -80.92867431909800757, 0.3379927550398999503 ) ) ;
#9206=DIRECTION ( 'NONE',  ( -1.000000000000000000, 0.000000000000000000, 0.000000000000000000 ) ) ;
#9217=B_SPLINE_CURVE_WITH_KNOTS ( 'NONE', 3,
 ( #5535, #25224, #16087, #38800, #41558, #56528, #6932, #47974, #3090, #43243, #2801, #21084, #20796, #46305, #19127, #30218, #34068, #23544 ),
 .UNSPECIFIED., .F., .F.,
 ( 4, 2, 2, 2, 2, 2, 2, 2, 4 ),
 ( 0.000000000000000000, 0.1250000000000000000, 0.2500000000000000000, 0.3750000000000000000, 0.5000000000000000000, 0.6250000000000000000, 0.7500000000000000000, 0.8750000000000000000, 1.000000000000000000 ),
 .UNSPECIFIED. ) ;
#9223=CARTESIAN_POINT ( 'NONE',  ( 0.3926218265389159190, -77.85416666666667140, 1.460959015002474715 ) ) ;
#9243=MECHANICAL_DESIGN_GEOMETRIC_PRESENTATION_REPRESENTATION('',(#41308),#19612);
#9282=ORIENTED_EDGE ( 'NONE', *, *, #24871, .F. ) ;
#9298=CARTESIAN_POINT ( 'NONE',  ( 1.313995274498999999, -80.45821400603800555, -0.2280190045613000038 ) ) ;
#9313=CARTESIAN_POINT ( 'NONE',  ( -1.210921577777000158, -78.23125641502100791, 0.5587889421650999999 ) ) ;
#9315=DIRECTION ( 'NONE',  ( -1.000000000000000000, 3.791735831002999804E-11, 3.791715846987999626E-11 ) ) ;
#9321=CARTESIAN_POINT ( 'NONE',  ( 1.500000000000000000, -80.25000000000000000, 0.000000000000000000 ) ) ;
#9324=B_SPLINE_CURVE_WITH_KNOTS ( 'NONE', 3,
 ( #16340, #56203, #42917, #42339, #46785, #19899, #33456, #2474, #56490, #1905, #34318, #52068, #47073, #11905, #20477, #29884, #38473, #37891 ),
 .UNSPECIFIED., .F., .F.,
 ( 4, 2, 2, 2, 2, 2, 2, 2, 4 ),
 ( 0.000000000000000000, 0.1250000000000000000, 0.2500000000000000000, 0.3750000000000000000, 0.5000000000000000000, 0.6250000000000000000, 0.7500000000000000000, 0.8750000000000000000, 1.000000000000000000 ),
 .UNSPECIFIED. ) ;
#9336=CARTESIAN_POINT ( 'NONE',  ( -0.3379921552883999869, -81.90302968668000005, -1.367316507193000019 ) ) ;
#9342=CARTESIAN_POINT ( 'NONE',  ( -1.247892825656000015, -79.17060648544099877, -0.1947040076506000028 ) ) ;
#9344=VERTEX_POINT ( 'NONE', #26415 ) ;
#9363=CARTESIAN_POINT ( 'NONE',  ( -1.149554727142765964, -79.68538967717259425, -0.5515177578643482015 ) ) ;
#9397=CARTESIAN_POINT ( 'NONE',  ( -1.021885754039999927, -78.85826102536199755, -0.9827557610011000699 ) ) ;
#9416=CYLINDRICAL_SURFACE ( 'NONE', #51696, 0.5000000000000000000 ) ;
#9417=CARTESIAN_POINT ( 'NONE',  ( -0.9218200799623714747, -81.47291666666669130, -1.199500263597270466 ) ) ;
#9423=ORIENTED_EDGE ( 'NONE', *, *, #31123, .T. ) ;
#9445=CARTESIAN_POINT ( 'NONE',  ( 0.2296925013217000211, -80.48978759434999120, -1.498727297740999775 ) ) ;
#9448=CARTESIAN_POINT ( 'NONE',  ( -1.295285823243000012, -78.17326554362610125, -0.2505997727336000125 ) ) ;
#9480=B_SPLINE_CURVE_WITH_KNOTS ( 'NONE', 3,
 ( #18353, #8608, #36343, #5347, #13910, #49355, #5063, #23356, #31904, #27476, #50234, #662, #32192, #17765, #54075, #31022, #27770, #31609 ),
 .UNSPECIFIED., .F., .F.,
 ( 4, 2, 2, 2, 2, 2, 2, 2, 4 ),
 ( 0.000000000000000000, 0.1250000000000000000, 0.2500000000000000000, 0.3750000000000000000, 0.5000000000000000000, 0.6250000000000000000, 0.7500000000000000000, 0.8750000000000000000, 1.000000000000000000 ),
 .UNSPECIFIED. ) ;
#9486=CARTESIAN_POINT ( 'NONE',  ( -0.8625730533285999035, -81.22635005938499830, -0.9982651640015999250 ) ) ;
#9553=CARTESIAN_POINT ( 'NONE',  ( 0.000000000000000000, -77.50000000000000000, 0.000000000000000000 ) ) ;
#9555=EDGE_CURVE ( 'NONE', #35383, #5753, #30937, .T. ) ;
#9575=CARTESIAN_POINT ( 'NONE',  ( -1.453051419519999943, -80.51449613900899749, -0.4232133907648999993 ) ) ;
#9577=EDGE_LOOP ( 'NONE', ( #32034, #30884, #15305, #35897 ) ) ;
#9590=CYLINDRICAL_SURFACE ( 'NONE', #36663, 1.500000000000000000 ) ;
#9592=CARTESIAN_POINT ( 'NONE',  ( -1.319155384867000125, -80.25392490671100632, 0.1959724986398999891 ) ) ;
#9607=CARTESIAN_POINT ( 'NONE',  ( -0.1120320062231000002, -77.88396805135350576, -1.328911429676000067 ) ) ;
#9615=CARTESIAN_POINT ( 'NONE',  ( 0.9432352957733999288, -82.03436888729800103, 0.9428059748164999698 ) ) ;
#9626=CARTESIAN_POINT ( 'NONE',  ( -0.6688296391966999099, -81.65955898600100227, 1.127159194743000192 ) ) ;
#9636=CARTESIAN_POINT ( 'NONE',  ( -0.1963495408493606265, -79.01458333333334849, -1.500000000000000222 ) ) ;
#9637=ORIENTED_EDGE ( 'NONE', *, *, #39362, .F. ) ;
#9654=CARTESIAN_POINT ( 'NONE',  ( -1.018293611623504402, -80.09882820534807024, 0.7672941069546416193 ) ) ;
#9687=CARTESIAN_POINT ( 'NONE',  ( -1.377158602743000060, -77.81639593435950530, -0.3366111412210999743 ) ) ;
#9701=VERTEX_POINT ( 'NONE', #1921 ) ;
#9734=CARTESIAN_POINT ( 'NONE',  ( -0.6219878248318000402, -79.94404873715900806, -1.382777385570999940 ) ) ;
#9746=AXIS2_PLACEMENT_3D ( 'NONE', #57283, #34251, #47297 ) ;
#9809=CARTESIAN_POINT ( 'NONE',  ( -1.403403115923000044, -77.46141162325051255, 0.5665048067823000855 ) ) ;
#9845=DIRECTION ( 'NONE',  ( 0.000000000000000000, -1.000000000000000000, 0.000000000000000000 ) ) ;
#9866=EDGE_CURVE ( 'NONE', #4192, #46183, #8372, .T. ) ;
#9868=CARTESIAN_POINT ( 'NONE',  ( 1.386500578471000056, -81.36942886518100693, 0.2961005337747000254 ) ) ;
#9892=CARTESIAN_POINT ( 'NONE',  ( 0.000000000000000000, -76.79999999999999716, 0.000000000000000000 ) ) ;
#9899=CARTESIAN_POINT ( 'NONE',  ( -0.5409299486741000473, -79.13012224168299724, 1.218996123443000013 ) ) ;
#9918=CARTESIAN_POINT ( 'NONE',  ( -1.114850945326000042, -81.91137662116999252, -1.012920685771000029 ) ) ;
#9925=CARTESIAN_POINT ( 'NONE',  ( 0.9236342483431000394, -80.34477190545899816, -0.9420537984437000745 ) ) ;
#9953=EDGE_CURVE ( 'NONE', #27527, #17474, #42834, .T. ) ;
#9958=B_SPLINE_CURVE_WITH_KNOTS ( 'NONE', 3,
 ( #47466, #6989, #47747, #38857, #56877, #31437, #58324, #40315, #8726, #30568, #22003, #44447, #3999, #12571, #35574, #48888, #8431, #44747, #3431, #57730, #21433, #12286, #53601, #17287, #26425, #39441, #13436, #48601, #35275, #35876, #49173, #57448, #49477, #4298, #17887, #58026, #40009, #13141, #17587, #26719, #31134, #22299, #53308, #53905, #43885, #9028, #40611, #8147, #27014, #12851, #48316, #45050, #4603, #22601, #208, #18183, #34989, #30851, #25856, #36178, #30275, #7856, #17007, #3714, #53018 ),
 .UNSPECIFIED., .F., .F.,
 ( 4, 2, 2, 2, 2, 2, 2, 2, 2, 2, 2, 2, 2, 2, 2, 2, 1, 2, 2, 2, 2, 2, 2, 2, 2, 2, 2, 2, 2, 2, 2, 2, 4 ),
 ( 0.000000000000000000, 0.03125000000000000000, 0.06250000000000000000, 0.09375000000000000000, 0.1250000000000000000, 0.1562500000000000000, 0.1875000000000000000, 0.2187500000000000000, 0.2500000000000000000, 0.2812500000000000000, 0.3125000000000000000, 0.3437500000000000000, 0.3750000000000000000, 0.4062500000000000000, 0.4375000000000000000, 0.4687500000000000000, 0.5000000000000000000, 0.5312500000000000000, 0.5625000000000000000, 0.5937500000000000000, 0.6250000000000000000, 0.6562500000000000000, 0.6875000000000000000, 0.7187500000000000000, 0.7500000000000000000, 0.7812500000000000000, 0.8125000000000000000, 0.8437500000000000000, 0.8750000000000000000, 0.9062500000000000000, 0.9375000000000000000, 0.9687500000000000000, 1.000000000000000000 ),
 .UNSPECIFIED. ) ;
#10004=CARTESIAN_POINT ( 'NONE',  ( -1.250000000000000000, -67.52659999995799467, 0.000000000000000000 ) ) ;
#10073=CARTESIAN_POINT ( 'NONE',  ( 0.6718344995053999735, -81.32557530614698749, -1.135431202457000133 ) ) ;
#10091=CARTESIAN_POINT ( 'NONE',  ( 0.000000000000000000, -75.67500000000001137, 0.000000000000000000 ) ) ;
#10103=CARTESIAN_POINT ( 'NONE',  ( 0.7608607662309999631, -78.15598835058560212, -1.424185669224000028 ) ) ;
#10153=CARTESIAN_POINT ( 'NONE',  ( 1.500000000000001110, -78.13958333333334849, -0.1963495408493590721 ) ) ;
#10156=DIRECTION ( 'NONE',  ( 0.000000000000000000, 0.000000000000000000, 1.000000000000000000 ) ) ;
#10161=CARTESIAN_POINT ( 'NONE',  ( -1.098028760202000020, -82.10785915155000225, -1.045495904960999978 ) ) ;
#10176=DIRECTION ( 'NONE',  ( -1.000000000000000000, 0.000000000000000000, 0.000000000000000000 ) ) ;
#10192=CARTESIAN_POINT ( 'NONE',  ( 0.5704417986824000808, -78.88205912477799586, -1.205475954488999912 ) ) ;
#10207=CARTESIAN_POINT ( 'NONE',  ( 1.294956495611000014, -82.10782256861200779, -0.9466954001098000226 ) ) ;
#10214=CARTESIAN_POINT ( 'NONE',  ( -1.172662378873000177, -80.19593403531600018, -0.6045068694098000295 ) ) ;
#10249=CARTESIAN_POINT ( 'NONE',  ( -1.213636094208999872, -80.66834171116700247, -0.5527192377158001158 ) ) ;
#10293=CARTESIAN_POINT ( 'NONE',  ( 0.5704417986824000808, -78.83828510719899896, -1.205475954488999912 ) ) ;
#10358=CARTESIAN_POINT ( 'NONE',  ( 0.2130225254155999892, -82.02015203348199179, 1.301993463592000078 ) ) ;
#10388=CARTESIAN_POINT ( 'NONE',  ( 0.5117640625906000329, -79.58524224479700138, 1.216002981391000048 ) ) ;
#10390=CARTESIAN_POINT ( 'NONE',  ( 1.603441158369999897, -78.75133983115900094, 0.1902368389766999901 ) ) ;
#10408=CARTESIAN_POINT ( 'NONE',  ( -0.3528755875620728233, -78.14773221022913674, 1.224383399418459861 ) ) ;
#10429=CARTESIAN_POINT ( 'NONE',  ( -0.1963495408493605987, -79.61458333333334281, -1.500000000000000444 ) ) ;
#10449=CARTESIAN_POINT ( 'NONE',  ( -1.404437343888000012, -82.11361821589699161, -0.1941552913445999951 ) ) ;
#10481=CARTESIAN_POINT ( 'NONE',  ( 0.9834589317531000630, -79.03089699492099385, 0.9007689179829999615 ) ) ;
#10501=CARTESIAN_POINT ( 'NONE',  ( 1.423274683982999944, -81.62922810174299570, 0.4931431035810000529 ) ) ;
#10508=DIRECTION ( 'NONE',  ( 0.000000000000000000, 1.000000000000000000, 0.000000000000000000 ) ) ;
#10530=CIRCLE ( 'NONE', #57622, 0.5000000000000000000 ) ;
#10545=CARTESIAN_POINT ( 'NONE',  ( -1.000649921775999873, -79.57686399678399880, 0.8816325131470000853 ) ) ;
#10573=DIRECTION ( 'NONE',  ( -1.000000000000000000, 0.000000000000000000, 0.000000000000000000 ) ) ;
#10586=CARTESIAN_POINT ( 'NONE',  ( -0.1765672563250000049, -78.29254625000710632, -1.321892640673999919 ) ) ;
#10617=CARTESIAN_POINT ( 'NONE',  ( 1.452792874191000116, -80.69399715222199632, 0.7047031062512999489 ) ) ;
#10643=CARTESIAN_POINT ( 'NONE',  ( 1.500000000000000000, -81.15000000000000568, 0.000000000000000000 ) ) ;
#10644=CONICAL_SURFACE ( 'NONE', #50250, 2.149999999947999729, 0.7853981633972997312 ) ;
#10648=CARTESIAN_POINT ( 'NONE',  ( -1.250000000000000000, -82.25000000000000000, 8.279869130157999738E-11 ) ) ;
#10685=ORIENTED_EDGE ( 'NONE', *, *, #39465, .T. ) ;
#10709=CARTESIAN_POINT ( 'NONE',  ( -1.267102727772119630, -78.25904358090664914, -0.1447965901780092768 ) ) ;
#10719=CARTESIAN_POINT ( 'NONE',  ( -0.1832406609208000192, -81.87969241135199638, -1.320984106490000087 ) ) ;
#10730=CARTESIAN_POINT ( 'NONE',  ( -1.310679582531389498, -80.45833333333332860, 0.7554284705563444335 ) ) ;
#10739=FACE_OUTER_BOUND ( 'NONE', #2504, .T. ) ;
#10744=CARTESIAN_POINT ( 'NONE',  ( -0.7554284705563483193, -77.98333333333334849, -1.310679582531387721 ) ) ;
#10748=CARTESIAN_POINT ( 'NONE',  ( 0.000000000000000000, -75.67500000000001137, 0.000000000000000000 ) ) ;
#10750=VERTEX_POINT ( 'NONE', #8433 ) ;
#10751=CARTESIAN_POINT ( 'NONE',  ( -0.2083289567832000144, -81.66134554112100830, -1.501845930097000181 ) ) ;
#10759=CARTESIAN_POINT ( 'NONE',  ( -1.500000000000000000, -80.90000000000000568, 0.000000000000000000 ) ) ;
#10779=CARTESIAN_POINT ( 'NONE',  ( 0.3926218265389159745, -78.75416666666666288, 1.460959015002474493 ) ) ;
#10799=CARTESIAN_POINT ( 'NONE',  ( -1.004225369717999916, -80.97922849090299735, -1.250800220804000107 ) ) ;
#10816=B_SPLINE_CURVE_WITH_KNOTS ( 'NONE', 3,
 ( #36607, #54630, #54341, #13880 ),
 .UNSPECIFIED., .F., .F.,
 ( 4, 4 ),
 ( 0.000000000000000000, 1.000000000000000000 ),
 .UNSPECIFIED. ) ;
#10831=VERTEX_POINT ( 'NONE', #41482 ) ;
#10840=AXIS2_PLACEMENT_3D ( 'NONE', #13369, #31367, #22233 ) ;
#10845=CARTESIAN_POINT ( 'NONE',  ( -1.154258600661999923, -79.67608924354598798, -0.6680293646364998672 ) ) ;
#10861=CARTESIAN_POINT ( 'NONE',  ( 0.1510373474112000070, -81.50030724171101326, 1.325052402434999888 ) ) ;
#10885=CARTESIAN_POINT ( 'NONE',  ( -1.182296476285000120, -78.59606059609599527, 0.6170503964917000150 ) ) ;
#10952=CARTESIAN_POINT ( 'NONE',  ( 0.6157886138241999152, -81.82170153995799922, -1.166777612888000082 ) ) ;
#10954=CARTESIAN_POINT ( 'NONE',  ( -0.2497519934274041176, -78.54048298376281423, 1.249453341561128195 ) ) ;
#10977=CARTESIAN_POINT ( 'NONE',  ( -1.460959015002474937, -79.97916666666665719, 0.3926218265389144757 ) ) ;
#10979=ORIENTED_EDGE ( 'NONE', *, *, #6666, .T. ) ;
#10985=CARTESIAN_POINT ( 'NONE',  ( -1.431457626485999945, -78.45366409087199600, 0.7470896798747000966 ) ) ;
#11008=CARTESIAN_POINT ( 'NONE',  ( 0.9388019354105423542, -81.95930158213857908, 0.8620481451250026073 ) ) ;
#11010=CARTESIAN_POINT ( 'NONE',  ( 1.193978368322000216, -81.93514364053599763, -0.5941311122250999555 ) ) ;
#11013=EDGE_CURVE ( 'NONE', #34724, #35383, #20682, .T. ) ;
#11017=EDGE_CURVE ( 'NONE', #7313, #51480, #58395, .T. ) ;
#11033=VECTOR ( 'NONE', #35613, 1000.000000000000000 ) ;
#11045=CARTESIAN_POINT ( 'NONE',  ( -1.311997437969999902, -81.07175312489499674, 0.5373286780417999564 ) ) ;
#11046=EDGE_LOOP ( 'NONE', ( #26393, #25447, #26248, #12015, #43966 ) ) ;
#11066=CARTESIAN_POINT ( 'NONE',  ( -1.500000000000000000, -80.50000000000000000, 0.000000000000000000 ) ) ;
#11068=AXIS2_PLACEMENT_3D ( 'NONE', #27576, #5159, #23160 ) ;
#11075=CARTESIAN_POINT ( 'NONE',  ( 0.7554284705563452107, -78.73333333333332007, 1.310679582531388609 ) ) ;
#11079=DIRECTION ( 'NONE',  ( 0.000000000000000000, -1.000000000000000000, 0.000000000000000000 ) ) ;
#11095=CARTESIAN_POINT ( 'NONE',  ( 1.602797262804000145, -82.15484732184999928, -0.06469291290319000021 ) ) ;
#11141=CARTESIAN_POINT ( 'NONE',  ( 0.5173218454072999739, -79.52141276759999755, 1.229208833401000067 ) ) ;
#11153=CARTESIAN_POINT ( 'NONE',  ( -1.310615285706999922, -81.64914511185500601, -0.2467057407436999972 ) ) ;
#11154=CARTESIAN_POINT ( 'NONE',  ( 0.1963495408493637351, -80.53541666666667709, -1.499999999999999778 ) ) ;
#11172=CARTESIAN_POINT ( 'NONE',  ( 1.602460118848999970, -79.73214323184600971, -0.1983317763271000012 ) ) ;
#11175=DIRECTION ( 'NONE',  ( 0.000000000000000000, -1.000000000000000000, 0.000000000000000000 ) ) ;
#11177=CARTESIAN_POINT ( 'NONE',  ( -1.210921577777000158, -78.14370837986389517, 0.5587889421650999999 ) ) ;
#11242=CARTESIAN_POINT ( 'NONE',  ( -1.000309426110861599, -79.09703484861441325, 0.7891363950083513101 ) ) ;
#11272=CARTESIAN_POINT ( 'NONE',  ( -1.092853437769999880, -78.60826102536199755, -1.051005954092999906 ) ) ;
#11284=CARTESIAN_POINT ( 'NONE',  ( -1.249999986291000065, -76.30000000051599329, 0.6999999994844999796 ) ) ;
#11287=CARTESIAN_POINT ( 'NONE',  ( 0.01020701576794861079, -78.62478094170407417, 1.275250707744829848 ) ) ;
#11295=CARTESIAN_POINT ( 'NONE',  ( -0.4908969598308604021, -81.24373489875783605, -1.175594168089061586 ) ) ;
#11320=CARTESIAN_POINT ( 'NONE',  ( -0.1963495408493606265, -78.01458333333334849, -1.500000000000000222 ) ) ;
#11321=ORIENTED_EDGE ( 'NONE', *, *, #76, .T. ) ;
#11345=ADVANCED_FACE ( 'NONE', ( #26255 ), #17113, .T. ) ;
#11360=AXIS2_PLACEMENT_3D ( 'NONE', #31219, #17968, #35960 ) ;
#11361=CARTESIAN_POINT ( 'NONE',  ( 0.000000000000000000, -76.00000000000000000, 0.000000000000000000 ) ) ;
#11362=CARTESIAN_POINT ( 'NONE',  ( -1.320128238786999919, -78.77699527221300002, -0.1893081677438999966 ) ) ;
#11377=ADVANCED_FACE ( 'NONE', ( #16543 ), #44269, .T. ) ;
#11378=CARTESIAN_POINT ( 'NONE',  ( -1.417334032777999964, -79.02654225787900089, -0.4910847579886000736 ) ) ;
#11395=FACE_OUTER_BOUND ( 'NONE', #42401, .T. ) ;
#11401=( LENGTH_UNIT ( ) NAMED_UNIT ( * ) SI_UNIT ( .MILLI., .METRE. ) );
#11422=CARTESIAN_POINT ( 'NONE',  ( 0.9788970803261000109, -79.86870113126700232, -0.9057243817226000582 ) ) ;
#11436=CARTESIAN_POINT ( 'NONE',  ( -0.1963495408493605987, -77.61458333333330017, -1.500000000000000444 ) ) ;
#11455=CARTESIAN_POINT ( 'NONE',  ( -1.500000000000000000, -77.50000000000000000, 0.000000000000000000 ) ) ;
#11462=CARTESIAN_POINT ( 'NONE',  ( 0.9384621721472999889, -78.49099674353139733, 0.9475573338641000154 ) ) ;
#11468=ORIENTED_EDGE ( 'NONE', *, *, #4758, .F. ) ;
#11487=CARTESIAN_POINT ( 'NONE',  ( -1.500000000000000444, -81.38958333333330586, 0.1963495408493560745 ) ) ;
#11531=CARTESIAN_POINT ( 'NONE',  ( -1.160672508370670153, -78.68359632043879515, -0.5250652338630038551 ) ) ;
#11558=CYLINDRICAL_SURFACE ( 'NONE', #9746, 1.500000000000000000 ) ;
#11561=CARTESIAN_POINT ( 'NONE',  ( -1.021885754039999927, -78.66363271308999572, -0.9827557610011000699 ) ) ;
#11585=CARTESIAN_POINT ( 'NONE',  ( 0.8399831259196580691, -81.83208972731527808, -0.9577039101323847614 ) ) ;
#11610=PRODUCT_DEFINITION_SHAPE ( 'NONE', 'NONE',  #49537 ) ;
#11615=VERTEX_POINT ( 'NONE', #39422 ) ;
#11642=CARTESIAN_POINT ( 'NONE',  ( -0.6204398466918998878, -82.19746881207100841, -1.165230367032999981 ) ) ;
#11648=CARTESIAN_POINT ( 'NONE',  ( -0.7554284705563540925, -78.81666666666669130, 1.310679582531384391 ) ) ;
#11649=CARTESIAN_POINT ( 'NONE',  ( 0.2086861075963999945, -78.62815740206998782, 1.317203954600000060 ) ) ;
#11676=CARTESIAN_POINT ( 'NONE',  ( 1.460959015002472494, -78.77083333333337123, 0.3926218265389233020 ) ) ;
#11678=CARTESIAN_POINT ( 'NONE',  ( 0.7554284705563453217, -81.33333333333332860, 1.310679582531389276 ) ) ;
#11679=CARTESIAN_POINT ( 'NONE',  ( -1.500000000000000000, -80.90000000000000568, 0.000000000000000000 ) ) ;
#11684=VERTEX_POINT ( 'NONE', #22277 ) ;
#11712=CARTESIAN_POINT ( 'NONE',  ( -0.2340539085346999837, -80.06715162479200387, 1.312933706406000267 ) ) ;
#11724=AXIS2_PLACEMENT_3D ( 'NONE', #12270, #53003, #56567 ) ;
#11726=CARTESIAN_POINT ( 'NONE',  ( 1.500000000000000888, -79.23137852148992977, -0.3510066005171250114 ) ) ;
#11754=ADVANCED_FACE ( 'NONE', ( #5158 ), #40591, .T. ) ;
#11760=ORIENTED_EDGE ( 'NONE', *, *, #39005, .F. ) ;
#11761=CARTESIAN_POINT ( 'NONE',  ( 0.4532606190057231199, -79.30375411270249231, -1.190852882372544386 ) ) ;
#11764=CARTESIAN_POINT ( 'NONE',  ( 1.460959015002472494, -80.67083333333334849, 0.3926218265389232465 ) ) ;
#11765=CARTESIAN_POINT ( 'NONE',  ( -0.7554284705563540925, -81.31666666666669130, 1.310679582531384391 ) ) ;
#11782=ADVANCED_FACE ( 'NONE', ( #187 ), #9590, .T. ) ;
#11786=CARTESIAN_POINT ( 'NONE',  ( 1.500000000000000000, -78.75000000000000000, 0.000000000000000000 ) ) ;
#11791=LINE ( 'NONE', #48671, #41048 ) ;
#11801=VECTOR ( 'NONE', #49398, 1000.000000000000000 ) ;
#11814=CARTESIAN_POINT ( 'NONE',  ( -1.266763334644595895, -78.15884741929295387, -0.1447707219529647815 ) ) ;
#11841=CARTESIAN_POINT ( 'NONE',  ( 1.209428572278999914, -79.59100130914399074, 0.7398254253092000354 ) ) ;
#11846=CARTESIAN_POINT ( 'NONE',  ( -0.1190996060027000036, -77.72099286884960634, -1.412746526842000083 ) ) ;
#11856=LINE ( 'NONE', #54041, #22468 ) ;
#11871=CARTESIAN_POINT ( 'NONE',  ( -1.051406088259749128, -82.10241491881451736, 0.7198062334868400303 ) ) ;
#11872=ORIENTED_EDGE ( 'NONE', *, *, #23252, .T. ) ;
#11892=DIRECTION ( 'NONE',  ( -1.000000000000000000, 0.000000000000000000, 0.000000000000000000 ) ) ;
#11905=CARTESIAN_POINT ( 'NONE',  ( -1.199500263597270022, -78.05208333333332860, -0.9218200799623730290 ) ) ;
#11907=ADVANCED_FACE ( 'NONE', ( #16053 ), #42633, .T. ) ;
#11922=CARTESIAN_POINT ( 'NONE',  ( -0.5837186552087999525, -82.24414371479799968, -1.096265345431000071 ) ) ;
#11923=EDGE_CURVE ( 'NONE', #1594, #41674, #36657, .T. ) ;
#11979=ORIENTED_EDGE ( 'NONE', *, *, #39787, .T. ) ;
#11997=CARTESIAN_POINT ( 'NONE',  ( -4.000000000000000000, -76.79999999999999716, 0.000000000000000000 ) ) ;
#12008=CARTESIAN_POINT ( 'NONE',  ( -1.460959015002473382, -77.52083333333332860, -0.3926218265389205819 ) ) ;
#12012=CARTESIAN_POINT ( 'NONE',  ( -1.066991882994506646, -79.46378521489916125, -1.111185832896742998 ) ) ;
#12015=ORIENTED_EDGE ( 'NONE', *, *, #38636, .T. ) ;
#12025=CARTESIAN_POINT ( 'NONE',  ( -0.7332490996008999007, -80.07943159551300027, -1.438596428395999993 ) ) ;
#12028=CARTESIAN_POINT ( 'NONE',  ( 1.356641013456250544, -82.10677083333045800, 0.3654621275246989209 ) ) ;
#12046=CARTESIAN_POINT ( 'NONE',  ( -1.099193429257143029, -79.19244373973189965, -0.6451977031882378810 ) ) ;
#12050=CARTESIAN_POINT ( 'NONE',  ( -1.500000000000000000, -78.39999999999999147, 0.000000000000000000 ) ) ;
#12075=CARTESIAN_POINT ( 'NONE',  ( 0.2064441143900000164, -78.60443884411000681, 1.303052737963999785 ) ) ;
#12115=CARTESIAN_POINT ( 'NONE',  ( 0.3926218265389159190, -79.85416666666668561, 1.460959015002474715 ) ) ;
#12125=CARTESIAN_POINT ( 'NONE',  ( -1.287313221243000072, -78.06828123251710849, 0.5940404451740000091 ) ) ;
#12137=ORIENTED_EDGE ( 'NONE', *, *, #23673, .T. ) ;
#12152=CARTESIAN_POINT ( 'NONE',  ( -0.8056434147970419346, -81.72077935434506912, -0.9882239605117585368 ) ) ;
#12206=CARTESIAN_POINT ( 'NONE',  ( -0.3904991445228000457, -82.21237762652100400, -1.255013400307000149 ) ) ;
#12228=CARTESIAN_POINT ( 'NONE',  ( -1.500000000000000000, -79.90000000000000568, 0.000000000000000000 ) ) ;
#12248=ADVANCED_FACE ( 'NONE', ( #29535 ), #14453, .F. ) ;
#12261=B_SPLINE_CURVE_WITH_KNOTS ( 'NONE', 3,
 ( #21754, #35315, #4340, #12892, #8767, #17328, #26759, #30893, #48926, #44486 ),
 .UNSPECIFIED., .F., .F.,
 ( 4, 2, 2, 2, 4 ),
 ( 0.1666666058611807055, 0.3749999543958855153, 0.5833333029305902695, 0.7916666514652952458, 1.000000000000000000 ),
 .UNSPECIFIED. ) ;
#12266=VECTOR ( 'NONE', #1588, 1000.000000000000000 ) ;
#12268=EDGE_CURVE ( 'NONE', #18435, #19319, #54958, .T. ) ;
#12270=CARTESIAN_POINT ( 'NONE',  ( 1.750000000000000000, -76.29999999999999716, -0.5000000000000000000 ) ) ;
#12286=CARTESIAN_POINT ( 'NONE',  ( -1.237049208466255878, -79.76968421440388113, -0.3056626403079319432 ) ) ;
#12289=CARTESIAN_POINT ( 'NONE',  ( -1.127489577578000057, -80.76097822051700348, -0.5989559841152000130 ) ) ;
#12307=CARTESIAN_POINT ( 'NONE',  ( -0.9624967649451999785, -80.61439197592500250, -1.086495216026000188 ) ) ;
#12309=CARTESIAN_POINT ( 'NONE',  ( -0.3450130740848871280, -82.18489583333146697, 1.280549398083555390 ) ) ;
#12333=CARTESIAN_POINT ( 'NONE',  ( 1.310679582531385501, -81.19166666666669130, 0.7554284705563518720 ) ) ;
#12345=DIRECTION ( 'NONE',  ( 0.000000000000000000, 1.000000000000000000, 0.000000000000000000 ) ) ;
#12351=CARTESIAN_POINT ( 'NONE',  ( 0.6906586288378000482, -79.06822964757999728, -1.459522026167999975 ) ) ;
#12357=CARTESIAN_POINT ( 'NONE',  ( -1.242864761025999965, -77.72794916437750601, 0.2245736866142999943 ) ) ;
#12377=CARTESIAN_POINT ( 'NONE',  ( -0.9218200799623714747, -78.47291666666666288, -1.199500263597270466 ) ) ;
#12385=CONICAL_SURFACE ( 'NONE', #7665, 0.5999999993581000002, 0.7853981633972997312 ) ;
#12389=ORIENTED_EDGE ( 'NONE', *, *, #7536, .F. ) ;
#12405=CARTESIAN_POINT ( 'NONE',  ( 2.000000000000000000, -76.29999999999999716, 0.000000000000000000 ) ) ;
#12410=CARTESIAN_POINT ( 'NONE',  ( 1.396889377938999921, -80.53364115338500540, -0.2424037069397000088 ) ) ;
#12413=CARTESIAN_POINT ( 'NONE',  ( -0.1877060973040000080, -78.21711910266039069, -1.405284953735000064 ) ) ;
#12440=CARTESIAN_POINT ( 'NONE',  ( 1.500000000000000000, -79.14999999999999147, 0.000000000000000000 ) ) ;
#12467=CARTESIAN_POINT ( 'NONE',  ( 1.310679582531385279, -81.79166666666901619, 0.7554284705563519831 ) ) ;
#12486=ADVANCED_FACE ( 'NONE', ( #3693 ), #29173, .T. ) ;
#12489=CARTESIAN_POINT ( 'NONE',  ( -0.6804402928152999408, -82.23668930757399664, -1.032525207220000185 ) ) ;
#12493=DIRECTION ( 'NONE',  ( 1.000000000000000000, 0.000000000000000000, 0.000000000000000000 ) ) ;
#12500=CARTESIAN_POINT ( 'NONE',  ( -0.5900578684300998855, -82.27212043593699775, -1.108170840844000082 ) ) ;
#12541=CARTESIAN_POINT ( 'NONE',  ( -1.199500263597274685, -78.44791666666668561, 0.9218200799623673669 ) ) ;
#12549=VERTEX_POINT ( 'NONE', #32001 ) ;
#12564=B_SPLINE_CURVE_WITH_KNOTS ( 'NONE', 3,
 ( #17724, #35711, #48444, #44009 ),
 .UNSPECIFIED., .F., .F.,
 ( 4, 4 ),
 ( 0.000000000000000000, 1.000000000000000000 ),
 .UNSPECIFIED. ) ;
#12571=CARTESIAN_POINT ( 'NONE',  ( 0.7034081407617550630, -79.57886472181323256, 1.062556203884562844 ) ) ;
#12576=CARTESIAN_POINT ( 'NONE',  ( -1.179157772963000061, -82.13943273986299687, 0.6230118014947999550 ) ) ;
#12590=CARTESIAN_POINT ( 'NONE',  ( 1.293420685949000060, -79.34100130914399074, 0.7912046490545000532 ) ) ;
#12607=EDGE_LOOP ( 'NONE', ( #19375, #27047, #19191, #35608, #49345, #57470, #33009, #38594, #21394 ) ) ;
#12613=CARTESIAN_POINT ( 'NONE',  ( -0.2776637860332794583, -79.54227634049593121, 1.244172164868827757 ) ) ;
#12630=CARTESIAN_POINT ( 'NONE',  ( -0.1131650557487513253, -80.86835801496910392, -1.320356500459302307 ) ) ;
#12689=ORIENTED_EDGE ( 'NONE', *, *, #27360, .T. ) ;
#12693=CARTESIAN_POINT ( 'NONE',  ( 1.086271320152000008, -79.49177606238200156, -0.9110860045855999623 ) ) ;
#12695=CARTESIAN_POINT ( 'NONE',  ( 1.301001062148999798, -78.42132866053150053, 0.2190019327816999928 ) ) ;
#12708=CIRCLE ( 'NONE', #35319, 4.000000000000000000 ) ;
#12719=ORIENTED_EDGE ( 'NONE', *, *, #24622, .F. ) ;
#12731=VERTEX_POINT ( 'NONE', #37605 ) ;
#12759=ORIENTED_EDGE ( 'NONE', *, *, #14422, .T. ) ;
#12762=CARTESIAN_POINT ( 'NONE',  ( -0.3926218265389255779, -77.89583333333338544, 1.460959015002472494 ) ) ;
#12782=CARTESIAN_POINT ( 'NONE',  ( -0.3713770062794000126, -82.28702925038599858, -1.193557338046999927 ) ) ;
#12819=CARTESIAN_POINT ( 'NONE',  ( -1.494228022679999768, -80.96100974943900042, 0.6119612316942000252 ) ) ;
#12823=CARTESIAN_POINT ( 'NONE',  ( -1.310679582531389498, -78.45833333333332860, 0.7554284705563444335 ) ) ;
#12832=ORIENTED_EDGE ( 'NONE', *, *, #36248, .F. ) ;
#12836=CARTESIAN_POINT ( 'NONE',  ( -0.6056189234361001317, -80.30937613589500756, -1.188192690176999911 ) ) ;
#12851=CARTESIAN_POINT ( 'NONE',  ( 1.062425010523426527, -80.45345406285113654, -0.7035154447333287209 ) ) ;
#12854=CARTESIAN_POINT ( 'NONE',  ( 0.000000000000000000, -77.40000000000736691, 0.000000000000000000 ) ) ;
#12855=CARTESIAN_POINT ( 'NONE',  ( -1.234140985588999984, -81.14718027224098762, 0.5054425604136000283 ) ) ;
#12863=DIRECTION ( 'NONE',  ( 0.8320502943378438321, -0.5547001962252288143, 2.960700184868154238E-12 ) ) ;
#12865=CARTESIAN_POINT ( 'NONE',  ( 1.330850115287000035, -81.57385641401499754, 0.4611193915267000065 ) ) ;
#12870=CARTESIAN_POINT ( 'NONE',  ( 0.5881506857339000582, -79.39061393252499954, 1.397505295191999952 ) ) ;
#12871=EDGE_LOOP ( 'NONE', ( #27038, #9423, #20374 ) ) ;
#12874=CARTESIAN_POINT ( 'NONE',  ( -0.1738511558967903159, -82.17838541666473873, 1.321614583343871274 ) ) ;
#12892=CARTESIAN_POINT ( 'NONE',  ( 0.7352315925313128719, -82.04166666286488407, -1.273945750275897071 ) ) ;
#12894=CARTESIAN_POINT ( 'NONE',  ( -1.084778369707915413, -80.19423709646559928, -0.6700028332395955299 ) ) ;
#12896=B_SPLINE_CURVE_WITH_KNOTS ( 'NONE', 3,
 ( #37876, #19299, #37583, #37290, #20177, #46182, #10744, #24886, #11320, #29019, #6000, #46772, #38164, #15450, #50604, #15736, #10153, #55306 ),
 .UNSPECIFIED., .F., .F.,
 ( 4, 2, 2, 2, 2, 2, 2, 2, 4 ),
 ( 0.000000000000000000, 0.1250000000000000000, 0.2500000000000000000, 0.3750000000000000000, 0.5000000000000000000, 0.6250000000000000000, 0.7500000000000000000, 0.8750000000000000000, 1.000000000000000000 ),
 .UNSPECIFIED. ) ;
#12911=CARTESIAN_POINT ( 'NONE',  ( 1.316195966539962292, -81.00943227468225416, 0.1540212709399112478 ) ) ;
#12917=CARTESIAN_POINT ( 'NONE',  ( -0.6149910796752999786, -79.26092107675799525, 1.385894317580000035 ) ) ;
#12973=CARTESIAN_POINT ( 'NONE',  ( 1.243995776054000135, -80.08712754295498826, 0.6800984409344000836 ) ) ;
#12975=CARTESIAN_POINT ( 'NONE',  ( -0.5931688960305999681, -78.57016653067499590, 1.178438064142999897 ) ) ;
#12986=DIRECTION ( 'NONE',  ( 6.203992508747998875E-09, -1.000000000000000000, 6.182590554452000020E-10 ) ) ;
#12995=CARTESIAN_POINT ( 'NONE',  ( -0.6201509082777801884, -79.16543617070907146, 1.113615692535757429 ) ) ;
#13000=CARTESIAN_POINT ( 'NONE',  ( -0.6747260877994001316, -82.22962677363800310, -1.052256958371999840 ) ) ;
#13002=CARTESIAN_POINT ( 'NONE',  ( -1.500000000000000000, -79.39999999999999147, 0.000000000000000000 ) ) ;
#13056=EDGE_LOOP ( 'NONE', ( #36641, #22565, #8748, #41660 ) ) ;
#13067=CARTESIAN_POINT ( 'NONE',  ( -0.5900578684300998855, -82.23765691653800047, -1.108170840844000082 ) ) ;
#13096=CARTESIAN_POINT ( 'NONE',  ( 0.03840800099673202100, -77.77721185482320720, -1.273617133072684426 ) ) ;
#13105=CARTESIAN_POINT ( 'NONE',  ( -1.365100536947999821, -80.53103368013600516, -0.7251819899571000372 ) ) ;
#13122=CARTESIAN_POINT ( 'NONE',  ( -0.1698911186725000078, -80.65082589376000044, 1.322768475116000042 ) ) ;
#13141=CARTESIAN_POINT ( 'NONE',  ( -0.6452061973881114687, -80.16722482396566818, 1.099126683074162392 ) ) ;
#13146=CARTESIAN_POINT ( 'NONE',  ( -0.4870599102559999838, -82.27173306887900139, -1.180149847382000017 ) ) ;
#13154=CARTESIAN_POINT ( 'NONE',  ( -0.7187448651093000240, -81.71493067372900043, 1.211279877421999940 ) ) ;
#13160=CARTESIAN_POINT ( 'NONE',  ( -0.6438247211726000341, -80.19017497096899660, -1.263150469460000203 ) ) ;
#13196=CARTESIAN_POINT ( 'NONE',  ( 1.500000000000000000, -80.15000000000000568, 0.000000000000000000 ) ) ;
#13202=CARTESIAN_POINT ( 'NONE',  ( -1.321889952614464736, -81.24455604087124527, 0.09328200148542904746 ) ) ;
#13213=CARTESIAN_POINT ( 'NONE',  ( 1.199500263597268246, -80.80208333333334281, 0.9218200799623752495 ) ) ;
#13216=CARTESIAN_POINT ( 'NONE',  ( -0.7554284705563540925, -79.81666666666667709, 1.310679582531384391 ) ) ;
#13217=CARTESIAN_POINT ( 'NONE',  ( -1.403409243600000300, -78.80864840198100296, -0.2012507760191999950 ) ) ;
#13233=VERTEX_POINT ( 'NONE', #54459 ) ;
#13248=FILL_AREA_STYLE ('',( #40719 ) ) ;
#13341=( NAMED_UNIT ( * ) PLANE_ANGLE_UNIT ( ) SI_UNIT ( $, .RADIAN. ) );
#13369=CARTESIAN_POINT ( 'NONE',  ( 0.000000000000000000, -82.50000000000000000, 0.000000000000000000 ) ) ;
#13391=CARTESIAN_POINT ( 'NONE',  ( -0.2213420416186210049, -77.76131037297035675, -1.254942581273592817 ) ) ;
#13399=CARTESIAN_POINT ( 'NONE',  ( -1.499999999985999866, -82.00000000001401190, -1.019196462549000076E-10 ) ) ;
#13418=CARTESIAN_POINT ( 'NONE',  ( 0.5765222740522000233, -80.10508703656800833, 1.202579817323000233 ) ) ;
#13425=DIRECTION ( 'NONE',  ( 0.000000000000000000, 1.000000000000000000, 0.000000000000000000 ) ) ;
#13436=CARTESIAN_POINT ( 'NONE',  ( 0.09626986684956309603, -79.88099558508119458, -1.271715491304152401 ) ) ;
#13437=ORIENTED_EDGE ( 'NONE', *, *, #54768, .T. ) ;
#13442=CARTESIAN_POINT ( 'NONE',  ( 1.193978368322000216, -81.89136962295700073, -0.5941311122250999555 ) ) ;
#13454=CARTESIAN_POINT ( 'NONE',  ( -1.404978054315000113, -81.29170789458800073, 0.09914529170176999973 ) ) ;
#13460=CARTESIAN_POINT ( 'NONE',  ( 1.209428572278999914, -79.39637299687198890, 0.7398254253092000354 ) ) ;
#13463=CARTESIAN_POINT ( 'NONE',  ( 1.199500263597271577, -79.09791666666667709, -0.9218200799623702535 ) ) ;
#13482=CARTESIAN_POINT ( 'NONE',  ( 1.310737403901690357, -81.69186661536872407, 0.7553186815146348820 ) ) ;
#13485=CARTESIAN_POINT ( 'NONE',  ( -0.6450463279315846732, -80.06702524164226986, 1.098828897408985261 ) ) ;
#13509=CARTESIAN_POINT ( 'NONE',  ( 0.3299670982549000042, -79.26668014110398985, 1.580613947285000043 ) ) ;
#13515=CARTESIAN_POINT ( 'NONE',  ( -1.199500263597274241, -79.84791666666664867, 0.9218200799623669228 ) ) ;
#13516=CARTESIAN_POINT ( 'NONE',  ( 1.398095685538000010, -78.56058528507598737, 0.2353462009024000212 ) ) ;
#13521=CARTESIAN_POINT ( 'NONE',  ( -1.250000000000000000, -77.75000000000000000, 0.000000000000000000 ) ) ;
#13524=CARTESIAN_POINT ( 'NONE',  ( 1.460959015002474048, -81.72916666666669983, -0.3926218265389178064 ) ) ;
#13533=DIRECTION ( 'NONE',  ( 1.000000000000000000, 0.000000000000000000, 0.000000000000000000 ) ) ;
#13538=CARTESIAN_POINT ( 'NONE',  ( 0.7554284705563509839, -81.56666666666669130, -1.310679582531386167 ) ) ;
#13551=ORIENTED_EDGE ( 'NONE', *, *, #34135, .T. ) ;
#13569=CARTESIAN_POINT ( 'NONE',  ( 1.130428667122000075, -80.59477190545899816, -1.152972209120999958 ) ) ;
#13698=CARTESIAN_POINT ( 'NONE',  ( 0.8346931312170999817, -80.71870569687999364, -1.265782155144000054 ) ) ;
#13729=CARTESIAN_POINT ( 'NONE',  ( -1.295435361468000091, -77.74096878701278968, -0.3166359884281000348 ) ) ;
#13736=CARTESIAN_POINT ( 'NONE',  ( -1.234140985588999984, -81.23472830739800088, 0.5054425604136000283 ) ) ;
#13745=CARTESIAN_POINT ( 'NONE',  ( -1.296597938961999930, -81.75360849247699946, -0.1914542273854999976 ) ) ;
#13768=AXIS2_PLACEMENT_3D ( 'NONE', #44883, #53740, #35118 ) ;
#13772=CARTESIAN_POINT ( 'NONE',  ( 0.7834266488161117925, -81.73351092137228591, 1.338899150759432333 ) ) ;
#13808=CARTESIAN_POINT ( 'NONE',  ( 1.045500971020000058, -79.10632414226799369, 0.9575944129536000382 ) ) ;
#13812=CIRCLE ( 'NONE', #13768, 2.000000000000000000 ) ;
#13831=DIRECTION ( 'NONE',  ( 0.000000000000000000, -1.000000000000000000, 0.000000000000000000 ) ) ;
#13832=CARTESIAN_POINT ( 'NONE',  ( 0.9218200799623741393, -81.57708333333334849, -1.199500263597268690 ) ) ;
#13863=CARTESIAN_POINT ( 'NONE',  ( 0.3742884389835000047, -79.49753512672899092, -1.469294133937999902 ) ) ;
#13865=CARTESIAN_POINT ( 'NONE',  ( 0.6775591888709999733, -77.82597717995859909, -1.132025780260999870 ) ) ;
#13867=EDGE_CURVE ( 'NONE', #51104, #29318, #2072, .T. ) ;
#13880=CARTESIAN_POINT ( 'NONE',  ( -0.3862712429687000237, -82.25000000000000000, -1.188820645369000006 ) ) ;
#13904=AXIS2_PLACEMENT_3D ( 'NONE', #10748, #24602, #23721 ) ;
#13910=CARTESIAN_POINT ( 'NONE',  ( 1.199500263597271799, -81.19791666666667140, -0.9218200799623701425 ) ) ;
#13990=CARTESIAN_POINT ( 'NONE',  ( -1.462679955183999958, -81.45713598324900317, 0.6839453740269999527 ) ) ;
#14006=FACE_OUTER_BOUND ( 'NONE', #34021, .T. ) ;
#14007=CARTESIAN_POINT ( 'NONE',  ( 0.2659376973789999710, -79.90663654304400154, -1.306848610430999980 ) ) ;
#14020=CARTESIAN_POINT ( 'NONE',  ( 1.324344358081999795, -78.98128437153999926, 0.1571239973995999795 ) ) ;
#14043=CARTESIAN_POINT ( 'NONE',  ( -0.1202781060011000047, -80.91550986868499251, -1.403348216202000120 ) ) ;
#14049=CARTESIAN_POINT ( 'NONE',  ( -0.8374915928969000056, -80.72513535138099883, -0.9453856285906999668 ) ) ;
#14052=CARTESIAN_POINT ( 'NONE',  ( -1.310679582531386389, -78.94166666666664867, -0.7554284705563492075 ) ) ;
#14071=EDGE_LOOP ( 'NONE', ( #37173, #11468, #30014, #14786 ) ) ;
#14072=CARTESIAN_POINT ( 'NONE',  ( -0.8487208968565155276, -79.71719264087836621, -0.9500917389677994151 ) ) ;
#14085=CARTESIAN_POINT ( 'NONE',  ( -0.4872545538094000261, -79.22957563311599927, -1.241463230931000084 ) ) ;
#14106=CARTESIAN_POINT ( 'NONE',  ( -1.256882289721999779, -78.75903577859999416, 0.6559773548962000156 ) ) ;
#14122=CARTESIAN_POINT ( 'NONE',  ( 1.401388975520859947, -80.71718075262650416, -0.6178868534844423888 ) ) ;
#14125=CARTESIAN_POINT ( 'NONE',  ( 1.302799686710000016, -77.90148386876100517, 0.2851120931344000020 ) ) ;
#14126=CARTESIAN_POINT ( 'NONE',  ( 1.250000000000000000, -76.40000000064199526, 0.000000000000000000 ) ) ;
#14133=VERTEX_POINT ( 'NONE', #54373 ) ;
#14150=CARTESIAN_POINT ( 'NONE',  ( 1.493900225960000050, -80.58901284111300356, -0.2592381030950999810 ) ) ;
#14257=CARTESIAN_POINT ( 'NONE',  ( -1.500000000000000000, -79.50000000000000000, 0.000000000000000000 ) ) ;
#14276=CARTESIAN_POINT ( 'NONE',  ( -0.5537454541186001000, -82.14093423380400338, -1.341729424668000048 ) ) ;
#14293=CARTESIAN_POINT ( 'NONE',  ( 0.000000000000000000, -76.39999999999899671, 0.000000000000000000 ) ) ;
#14296=CARTESIAN_POINT ( 'NONE',  ( -1.180685663403765906, -79.24320892454549892, -0.4090891148645076081 ) ) ;
#14308=CARTESIAN_POINT ( 'NONE',  ( 0.6849175148897999055, -77.93358067473459982, -1.144319635748999975 ) ) ;
#14328=CARTESIAN_POINT ( 'NONE',  ( -1.502550642848000217, -81.34707958231599889, 0.1060307108173999951 ) ) ;
#14334=CARTESIAN_POINT ( 'NONE',  ( -1.108343018679999847, -79.20368156769499990, -0.7155276831893999656 ) ) ;
#14352=DIRECTION ( 'NONE',  ( 1.000000000000000000, 0.000000000000000000, 0.000000000000000000 ) ) ;
#14354=LINE ( 'NONE', #27640, #25239 ) ;
#14355=EDGE_LOOP ( 'NONE', ( #22024, #2751, #36379, #41750 ) ) ;
#14390=CARTESIAN_POINT ( 'NONE',  ( 1.310679582531385501, -79.69166666666669130, 0.7554284705563518720 ) ) ;
#14391=CARTESIAN_POINT ( 'NONE',  ( 1.495190308928000089, -78.61595697280399975, 0.2516904690231000497 ) ) ;
#14422=EDGE_CURVE ( 'NONE', #9344, #54221, #32018, .T. ) ;
#14453=B_SPLINE_SURFACE_WITH_KNOTS ( 'NONE', 3, 3, ( 
 ( #5655, #1542, #41676, #1257, #14800, #55545, #15096, #32794, #10388, #5948, #19534, #43421, #43142, #44281, #35399, #25405, #17126, #30108, #34539, #21838, #25118, #8267, #16271, #56714, #3273, #47872, #48723, #44002, #3840, #3552, #52572, #57282, #39271, #21265, #57564 ),
 ( #35109, #53430, #7978, #48436, #39843, #12693, #57858, #11841, #48159, #2701, #29822, #30686, #39560, #26268, #34250, #7690, #7402, #12973, #20695, #25691, #7118, #38694, #25975, #2981, #43720, #20979, #12410, #38983, #56994, #16556, #16846, #34828, #52856, #30400, #41319 ),
 ( #18602, #35704, #36591, #619, #13863, #49305, #18307, #36880, #329, #36300, #40738, #9154, #41028, #9734, #903, #23311, #54323, #49008, #54027, #31859, #8856, #30971, #49900, #27723, #9445, #53733, #14150, #5012, #8556, #27435, #31559, #4727, #26846, #23017, #54612 ),
 ( #45470, #31263, #44574, #54892, #32150, #18884, #50189, #26548, #45767, #5301, #4130, #22129, #40140, #17720, #44876, #58153, #22725, #4429, #22429, #40442, #27138, #45177, #31, #18011, #36003, #13569, #49607, #10617, #33612, #51069, #15616, #42781, #33022, #28598, #32726 ) ),
 .UNSPECIFIED., .F., .F., .F.,
 ( 4, 4 ),
 ( 4, 1, 1, 1, 1, 1, 1, 1, 1, 1, 1, 1, 1, 1, 1, 1, 1, 1, 1, 1, 1, 1, 1, 1, 1, 1, 1, 1, 1, 1, 1, 1, 4 ),
 ( -0.05371687727926999917, 1.053716877278999986 ),
 ( -0.02000000000000000042, 0.01250000000000000069, 0.04499999999999999833, 0.07749999999999999944, 0.1100000000000000006, 0.1424999999999999878, 0.1749999999999999889, 0.2074999999999999900, 0.2399999999999999911, 0.2725000000000000200, 0.3049999999999999933, 0.3375000000000000222, 0.3699999999999999956, 0.4025000000000000244, 0.4349999999999999978, 0.4675000000000000266, 0.5000000000000000000, 0.5324999999999999734, 0.5649999999999999467, 0.5975000000000000311, 0.6300000000000000044, 0.6624999999999999778, 0.6949999999999999512, 0.7275000000000000355, 0.7600000000000000089, 0.7924999999999999822, 0.8249999999999999556, 0.8575000000000000400, 0.8900000000000000133, 0.9224999999999999867, 0.9549999999999999600, 0.9875000000000000444, 1.020000000000000018 ),
 .UNSPECIFIED. ) ;
#14484=CARTESIAN_POINT ( 'NONE',  ( 0.8380226388207999699, -80.97828694247898795, 1.018961948080000068 ) ) ;
#14513=CARTESIAN_POINT ( 'NONE',  ( 1.310679582531385279, -77.79166666666667140, 0.7554284705563519831 ) ) ;
#14547=PLANE ( 'NONE',  #2536 ) ;
#14564=DIRECTION ( 'NONE',  ( 1.000000000000000000, 0.000000000000000000, 0.000000000000000000 ) ) ;
#14570=CARTESIAN_POINT ( 'NONE',  ( -0.8036425357743999243, -80.96676881378600399, 1.285729672962000025 ) ) ;
#14571=EDGE_LOOP ( 'NONE', ( #19595, #20540, #18736, #19544 ) ) ;
#14573=CARTESIAN_POINT ( 'NONE',  ( -1.499999999985999866, -82.00000000001401190, -1.019196462549000076E-10 ) ) ;
#14586=CARTESIAN_POINT ( 'NONE',  ( -1.310679582531389498, -79.45833333333332860, 0.7554284705563444335 ) ) ;
#14590=CARTESIAN_POINT ( 'NONE',  ( -1.180685663403765906, -79.20987559121225274, -0.4090891148645076081 ) ) ;
#14601=CARTESIAN_POINT ( 'NONE',  ( -0.8668440880359000733, -77.79058141039379848, -1.013523202003999923 ) ) ;
#14604=LINE ( 'NONE', #28468, #32587 ) ;
#14621=CARTESIAN_POINT ( 'NONE',  ( -0.8185753169346000613, -81.82567404918501097, 1.379521242779999879 ) ) ;
#14627=DIRECTION ( 'NONE',  ( 0.000000000000000000, 0.000000000000000000, -1.000000000000000000 ) ) ;
#14659=CARTESIAN_POINT ( 'NONE',  ( -1.308081345731999967, -80.61872908778599367, 0.2599445073669000017 ) ) ;
#14700=ORIENTED_EDGE ( 'NONE', *, *, #15421, .T. ) ;
#14701=CARTESIAN_POINT ( 'NONE',  ( 1.460959015002474493, -78.62916666666664867, -0.3926218265389176953 ) ) ;
#14756=EDGE_CURVE ( 'NONE', #45960, #32054, #48481, .T. ) ;
#14786=ORIENTED_EDGE ( 'NONE', *, *, #18366, .F. ) ;
#14788=CYLINDRICAL_SURFACE ( 'NONE', #8589, 1.500000000000000000 ) ;
#14797=ORIENTED_EDGE ( 'NONE', *, *, #5534, .F. ) ;
#14800=CARTESIAN_POINT ( 'NONE',  ( 0.3256773761571999937, -79.38679175127299459, -1.278468177226000035 ) ) ;
#14803=CARTESIAN_POINT ( 'NONE',  ( -1.163821121499999833, -78.55288933763399939, -1.119256147183999905 ) ) ;
#14841=CARTESIAN_POINT ( 'NONE',  ( 1.310679582531387943, -79.70833333333334281, -0.7554284705563468760 ) ) ;
#14859=CARTESIAN_POINT ( 'NONE',  ( -1.490057467831999993, -81.56212029435899069, -0.2804833236429000176 ) ) ;
#14862=CARTESIAN_POINT ( 'NONE',  ( -0.1963495408493673433, -81.88541666667427421, 1.499999999999999334 ) ) ;
#14875=ADVANCED_FACE ( 'NONE', ( #53686 ), #36552, .F. ) ;
#14891=CARTESIAN_POINT ( 'NONE',  ( -0.5996107393304999089, -78.63399600787198551, 1.191235959310000148 ) ) ;
#14900=DIRECTION ( 'NONE',  ( -1.140590449755075033E-08, -0.7071067811865474617, 0.7071067811865474617 ) ) ;
#14910=CARTESIAN_POINT ( 'NONE',  ( -1.360024375902000093, -81.81732711469500430, 0.6474833154074999264 ) ) ;
#14913=EDGE_CURVE ( 'NONE', #32054, #9701, #7378, .T. ) ;
#14918=CARTESIAN_POINT ( 'NONE',  ( 1.315649220613000159, -79.40213206121900669, -0.09814633906038999767 ) ) ;
#14929=ORIENTED_EDGE ( 'NONE', *, *, #14913, .F. ) ;
#14930=ORIENTED_EDGE ( 'NONE', *, *, #43557, .F. ) ;
#14955=CARTESIAN_POINT ( 'NONE',  ( -1.120379678216000041, -79.17996300973499046, -0.7232983489183999470 ) ) ;
#14977=ORIENTED_EDGE ( 'NONE', *, *, #38413, .T. ) ;
#14994=CARTESIAN_POINT ( 'NONE',  ( -0.7022187824378000043, -82.19906693409399168, -1.095132696781000003 ) ) ;
#14996=CARTESIAN_POINT ( 'NONE',  ( 0.9384621721472999889, -78.44722272595291201, 0.9475573338641000154 ) ) ;
#15040=ORIENTED_EDGE ( 'NONE', *, *, #31457, .T. ) ;
#15054=CARTESIAN_POINT ( 'NONE',  ( 0.7833523767573995489, -81.06795188156627319, -1.316067733153899688 ) ) ;
#15067=CARTESIAN_POINT ( 'NONE',  ( -0.4818272427706999927, -82.25167760925999971, -1.167471054476999948 ) ) ;
#15075=DIRECTION ( 'NONE',  ( 0.000000000000000000, 0.000000000000000000, -1.000000000000000000 ) ) ;
#15085=CARTESIAN_POINT ( 'NONE',  ( -1.310679582531389276, -80.35833333333332007, 0.7554284705563443225 ) ) ;
#15096=CARTESIAN_POINT ( 'NONE',  ( 1.315649220613000159, -79.48601699803499798, -0.09814633906038999767 ) ) ;
#15098=CARTESIAN_POINT ( 'NONE',  ( -1.521132372192000037, -77.47794916437754864, 0.2748539626865999508 ) ) ;
#15104=ADVANCED_FACE ( 'NONE', ( #43315 ), #41330, .F. ) ;
#15115=CARTESIAN_POINT ( 'NONE',  ( 1.232757602695059962, -78.02051921516918753, 0.3250462290969571844 ) ) ;
#15124=CARTESIAN_POINT ( 'NONE',  ( -0.8719406389885000497, -81.33395355416099903, -1.009106372638000071 ) ) ;
#15138=CARTESIAN_POINT ( 'NONE',  ( 0.9218200799623742503, -79.67708333333332860, -1.199500263597268912 ) ) ;
#15143=LINE ( 'NONE', #5701, #12266 ) ;
#15157=CARTESIAN_POINT ( 'NONE',  ( -1.378883651915999931, -81.12136574827599134, -0.3297563563739999704 ) ) ;
#15168=EDGE_CURVE ( 'NONE', #31705, #50394, #9480, .T. ) ;
#15175=VECTOR ( 'NONE', #53647, 1000.000000000000000 ) ;
#15190=CARTESIAN_POINT ( 'NONE',  ( 1.000000000000000000, -82.50000000000000000, 0.000000000000000000 ) ) ;
#15208=CARTESIAN_POINT ( 'NONE',  ( 0.4316438933813000478, -81.26137701033098892, 1.544936262575999919 ) ) ;
#15215=CARTESIAN_POINT ( 'NONE',  ( -1.500000000000000444, -80.88958333333332007, 0.1963495408493560745 ) ) ;
#15255=CARTESIAN_POINT ( 'NONE',  ( 1.137658753740000028, -79.42802612664000605, 0.6959227610743999870 ) ) ;
#15268=CARTESIAN_POINT ( 'NONE',  ( 1.304222966381000104, -81.40108199494899566, 0.2785293583740000023 ) ) ;
#15285=B_SPLINE_CURVE_WITH_KNOTS ( 'NONE', 3,
 ( #2783, #47680, #24924, #24350 ),
 .UNSPECIFIED., .F., .F.,
 ( 4, 4 ),
 ( 0.000000000000000000, 1.000000000000000000 ),
 .UNSPECIFIED. ) ;
#15295=CARTESIAN_POINT ( 'NONE',  ( -0.2406813341972999787, -78.74489846623899325, -1.311734976874999958 ) ) ;
#15305=ORIENTED_EDGE ( 'NONE', *, *, #5534, .T. ) ;
#15306=ORIENTED_EDGE ( 'NONE', *, *, #24648, .T. ) ;
#15365=AXIS2_PLACEMENT_3D ( 'NONE', #15496, #56812, #34350 ) ;
#15373=CARTESIAN_POINT ( 'NONE',  ( -1.268608120215463542, -78.14294593744003237, 0.1161361650036817905 ) ) ;
#15399=CARTESIAN_POINT ( 'NONE',  ( 1.482146596920999926, -77.70947474015589762, -0.6406678853001999130 ) ) ;
#15402=DIRECTION ( 'NONE',  ( 1.000000000000000000, 0.000000000000000000, 0.000000000000000000 ) ) ;
#15416=CARTESIAN_POINT ( 'NONE',  ( 1.030546858859699766, -78.44986307349660137, -0.7510367337251727671 ) ) ;
#15421=EDGE_CURVE ( 'NONE', #39914, #11684, #20052, .T. ) ;
#15426=CARTESIAN_POINT ( 'NONE',  ( -0.4870599102559999838, -82.31550708645799830, -1.180149847382000017 ) ) ;
#15450=CARTESIAN_POINT ( 'NONE',  ( 1.199500263597271577, -78.09791666666667709, -0.9218200799623702535 ) ) ;
#15460=CARTESIAN_POINT ( 'NONE',  ( -0.2635301427987000178, -82.15747177493101105, -1.396495434320000006 ) ) ;
#15471=VERTEX_POINT ( 'NONE', #37963 ) ;
#15477=LINE ( 'NONE', #24036, #45484 ) ;
#15496=CARTESIAN_POINT ( 'NONE',  ( 0.000000000000000000, -82.00000000000000000, 0.000000000000000000 ) ) ;
#15508=CARTESIAN_POINT ( 'NONE',  ( 0.5479250432661000314, -82.06079781537400208, -1.507621479251000096 ) ) ;
#15550=CARTESIAN_POINT ( 'NONE',  ( -1.319155384867000125, -80.16637687155399306, 0.1959724986398999891 ) ) ;
#15564=CARTESIAN_POINT ( 'NONE',  ( -1.208084210770999922, -81.59953248847399720, 0.5648970606752000689 ) ) ;
#15565=CARTESIAN_POINT ( 'NONE',  ( -1.310679582531386389, -80.44166666666664867, -0.7554284705563492075 ) ) ;
#15582=CARTESIAN_POINT ( 'NONE',  ( 1.452792874191000116, -80.27788208903798761, 0.7047031062512999489 ) ) ;
#15587=CARTESIAN_POINT ( 'NONE',  ( 1.166929042523999982, -78.84412371300099664, -0.6456414311070000078 ) ) ;
#15616=CARTESIAN_POINT ( 'NONE',  ( -1.102025757167999886, -80.84283502236499430, 1.180137589876000037 ) ) ;
#15657=CARTESIAN_POINT ( 'NONE',  ( -0.8704825706172066857, -78.71539928414449605, -0.9315426300253514258 ) ) ;
#15671=CARTESIAN_POINT ( 'NONE',  ( 1.500000000000000000, -80.15000000000000568, 0.000000000000000000 ) ) ;
#15677=CARTESIAN_POINT ( 'NONE',  ( -1.500000000000000000, -80.00000000000000000, 0.000000000000000000 ) ) ;
#15686=CARTESIAN_POINT ( 'NONE',  ( 1.272474653676000100, -78.31634434942250778, -0.6251940786299999830 ) ) ;
#15712=CARTESIAN_POINT ( 'NONE',  ( 0.8181542670502196524, -80.83029637058210426, -0.9768312912188416020 ) ) ;
#15713=VERTEX_POINT ( 'NONE', #17092 ) ;
#15714=CARTESIAN_POINT ( 'NONE',  ( -0.9200108141794000050, -81.83007978797098758, -0.9654823929056000065 ) ) ;
#15732=DIRECTION ( 'NONE',  ( 0.000000000000000000, -1.000000000000000000, 0.000000000000000000 ) ) ;
#15736=CARTESIAN_POINT ( 'NONE',  ( 1.460959015002474493, -78.12916666666669130, -0.3926218265389176953 ) ) ;
#15752=EDGE_CURVE ( 'NONE', #43416, #17252, #34633, .T. ) ;
#15765=EDGE_CURVE ( 'NONE', #51480, #14133, #31230, .T. ) ;
#15767=CARTESIAN_POINT ( 'NONE',  ( -0.4779922839590000083, -82.25159812202299747, -1.146319568230000030 ) ) ;
#15775=DIRECTION ( 'NONE',  ( 0.000000000000000000, 1.000000000000000000, 0.000000000000000000 ) ) ;
#15788=CARTESIAN_POINT ( 'NONE',  ( -1.333333333333333259, -77.60000000000000853, 0.000000000000000000 ) ) ;
#15818=VECTOR ( 'NONE', #17680, 1000.000000000000000 ) ;
#15842=CARTESIAN_POINT ( 'NONE',  ( -1.248430190247999949, -79.17412440393199802, 0.06262635289305999720 ) ) ;
#15847=DIRECTION ( 'NONE',  ( 1.000000000000000000, 0.000000000000000000, 0.000000000000000000 ) ) ;
#15853=B_SPLINE_SURFACE_WITH_KNOTS ( 'NONE', 3, 3, ( 
 ( #7012, #2026, #20024, #38878, #21161, #29718, #29147, #25014, #56898, #39167, #33282, #3171, #56607, #25303, #51323, #46903, #11172, #16455, #2597, #7301, #6429, #16167, #34437, #12025, #34145, #52185, #38008, #15582, #30005, #24733, #33577, #51616, #48059, #7590, #25589 ),
 ( #43611, #47766, #47193, #6725, #42747, #20306, #38301, #12590, #12870, #4319, #22622, #40633, #45070, #22023, #8747, #4622, #16743, #53043, #27033, #26738, #53928, #21735, #35010, #44769, #22318, #26169, #17309, #30297, #34723, #48336, #21454, #35295, #17605, #12307, #40335 ),
 ( #4017, #52753, #39742, #44466, #30589, #7875, #35594, #13460, #53622, #53325, #44188, #58344, #48620, #58045, #30873, #48908, #8167, #17907, #35896, #25877, #3734, #57752, #43904, #13160, #8449, #49498, #26444, #3448, #9047, #39461, #40031, #57465, #31157, #49195, #17026 ),
 ( #27331, #9342, #14334, #514, #1368, #55081, #14918, #54216, #49796, #50378, #228, #23490, #32913, #19364, #36198, #32620, #36483, #23204, #23781, #37063, #41796, #40927, #10214, #28193, #45953, #9925, #41503, #54791, #45365, #46246, #37357, #4914, #41209, #14049, #5774 ) ),
 .UNSPECIFIED., .F., .F., .F.,
 ( 4, 4 ),
 ( 4, 1, 1, 1, 1, 1, 1, 1, 1, 1, 1, 1, 1, 1, 1, 1, 1, 1, 1, 1, 1, 1, 1, 1, 1, 1, 1, 1, 1, 1, 1, 1, 4 ),
 ( -0.05371687727927999811, 1.053716877278999986 ),
 ( -0.02000000000000000042, 0.01250000000000000069, 0.04499999999999999833, 0.07749999999999999944, 0.1100000000000000006, 0.1424999999999999878, 0.1749999999999999889, 0.2074999999999999900, 0.2399999999999999911, 0.2725000000000000200, 0.3049999999999999933, 0.3375000000000000222, 0.3699999999999999956, 0.4025000000000000244, 0.4349999999999999978, 0.4675000000000000266, 0.5000000000000000000, 0.5324999999999999734, 0.5649999999999999467, 0.5975000000000000311, 0.6300000000000000044, 0.6624999999999999778, 0.6949999999999999512, 0.7275000000000000355, 0.7600000000000000089, 0.7924999999999999822, 0.8249999999999999556, 0.8575000000000000400, 0.8900000000000000133, 0.9224999999999999867, 0.9549999999999999600, 0.9875000000000000444, 1.020000000000000018 ),
 .UNSPECIFIED. ) ;
#15857=CARTESIAN_POINT ( 'NONE',  ( 1.316231252753000014, -81.89720822875999318, 0.2147359707272000207 ) ) ;
#15866=FACE_OUTER_BOUND ( 'NONE', #24453, .T. ) ;
#15880=CARTESIAN_POINT ( 'NONE',  ( 1.315129997485000146, -78.44138412015038853, 0.2213803045116000123 ) ) ;
#15900=LINE ( 'NONE', #56064, #45923 ) ;
#15916=DIRECTION ( 'NONE',  ( 0.000000000000000000, 1.000000000000000000, 0.000000000000000000 ) ) ;
#15940=ORIENTED_EDGE ( 'NONE', *, *, #51363, .F. ) ;
#15945=CARTESIAN_POINT ( 'NONE',  ( -1.397634362971892807, -81.93340492005572173, -0.6272248289412739597 ) ) ;
#15947=CARTESIAN_POINT ( 'NONE',  ( 1.103779259214931585, -78.85851262082059066, -0.6375342514394781723 ) ) ;
#15967=CARTESIAN_POINT ( 'NONE',  ( -0.7554284705563544255, -79.91666666666667140, 1.310679582531384169 ) ) ;
#15972=EDGE_CURVE ( 'NONE', #47577, #22104, #50729, .T. ) ;
#15979=CARTESIAN_POINT ( 'NONE',  ( -1.223493401540999947, -79.06053370013900405, 0.7163828769940999708 ) ) ;
#15998=CARTESIAN_POINT ( 'NONE',  ( 1.012512968712311334, -78.05232246393418905, 0.7737093686211432564 ) ) ;
#16005=CARTESIAN_POINT ( 'NONE',  ( 0.1532075572505490757, -81.78438528175662725, -1.264636186328577105 ) ) ;
#16033=VERTEX_POINT ( 'NONE', #14994 ) ;
#16034=ADVANCED_FACE ( 'NONE', ( #50161 ), #9416, .F. ) ;
#16053=FACE_OUTER_BOUND ( 'NONE', #55100, .T. ) ;
#16061=CARTESIAN_POINT ( 'NONE',  ( -0.7089775319598999870, -82.20557270575599773, -1.075828666865999983 ) ) ;
#16076=CARTESIAN_POINT ( 'NONE',  ( -0.4831833036036000117, -82.22787956406298804, -1.158768654956999988 ) ) ;
#16079=ORIENTED_EDGE ( 'NONE', *, *, #38706, .F. ) ;
#16087=CARTESIAN_POINT ( 'NONE',  ( 1.460959015002474048, -80.22916666666668561, -0.3926218265389178064 ) ) ;
#16088=DIRECTION ( 'NONE',  ( 0.7071067811865474617, -0.7071067811865474617, 7.724133980720514139E-12 ) ) ;
#16089=EDGE_CURVE ( 'NONE', #5425, #34724, #45439, .T. ) ;
#16100=CARTESIAN_POINT ( 'NONE',  ( 0.3926218265389159190, -78.85416666666667140, 1.460959015002474715 ) ) ;
#16135=CARTESIAN_POINT ( 'NONE',  ( 0.5765222740522000233, -80.01753900141099507, 1.202579817323000233 ) ) ;
#16155=ADVANCED_FACE ( 'NONE', ( #2314 ), #20309, .T. ) ;
#16167=CARTESIAN_POINT ( 'NONE',  ( -1.597158643424000157, -79.98020634875099688, 0.2372724044997999993 ) ) ;
#16180=B_SPLINE_CURVE_WITH_KNOTS ( 'NONE', 3,
 ( #4432, #21841, #39848, #30406 ),
 .UNSPECIFIED., .F., .F.,
 ( 4, 4 ),
 ( 0.000000000000000000, 1.000000000000000000 ),
 .UNSPECIFIED. ) ;
#16191=CARTESIAN_POINT ( 'NONE',  ( 1.274386203284063823, -79.39916300381975134, -0.01037360266173210400 ) ) ;
#16196=CARTESIAN_POINT ( 'NONE',  ( 1.199500263597268246, -81.20208333333334849, 0.9218200799623752495 ) ) ;
#16217=DIRECTION ( 'NONE',  ( -0.7071067811865474617, -0.7071067811865474617, 8.526560539801564177E-11 ) ) ;
#16223=CARTESIAN_POINT ( 'NONE',  ( 0.1988171392200138166, -81.03513263419276313, -1.518600332402399999 ) ) ;
#16227=CARTESIAN_POINT ( 'NONE',  ( -0.3862712429687000237, -82.25000000000000000, -1.188820645369000006 ) ) ;
#16243=CARTESIAN_POINT ( 'NONE',  ( 1.073551389641718368, -78.44507409264528519, 0.6868635585880937811 ) ) ;
#16271=CARTESIAN_POINT ( 'NONE',  ( -1.172662378873000177, -80.27981897213200568, -0.6045068694098000295 ) ) ;
#16275=CARTESIAN_POINT ( 'NONE',  ( -1.411465571349000081, -79.11014632351999865, -0.1328074485833999896 ) ) ;
#16296=CARTESIAN_POINT ( 'NONE',  ( -0.3807657621149953542, -79.14953454632663465, 1.216325176385994355 ) ) ;
#16302=CARTESIAN_POINT ( 'NONE',  ( -0.6696908800640647419, -81.06881859837598370, 1.084700732491975517 ) ) ;
#16322=LINE ( 'NONE', #16605, #33112 ) ;
#16332=EDGE_CURVE ( 'NONE', #13233, #23510, #12896, .T. ) ;
#16333=ORIENTED_EDGE ( 'NONE', *, *, #33569, .T. ) ;
#16340=CARTESIAN_POINT ( 'NONE',  ( 1.500000000000000000, -78.25000000000000000, 0.000000000000000000 ) ) ;
#16386=CARTESIAN_POINT ( 'NONE',  ( 1.500000000000000000, -78.76041666666668561, 0.1963495408493652339 ) ) ;
#16416=DIRECTION ( 'NONE',  ( 0.000000000000000000, -1.000000000000000000, 0.000000000000000000 ) ) ;
#16425=CARTESIAN_POINT ( 'NONE',  ( -1.120379678216000041, -79.26751104489200372, -0.7232983489183999470 ) ) ;
#16437=AXIS2_PLACEMENT_3D ( 'NONE', #42997, #16416, #52717 ) ;
#16438=CARTESIAN_POINT ( 'NONE',  ( 0.3926218265389220807, -77.64583333333334281, -1.460959015002473382 ) ) ;
#16439=CARTESIAN_POINT ( 'NONE',  ( -1.302418038466583106, -79.04516373638908533, -0.8227471584171217600 ) ) ;
#16447=PLANE ( 'NONE',  #53109 ) ;
#16455=CARTESIAN_POINT ( 'NONE',  ( 1.416781233620999947, -79.78175585522699009, 0.7745610770380000343 ) ) ;
#16504=EDGE_CURVE ( 'NONE', #31705, #57022, #39297, .T. ) ;
#16519=CARTESIAN_POINT ( 'NONE',  ( -1.417334032777999964, -79.42654225787899236, -0.4910847579886000736 ) ) ;
#16530=CARTESIAN_POINT ( 'NONE',  ( -1.244347653747824634, -78.66769483858584522, -0.2779331296326563172 ) ) ;
#16543=FACE_OUTER_BOUND ( 'NONE', #25116, .T. ) ;
#16556=CARTESIAN_POINT ( 'NONE',  ( -0.1806087918925000091, -80.68247902352800338, 1.406216040666999900 ) ) ;
#16559=CARTESIAN_POINT ( 'NONE',  ( 0.1641065589886999965, -77.91368429802710693, 1.507319194642999793 ) ) ;
#16582=CARTESIAN_POINT ( 'NONE',  ( -1.248018900756835192, -82.16602084622610391, -0.2580508266247266147 ) ) ;
#16596=CARTESIAN_POINT ( 'NONE',  ( -1.250000000000000000, -77.75000000000000000, 0.000000000000000000 ) ) ;
#16605=CARTESIAN_POINT ( 'NONE',  ( -1.249999986291000065, -76.30000000051599329, 0.6999999994844999796 ) ) ;
#16630=MANIFOLD_SOLID_BREP ( 'Stock-MAS-694-1', #28656 ) ;
#16657=DIRECTION ( 'NONE',  ( 0.000000000000000000, 0.000000000000000000, 1.000000000000000000 ) ) ;
#16658=CARTESIAN_POINT ( 'NONE',  ( -1.416666666666666741, -77.54999999999999716, 0.000000000000000000 ) ) ;
#16714=CARTESIAN_POINT ( 'NONE',  ( -0.2976639488673999967, -79.57102539098100635, 1.299989344602000108 ) ) ;
#16725=CARTESIAN_POINT ( 'NONE',  ( 0.1510373474112000070, -81.54408125928999596, 1.325052402434999888 ) ) ;
#16727=ADVANCED_FACE ( 'NONE', ( #44652 ), #29992, .T. ) ;
#16730=CARTESIAN_POINT ( 'NONE',  ( 1.371980222863132592, -79.61275704297987943, -0.7006253647128551920 ) ) ;
#16743=CARTESIAN_POINT ( 'NONE',  ( 1.504745031191999871, -79.78751491957400788, -0.1862378672923999945 ) ) ;
#16747=EDGE_CURVE ( 'NONE', #56598, #22393, #3106, .T. ) ;
#16759=ORIENTED_EDGE ( 'NONE', *, *, #11923, .F. ) ;
#16765=VERTEX_POINT ( 'NONE', #32217 ) ;
#16771=CARTESIAN_POINT ( 'NONE',  ( 0.7554284705563452107, -81.23333333333332007, 1.310679582531388609 ) ) ;
#16789=CARTESIAN_POINT ( 'NONE',  ( -1.568439782227999846, -77.92713930981540216, -0.3833649254202000090 ) ) ;
#16796=CARTESIAN_POINT ( 'NONE',  ( -0.1108284043172000077, -77.86024949339380896, -1.314634435239000032 ) ) ;
#16831=ORIENTED_EDGE ( 'NONE', *, *, #16089, .T. ) ;
#16846=CARTESIAN_POINT ( 'NONE',  ( -0.9676267263329999535, -80.73209164690899797, 1.036212325607999807 ) ) ;
#16848=CARTESIAN_POINT ( 'NONE',  ( -1.344169958103999862, -78.50903577859999416, 0.7015335173854999606 ) ) ;
#16874=CARTESIAN_POINT ( 'NONE',  ( -0.9056407151152020552, -81.21193193505192198, -0.8974757952510434844 ) ) ;
#16972=CONICAL_SURFACE ( 'NONE', #29219, 3.399999999997999733, 0.9827937232471395390 ) ;
#17007=CARTESIAN_POINT ( 'NONE',  ( -1.229805502134054151, -80.77148655050061166, -0.3338661523633573713 ) ) ;
#17010=CARTESIAN_POINT ( 'NONE',  ( -0.6509962010243000030, -81.59369388267100476, 1.163950211895000031 ) ) ;
#17015=CARTESIAN_POINT ( 'NONE',  ( -1.302418038466582884, -79.44516373638910522, -0.8227471584171216490 ) ) ;
#17026=CARTESIAN_POINT ( 'NONE',  ( -0.6603457068528999496, -80.68630120477999412, -1.153171400786999978 ) ) ;
#17029=CARTESIAN_POINT ( 'NONE',  ( 1.406250000003000045, -82.09374999999700151, -9.314605757769000352E-11 ) ) ;
#17068=CARTESIAN_POINT ( 'NONE',  ( 1.482146596920999926, -78.12558980333969316, -0.6406678853001999130 ) ) ;
#17075=CARTESIAN_POINT ( 'NONE',  ( -1.313442439244999926, -79.24940294806400232, -0.1235842678404999867 ) ) ;
#17092=CARTESIAN_POINT ( 'NONE',  ( -1.500000000000000000, -79.39999999999999147, 0.000000000000000000 ) ) ;
#17093=CARTESIAN_POINT ( 'NONE',  ( 0.3926218265389221362, -78.54583333333334849, -1.460959015002473160 ) ) ;
#17096=DIRECTION ( 'NONE',  ( 1.000000000000000000, 0.000000000000000000, 0.000000000000000000 ) ) ;
#17101=AXIS2_PLACEMENT_3D ( 'NONE', #43475, #15732, #11892 ) ;
#17113=CYLINDRICAL_SURFACE ( 'NONE', #49903, 1.500000000000000000 ) ;
#17122=STYLED_ITEM ( 'NONE', ( #22705 ), #463 ) ;
#17126=CARTESIAN_POINT ( 'NONE',  ( 1.309314855877999895, -79.98214323184599550, -0.1620500492231000123 ) ) ;
#17129=CARTESIAN_POINT ( 'NONE',  ( 1.211010829604999950, -77.87558980333969316, -0.5234676170970000708 ) ) ;
#17188=AXIS2_PLACEMENT_3D ( 'NONE', #6130, #55736, #10573 ) ;
#17216=DIRECTION ( 'NONE',  ( 0.000000000000000000, 0.000000000000000000, -1.000000000000000000 ) ) ;
#17236=CARTESIAN_POINT ( 'NONE',  ( -1.500000000000000000, -81.40000000000000568, 0.000000000000000000 ) ) ;
#17252=VERTEX_POINT ( 'NONE', #25420 ) ;
#17261=ORIENTED_EDGE ( 'NONE', *, *, #46258, .T. ) ;
#17269=CARTESIAN_POINT ( 'NONE',  ( -0.9565643533716999825, -80.20431228332999751, 0.9292797142584000580 ) ) ;
#17283=DIRECTION ( 'NONE',  ( 0.000000000000000000, -1.000000000000000000, 0.000000000000000000 ) ) ;
#17287=CARTESIAN_POINT ( 'NONE',  ( -0.8489568036168347875, -79.81738908755133366, -0.9503365090294664252 ) ) ;
#17293=CARTESIAN_POINT ( 'NONE',  ( -0.1187445621502999926, -81.33979215996299672, -1.328335755224000048 ) ) ;
#17304=CARTESIAN_POINT ( 'NONE',  ( -1.107301413750000130, -80.78176359222798908, -0.6019302607798000526 ) ) ;
#17309=CARTESIAN_POINT ( 'NONE',  ( 1.493900225960000050, -80.28364115338500540, -0.2592381030950999810 ) ) ;
#17323=ORIENTED_EDGE ( 'NONE', *, *, #36384, .T. ) ;
#17328=CARTESIAN_POINT ( 'NONE',  ( 1.151164884410004641, -82.06119791428943699, -0.8836085541159298673 ) ) ;
#17330=CARTESIAN_POINT ( 'NONE',  ( 0.2301609875668271243, -80.28964598758351201, -1.253928556708755915 ) ) ;
#17341=CARTESIAN_POINT ( 'NONE',  ( -0.7554284705563483193, -79.98333333333333428, -1.310679582531387721 ) ) ;
#17356=CARTESIAN_POINT ( 'NONE',  ( -1.140592747978000032, -79.46513063462899140, -0.9947442812858000583 ) ) ;
#17357=B_SPLINE_CURVE_WITH_KNOTS ( 'NONE', 3,
 ( #52536, #39237, #44541, #57249, #52822, #12377, #30655, #48408, #3521, #57534, #17093, #44252, #55154, #18575, #46034, #14701, #41289, #1161 ),
 .UNSPECIFIED., .F., .F.,
 ( 4, 2, 2, 2, 2, 2, 2, 2, 4 ),
 ( 0.000000000000000000, 0.1250000000000000000, 0.2500000000000000000, 0.3750000000000000000, 0.5000000000000000000, 0.6250000000000000000, 0.7500000000000000000, 0.8750000000000000000, 1.000000000000000000 ),
 .UNSPECIFIED. ) ;
#17364=CARTESIAN_POINT ( 'NONE',  ( 1.211010829604999950, -77.95947474015589762, -0.5234676170970000708 ) ) ;
#17381=CARTESIAN_POINT ( 'NONE',  ( 0.000000000000000000, -77.50000000000000000, 0.000000000000000000 ) ) ;
#17405=EDGE_CURVE ( 'NONE', #900, #13233, #11856, .T. ) ;
#17435=CARTESIAN_POINT ( 'NONE',  ( -0.6622445160018815002, -78.83150205867622162, -1.088607957794830217 ) ) ;
#17449=EDGE_CURVE ( 'NONE', #33741, #15471, #30983, .T. ) ;
#17474=VERTEX_POINT ( 'NONE', #57576 ) ;
#17509=FACE_OUTER_BOUND ( 'NONE', #40411, .T. ) ;
#17515=CARTESIAN_POINT ( 'NONE',  ( 0.000000000000000000, -82.25000000001401190, -1.249999999985999866 ) ) ;
#17549=ORIENTED_EDGE ( 'NONE', *, *, #24648, .F. ) ;
#17561=EDGE_LOOP ( 'NONE', ( #55236, #44144, #41588, #52032 ) ) ;
#17566=CARTESIAN_POINT ( 'NONE',  ( 0.9788970803261000109, -79.91247514884599923, -0.9057243817226000582 ) ) ;
#17587=CARTESIAN_POINT ( 'NONE',  ( -1.018555708747796107, -80.19902807273064127, 0.7675077034654457231 ) ) ;
#17591=CARTESIAN_POINT ( 'NONE',  ( -1.310615285706999922, -81.73669314701200506, -0.2467057407436999972 ) ) ;
#17599=CARTESIAN_POINT ( 'NONE',  ( -1.241956275658999909, -82.32625246582099976, -0.4726577424567999786 ) ) ;
#17605=CARTESIAN_POINT ( 'NONE',  ( -1.379800422845999908, -80.58131689367100137, -0.6283944928419999965 ) ) ;
#17646=CIRCLE ( 'NONE', #45824, 2.799999999999999822 ) ;
#17653=CARTESIAN_POINT ( 'NONE',  ( -1.049525737143000015, -77.97675193319649622, -1.227116502697000122 ) ) ;
#17662=CARTESIAN_POINT ( 'NONE',  ( 1.272474653676000100, -78.51097266169500699, -0.6251940786299999830 ) ) ;
#17680=DIRECTION ( 'NONE',  ( 1.000000000000000000, 7.077858357939000336E-11, -7.077867239723000107E-11 ) ) ;
#17720=CARTESIAN_POINT ( 'NONE',  ( -0.6623784515263000383, -79.99942042488599725, -1.472572141918999877 ) ) ;
#17724=CARTESIAN_POINT ( 'NONE',  ( -1.417334032777999964, -79.02654225787900089, -0.4910847579886000736 ) ) ;
#17734=CARTESIAN_POINT ( 'NONE',  ( -1.178447680628000205, -80.55308451575899653, -0.9280415206345000723 ) ) ;
#17746=CARTESIAN_POINT ( 'NONE',  ( 0.9218200799623692543, -79.22291666666664867, 1.199500263597272687 ) ) ;
#17765=CARTESIAN_POINT ( 'NONE',  ( -1.199500263597270022, -81.05208333333335702, -0.9218200799623730290 ) ) ;
#17789=ADVANCED_FACE ( 'NONE', ( #17509 ), #48804, .T. ) ;
#17844=CARTESIAN_POINT ( 'NONE',  ( -0.9820397338569999413, -80.80308451575899653, -0.7733679338621000099 ) ) ;
#17850=CARTESIAN_POINT ( 'NONE',  ( 1.445601399883000182, -81.70519910015499931, -0.7193403082786999914 ) ) ;
#17863=VERTEX_POINT ( 'NONE', #2992 ) ;
#17868=CARTESIAN_POINT ( 'NONE',  ( -1.327128730425999992, -79.75779867290000880, 0.1315503032697999675 ) ) ;
#17887=CARTESIAN_POINT ( 'NONE',  ( 0.3449928021110761911, -80.10361832643582147, 1.227624333057440120 ) ) ;
#17892=CARTESIAN_POINT ( 'NONE',  ( -0.1187445621502999926, -81.29601814238500879, -1.328335755224000048 ) ) ;
#17899=EDGE_CURVE ( 'NONE', #34384, #38110, #6545, .T. ) ;
#17901=CARTESIAN_POINT ( 'NONE',  ( 0.07256738472693000097, -81.61253423276301078, 1.308646213179999851 ) ) ;
#17907=CARTESIAN_POINT ( 'NONE',  ( 1.243995776054000135, -79.89249923068300063, 0.6800984409344000836 ) ) ;
#17927=CARTESIAN_POINT ( 'NONE',  ( -0.7555692214694499365, -81.81679953337950906, 1.310938934338384154 ) ) ;
#17929=CARTESIAN_POINT ( 'NONE',  ( 0.09625703868715393408, -79.78079856828991012, -1.271375911578840778 ) ) ;
#17952=CARTESIAN_POINT ( 'NONE',  ( -1.265160441076000009, -79.39322140577399978, -0.7115061034973000353 ) ) ;
#17955=VECTOR ( 'NONE', #22181, 1000.000000000000000 ) ;
#17960=CARTESIAN_POINT ( 'NONE',  ( 1.326698500471999997, -79.06247058323299370, -0.7340390780227000755 ) ) ;
#17968=DIRECTION ( 'NONE',  ( 0.000000000000000000, 0.000000000000000000, 1.000000000000000000 ) ) ;
#17979=DIRECTION ( 'NONE',  ( 0.000000000000000000, 1.000000000000000000, 0.000000000000000000 ) ) ;
#17981=CARTESIAN_POINT ( 'NONE',  ( -0.3926218265389189721, -81.50416666666666288, -1.460959015002473604 ) ) ;
#18011=CARTESIAN_POINT ( 'NONE',  ( -0.7332490996008999007, -80.49554665869699477, -1.438596428395999993 ) ) ;
#18012=CARTESIAN_POINT ( 'NONE',  ( 0.9728932632037999850, -78.96706751772300947, 0.8910916192982000217 ) ) ;
#18086=CIRCLE ( 'NONE', #41644, 0.5000000000000000000 ) ;
#18126=ADVANCED_FACE ( 'NONE', ( #34986 ), #48597, .T. ) ;
#18141=ORIENTED_EDGE ( 'NONE', *, *, #42688, .F. ) ;
#18143=CARTESIAN_POINT ( 'NONE',  ( 0.1828674678246000052, -81.35791073648699978, 1.604298418379999980 ) ) ;
#18152=CARTESIAN_POINT ( 'NONE',  ( 0.7554284705563453217, -78.33333333333334281, 1.310679582531389276 ) ) ;
#18161=DIRECTION ( 'NONE',  ( 0.000000000000000000, 0.000000000000000000, -1.000000000000000000 ) ) ;
#18164=CARTESIAN_POINT ( 'NONE',  ( 0.2020314717676000016, -80.40276277685400430, -1.318241039644999946 ) ) ;
#18179=CARTESIAN_POINT ( 'NONE',  ( 0.8912423865758999364, -78.08241854487779676, 0.9921004264782997684 ) ) ;
#18180=LINE ( 'NONE', #50062, #34533 ) ;
#18183=CARTESIAN_POINT ( 'NONE',  ( 0.4457333967380877615, -80.59656868229342308, 1.193944125407572443 ) ) ;
#18188=CARTESIAN_POINT ( 'NONE',  ( -0.4870599102559999838, -82.35928110403600044, -1.180149847382000017 ) ) ;
#18196=CIRCLE ( 'NONE', #43601, 3.799999999999999822 ) ;
#18200=CARTESIAN_POINT ( 'NONE',  ( 0.6819515120865000668, -80.96253462192299821, -1.232362876918000172 ) ) ;
#18228=ORIENTED_EDGE ( 'NONE', *, *, #11013, .F. ) ;
#18259=CARTESIAN_POINT ( 'NONE',  ( -0.6983046762106999150, -78.21329692140810153, 1.233867887851000100 ) ) ;
#18307=CARTESIAN_POINT ( 'NONE',  ( 1.512024872110000029, -79.59676037349100852, -0.1127957995495999927 ) ) ;
#18353=CARTESIAN_POINT ( 'NONE',  ( 1.500000000000000000, -81.25000000000000000, 0.000000000000000000 ) ) ;
#18358=EDGE_LOOP ( 'NONE', ( #14977, #36106, #56684, #31556, #19094 ) ) ;
#18366=EDGE_CURVE ( 'NONE', #33741, #47577, #18180, .T. ) ;
#18429=CARTESIAN_POINT ( 'NONE',  ( 0.8342270367883455329, -77.96802963705810896, 0.9637654413407948928 ) ) ;
#18430=AXIS2_PLACEMENT_3D ( 'NONE', #25920, #39209, #58390 ) ;
#18435=VERTEX_POINT ( 'NONE', #4600 ) ;
#18452=CARTESIAN_POINT ( 'NONE',  ( -1.261445002938999860, -79.27820998021699950, -0.1968185027220000216 ) ) ;
#18484=CARTESIAN_POINT ( 'NONE',  ( -1.268151001693999858, -80.82146036220999008, -0.3970563801964000494 ) ) ;
#18501=ORIENTED_EDGE ( 'NONE', *, *, #27537, .F. ) ;
#18516=CARTESIAN_POINT ( 'NONE',  ( 0.08737939559041406345, -80.01932079608359061, 1.271311736501290035 ) ) ;
#18528=CARTESIAN_POINT ( 'NONE',  ( 0.5765222740522000233, -79.97376498383199817, 1.202579817323000233 ) ) ;
#18529=EDGE_CURVE ( 'NONE', #12549, #54597, #55350, .T. ) ;
#18551=CARTESIAN_POINT ( 'NONE',  ( -1.223493401540999947, -79.25516201241099168, 0.7163828769940999708 ) ) ;
#18573=DIRECTION ( 'NONE',  ( -1.000000000000000000, 0.000000000000000000, 0.000000000000000000 ) ) ;
#18575=CARTESIAN_POINT ( 'NONE',  ( 1.199500263597271577, -78.59791666666667709, -0.9218200799623702535 ) ) ;
#18602=CARTESIAN_POINT ( 'NONE',  ( -1.419358333703000019, -79.34869725658599293, 0.07120080608633000407 ) ) ;
#18674=CARTESIAN_POINT ( 'NONE',  ( 1.500000000000000000, -78.25000000000000000, 0.000000000000000000 ) ) ;
#18725=CARTESIAN_POINT ( 'NONE',  ( 1.357451270064000015, -81.76057078788299748, -0.6754762517246000186 ) ) ;
#18727=ORIENTED_EDGE ( 'NONE', *, *, #6168, .T. ) ;
#18730=VECTOR ( 'NONE', #12986, 1000.000000000000000 ) ;
#18736=ORIENTED_EDGE ( 'NONE', *, *, #57995, .F. ) ;
#18754=CARTESIAN_POINT ( 'NONE',  ( -1.327706488546999797, -79.22934748844500064, -0.1249263990498000187 ) ) ;
#18775=CARTESIAN_POINT ( 'NONE',  ( 1.551259236285000176, -81.63757503623300238, -0.4083371041875000218 ) ) ;
#18781=CARTESIAN_POINT ( 'NONE',  ( -0.9218200799623775810, -81.42708333333332860, 1.199500263597266247 ) ) ;
#18802=ORIENTED_EDGE ( 'NONE', *, *, #15765, .T. ) ;
#18817=CARTESIAN_POINT ( 'NONE',  ( 1.170174673132000187, -79.92415236045100357, 0.6397400908730001001 ) ) ;
#18826=CARTESIAN_POINT ( 'NONE',  ( 1.069786343357907787, -81.94992733943924179, -0.7820817253628982169 ) ) ;
#18839=CARTESIAN_POINT ( 'NONE',  ( 1.407891339063999991, -79.05671151888600434, 0.1670362498605000023 ) ) ;
#18849=PLANE ( 'NONE',  #25517 ) ;
#18884=CARTESIAN_POINT ( 'NONE',  ( 1.237149555198000073, -79.60251943783799788, -1.037631781681999987 ) ) ;
#18926=CARTESIAN_POINT ( 'NONE',  ( -1.283123261360999967, -81.17673743600398950, -0.3068555137751999840 ) ) ;
#18958=CARTESIAN_POINT ( 'NONE',  ( -1.428376501803000131, -77.53332085210548996, 0.2580938706625000023 ) ) ;
#18995=CARTESIAN_POINT ( 'NONE',  ( -1.460959015002473382, -79.52083333333332860, -0.3926218265389205819 ) ) ;
#19014=CARTESIAN_POINT ( 'NONE',  ( -1.045973596602999933, -81.61173291773999949, -1.097670891906999957 ) ) ;
#19030=DIRECTION ( 'NONE',  ( 0.000000000000000000, -1.000000000000000000, 0.000000000000000000 ) ) ;
#19042=COLOUR_RGB ( '', 0.09019608, 0.27058824, 0.51372549) ;
#19048=CARTESIAN_POINT ( 'NONE',  ( -0.9420598709024999851, -79.23518609424799308, -0.8215979549846998964 ) ) ;
#19068=CARTESIAN_POINT ( 'NONE',  ( 0.9071727510942999562, -81.67625285498098719, 1.202471848463999793 ) ) ;
#19074=CARTESIAN_POINT ( 'NONE',  ( -0.7554284705563540925, -80.81666666666667709, 1.310679582531384391 ) ) ;
#19075=CARTESIAN_POINT ( 'NONE',  ( -0.1963495408493673433, -81.38541666666669983, 1.499999999999999334 ) ) ;
#19083=DIRECTION ( 'NONE',  ( 1.224058188705999773E-08, -0.9999999999999998890, -4.602708956829999399E-10 ) ) ;
#19094=ORIENTED_EDGE ( 'NONE', *, *, #11923, .T. ) ;
#19115=DIRECTION ( 'NONE',  ( 0.000000000000000000, 0.000000000000000000, -1.000000000000000000 ) ) ;
#19117=CARTESIAN_POINT ( 'NONE',  ( -0.2132868980366808553, -82.13802635239025562, 1.307894579808998703 ) ) ;
#19127=CARTESIAN_POINT ( 'NONE',  ( -1.310679582531386611, -80.04166666666668561, -0.7554284705563495406 ) ) ;
#19134=CARTESIAN_POINT ( 'NONE',  ( -0.1963495408493605987, -81.61458333333334281, -1.500000000000000444 ) ) ;
#19191=ORIENTED_EDGE ( 'NONE', *, *, #42988, .F. ) ;
#19226=AXIS2_PLACEMENT_3D ( 'NONE', #57340, #52916, #26034 ) ;
#19235=CARTESIAN_POINT ( 'NONE',  ( -0.3926218265389256890, -80.29583333333334849, 1.460959015002472050 ) ) ;
#19249=CYLINDRICAL_SURFACE ( 'NONE', #24701, 1.500000000000000000 ) ;
#19288=CARTESIAN_POINT ( 'NONE',  ( 0.7554284705563453217, -80.33333333333332860, 1.310679582531389276 ) ) ;
#19298=EDGE_CURVE ( 'NONE', #42334, #49068, #35316, .T. ) ;
#19299=CARTESIAN_POINT ( 'NONE',  ( -1.500000000000000222, -77.91041666666667709, -0.1963495408493622363 ) ) ;
#19303=B_SPLINE_CURVE_WITH_KNOTS ( 'NONE', 3,
 ( #7080, #2375, #56958, #16519 ),
 .UNSPECIFIED., .F., .F.,
 ( 4, 4 ),
 ( 0.000000000000000000, 1.000000000000000000 ),
 .UNSPECIFIED. ) ;
#19307=EDGE_LOOP ( 'NONE', ( #35887, #37511, #18501, #49076, #12389, #10979, #24083, #12719, #46790, #44856 ) ) ;
#19309=CARTESIAN_POINT ( 'NONE',  ( -1.253545579602000082, -82.06400559251599702, 0.6623148383621999535 ) ) ;
#19312=CARTESIAN_POINT ( 'NONE',  ( -1.310679582531389498, -81.95833333334499571, 0.7554284705563444335 ) ) ;
#19319=VERTEX_POINT ( 'NONE', #28742 ) ;
#19338=CARTESIAN_POINT ( 'NONE',  ( 1.224162466603000210, -77.93941928053710910, -0.5291525010897000225 ) ) ;
#19363=CARTESIAN_POINT ( 'NONE',  ( -1.460959015002474493, -80.87916666666667709, 0.3926218265389144757 ) ) ;
#19364=CARTESIAN_POINT ( 'NONE',  ( -0.5412065714428999641, -79.74942042488599725, -1.203187872875000064 ) ) ;
#19369=ADVANCED_FACE ( 'NONE', ( #14006 ), #32003, .T. ) ;
#19375=ORIENTED_EDGE ( 'NONE', *, *, #34608, .F. ) ;
#19382=ADVANCED_FACE ( 'NONE', ( #54748 ), #45964, .T. ) ;
#19400=CARTESIAN_POINT ( 'NONE',  ( -1.178447680628000205, -80.95308451575900222, -0.9280415206345000723 ) ) ;
#19408=CARTESIAN_POINT ( 'NONE',  ( 1.129337479010032785, -82.04397684591522477, 0.6933189978229028494 ) ) ;
#19442=CARTESIAN_POINT ( 'NONE',  ( 1.315129997485000146, -78.39761010257180374, 0.2213803045116000123 ) ) ;
#19492=DIRECTION ( 'NONE',  ( -1.000000000000000000, 0.000000000000000000, 0.000000000000000000 ) ) ;
#19498=VERTEX_POINT ( 'NONE', #54885 ) ;
#19534=CARTESIAN_POINT ( 'NONE',  ( -0.9898995639662998558, -79.68446749155899056, 0.8721608040441000131 ) ) ;
#19535=CARTESIAN_POINT ( 'NONE',  ( 1.500000000000000000, -77.75000000000000000, 0.000000000000000000 ) ) ;
#19536=CARTESIAN_POINT ( 'NONE',  ( -0.9855275769405000830, -77.61600855774059937, -1.152289182367999931 ) ) ;
#19544=ORIENTED_EDGE ( 'NONE', *, *, #50116, .F. ) ;
#19551=CARTESIAN_POINT ( 'NONE',  ( -1.268945471415019455, -78.24314195652412707, 0.1161799656682465792 ) ) ;
#19560=CARTESIAN_POINT ( 'NONE',  ( -1.208084210770999922, -81.73085454120899840, 0.5648970606752000689 ) ) ;
#19572=CARTESIAN_POINT ( 'NONE',  ( 1.500000000000000000, -80.26041666666668561, 0.1963495408493652339 ) ) ;
#19592=CARTESIAN_POINT ( 'NONE',  ( 0.1717165440430999945, -81.41328242421499795, 1.506471234578999896 ) ) ;
#19595=ORIENTED_EDGE ( 'NONE', *, *, #43314, .T. ) ;
#19603=CONICAL_SURFACE ( 'NONE', #55422, 2.149999999947999729, 0.7853981633972997312 ) ;
#19604=EDGE_LOOP ( 'NONE', ( #11872, #51731, #25383, #24799 ) ) ;
#19608=CARTESIAN_POINT ( 'NONE',  ( 1.199500263597268246, -79.30208333333332860, 0.9218200799623752495 ) ) ;
#19612=( GEOMETRIC_REPRESENTATION_CONTEXT ( 3 ) GLOBAL_UNCERTAINTY_ASSIGNED_CONTEXT ( ( #2411 ) ) GLOBAL_UNIT_ASSIGNED_CONTEXT ( ( #44948, #13341, #31337 ) ) REPRESENTATION_CONTEXT ( 'NONE', 'WORKASPACE' ) );
#19644=CARTESIAN_POINT ( 'NONE',  ( 1.593230767012999927, -81.16732750385499173, 0.1864398872768000259 ) ) ;
#19655=ORIENTED_EDGE ( 'NONE', *, *, #43557, .T. ) ;
#19732=CARTESIAN_POINT ( 'NONE',  ( -1.182296476285000120, -78.63983461367500638, 0.6170503964917000150 ) ) ;
#19793=CYLINDRICAL_SURFACE ( 'NONE', #8169, 1.500000000000000000 ) ;
#19805=CARTESIAN_POINT ( 'NONE',  ( 0.1730703278797017797, -78.28605927411624066, -1.262361427074957687 ) ) ;
#19822=CARTESIAN_POINT ( 'NONE',  ( -0.7554284705563540925, -80.31666666666664867, 1.310679582531384391 ) ) ;
#19833=CARTESIAN_POINT ( 'NONE',  ( 0.2526653223220000632, -78.35443884410990734, 1.594795962155999947 ) ) ;
#19851=CARTESIAN_POINT ( 'NONE',  ( -0.5951243518625245477, -78.16363383461164460, 1.127832697537623829 ) ) ;
#19860=CARTESIAN_POINT ( 'NONE',  ( 1.316231252753000014, -81.98475626391700644, 0.2147359707272000207 ) ) ;
#19869=LINE ( 'NONE', #32250, #21915 ) ;
#19874=CARTESIAN_POINT ( 'NONE',  ( 1.500000000000000888, -79.73958333333334281, -0.1963495408493590444 ) ) ;
#19891=CARTESIAN_POINT ( 'NONE',  ( -1.501972381289000014, -82.05824652816899345, -0.2076389427764999962 ) ) ;
#19899=CARTESIAN_POINT ( 'NONE',  ( 0.9218200799623742503, -78.17708333333332860, -1.199500263597268912 ) ) ;
#19923=CARTESIAN_POINT ( 'NONE',  ( 1.199500263597268246, -78.70208333333333428, 0.9218200799623752495 ) ) ;
#19934=ADVANCED_FACE ( 'NONE', ( #51798 ), #22932, .F. ) ;
#19944=CARTESIAN_POINT ( 'NONE',  ( -1.355217461342999918, -80.94787865541199778, -0.7366976956675999055 ) ) ;
#19951=CARTESIAN_POINT ( 'NONE',  ( -0.9218200799623778030, -80.82708333333336270, 1.199500263597266914 ) ) ;
#19990=CARTESIAN_POINT ( 'NONE',  ( 0.3292142484335000563, -79.32296227407599076, -1.292352404326999826 ) ) ;
#20007=CARTESIAN_POINT ( 'NONE',  ( 0.7554284705563509839, -80.56666666666664867, -1.310679582531386167 ) ) ;
#20024=CARTESIAN_POINT ( 'NONE',  ( -1.356492273396000092, -79.03756650451100541, -0.8757286844311999996 ) ) ;
#20030=CARTESIAN_POINT ( 'NONE',  ( -0.9612450871864000046, -78.69528584285799866, -0.9244371432244999909 ) ) ;
#20052=B_SPLINE_CURVE_WITH_KNOTS ( 'NONE', 3,
 ( #25038, #12046, #39483, #2618, #33884, #30026, #11761, #25610, #38616, #56633, #16191, #43923, #3469, #29738, #21476, #57485, #12613, #31179, #4342, #21757, #49219, #8770, #9363, #14072, #32069, #538, #17929, #36219, #39761, #35918, #44489, #40051, #57775, #36509, #40656, #18516, #50110, #13485, #9654, #27642, #54239, #49520, #12894, #26762, #30895, #31776, #17330, #44790, #3757, #22936, #246, #58069, #53949, #49817, #27055, #35318, #27354, #53348, #48928, #45392, #22343, #40358, #9069, #8470, #4933 ),
 .UNSPECIFIED., .F., .F.,
 ( 4, 2, 2, 2, 2, 2, 2, 2, 2, 2, 2, 2, 2, 2, 2, 2, 1, 2, 2, 2, 2, 2, 2, 2, 2, 2, 2, 2, 2, 2, 2, 2, 4 ),
 ( 0.000000000000000000, 0.03125000000000000000, 0.06249999999999998612, 0.09374999999999998612, 0.1249999999999999861, 0.1562499999999999722, 0.1874999999999999722, 0.2187499999999999722, 0.2499999999999999722, 0.2812500000000000000, 0.3125000000000000000, 0.3437500000000000000, 0.3750000000000000000, 0.4062500000000000000, 0.4375000000000000000, 0.4687500000000000000, 0.5000000000000000000, 0.5312500000000000000, 0.5625000000000000000, 0.5937500000000000000, 0.6250000000000000000, 0.6562500000000000000, 0.6875000000000000000, 0.7187500000000000000, 0.7500000000000000000, 0.7812500000000000000, 0.8125000000000000000, 0.8437500000000000000, 0.8750000000000000000, 0.9062500000000000000, 0.9375000000000000000, 0.9687500000000000000, 1.000000000000000000 ),
 .UNSPECIFIED. ) ;
#20066=DIRECTION ( 'NONE',  ( 0.000000000000000000, 1.000000000000000000, 0.000000000000000000 ) ) ;
#20097=CARTESIAN_POINT ( 'NONE',  ( -0.2293039177969000142, -82.26821515038699317, -1.215124277147999976 ) ) ;
#20120=EDGE_CURVE ( 'NONE', #14133, #27498, #38957, .T. ) ;
#20128=CARTESIAN_POINT ( 'NONE',  ( 1.481171800329999844, -77.81445905126490459, 0.3241480609735999940 ) ) ;
#20145=CARTESIAN_POINT ( 'NONE',  ( -0.6870218104159775407, -77.82969972257922109, -1.073419096667898032 ) ) ;
#20153=CARTESIAN_POINT ( 'NONE',  ( 1.130902752456465654, -80.86209933428780516, -0.5870578767658550801 ) ) ;
#20155=CARTESIAN_POINT ( 'NONE',  ( 1.304222966381000104, -81.53240404768499161, 0.2785293583740000023 ) ) ;
#20177=CARTESIAN_POINT ( 'NONE',  ( -1.199500263597270244, -77.95208333333333428, -0.9218200799623728070 ) ) ;
#20216=CARTESIAN_POINT ( 'NONE',  ( -0.9218200799623778030, -78.82708333333337691, 1.199500263597266914 ) ) ;
#20224=CARTESIAN_POINT ( 'NONE',  ( 0.000000000000000000, -76.00000000000000000, 0.000000000000000000 ) ) ;
#20270=CARTESIAN_POINT ( 'NONE',  ( -1.250000000000000000, -77.64999999999999147, 0.000000000000000000 ) ) ;
#20287=CARTESIAN_POINT ( 'NONE',  ( -1.199500263597270022, -77.55208333333331439, -0.9218200799623730290 ) ) ;
#20306=CARTESIAN_POINT ( 'NONE',  ( 1.161710437675000041, -79.24177606238200156, -0.9743588931339001169 ) ) ;
#20309=CYLINDRICAL_SURFACE ( 'NONE', #40339, 1.500000000000000000 ) ;
#20311=CARTESIAN_POINT ( 'NONE',  ( 1.196963559360000096, -78.39177149676930867, -0.5880938590690999446 ) ) ;
#20332=CARTESIAN_POINT ( 'NONE',  ( -0.3926218265389256890, -78.29583333333334849, 1.460959015002472050 ) ) ;
#20374=ORIENTED_EDGE ( 'NONE', *, *, #36983, .F. ) ;
#20378=CARTESIAN_POINT ( 'NONE',  ( -1.029292737021753279, -81.96672169472573444, -1.136050377789131538 ) ) ;
#20379=CARTESIAN_POINT ( 'NONE',  ( -0.9101267925792999591, -81.72247629319500106, -0.9551098530625999894 ) ) ;
#20383=CARTESIAN_POINT ( 'NONE',  ( 1.249999986291000065, -76.30000000051599329, -0.6999999994844999796 ) ) ;
#20400=LINE ( 'NONE', #52275, #45743 ) ;
#20412=CARTESIAN_POINT ( 'NONE',  ( 1.407891339063999991, -78.86208320661400251, 0.1670362498605000023 ) ) ;
#20430=CARTESIAN_POINT ( 'NONE',  ( -0.8911338523900714792, -77.81379809819678428, -0.9115342124767401577 ) ) ;
#20437=CARTESIAN_POINT ( 'NONE',  ( 1.207550169979716426, -80.92570526169950540, 0.4074191867525038813 ) ) ;
#20473=EDGE_LOOP ( 'NONE', ( #37043, #14930, #2896, #48008, #857, #24604, #11760, #36463, #25754, #53486 ) ) ;
#20477=CARTESIAN_POINT ( 'NONE',  ( -1.310679582531386611, -78.04166666666667140, -0.7554284705563495406 ) ) ;
#20501=CARTESIAN_POINT ( 'NONE',  ( 1.166929042523999982, -78.97544576573699260, -0.6456414311070999279 ) ) ;
#20504=CARTESIAN_POINT ( 'NONE',  ( -0.6878299077642000547, -82.21297074961400142, -1.043738481606000024 ) ) ;
#20540=ORIENTED_EDGE ( 'NONE', *, *, #35582, .F. ) ;
#20562=CARTESIAN_POINT ( 'NONE',  ( 1.313995274498999999, -80.41443998845899443, -0.2280190045613000038 ) ) ;
#20569=DIRECTION ( 'NONE',  ( -1.000000000000000000, 0.000000000000000000, 0.000000000000000000 ) ) ;
#20576=CARTESIAN_POINT ( 'NONE',  ( 0.7341740840635999632, -80.80573051437600895, -1.113348630318000021 ) ) ;
#20578=CARTESIAN_POINT ( 'NONE',  ( -1.500000000000000222, -80.41041666666666288, -0.1963495408493622363 ) ) ;
#20611=ORIENTED_EDGE ( 'NONE', *, *, #76, .F. ) ;
#20645=CARTESIAN_POINT ( 'NONE',  ( -0.5931688960305999681, -78.65405146749098719, 1.178438064142999897 ) ) ;
#20664=CARTESIAN_POINT ( 'NONE',  ( 0.8866125316423000280, -81.47441317628999968, 0.9769768825355000796 ) ) ;
#20667=CARTESIAN_POINT ( 'NONE',  ( -0.7109705001964822246, -78.57228594746854355, 1.058387015174929280 ) ) ;
#20682=CIRCLE ( 'NONE', #39508, 2.299999999999999822 ) ;
#20695=CARTESIAN_POINT ( 'NONE',  ( 0.6128924939060999000, -80.13674016633599706, 1.278445216313999877 ) ) ;
#20698=CARTESIAN_POINT ( 'NONE',  ( -1.376714249866999973, -78.01290954478920980, 0.6352952275891999845 ) ) ;
#20723=CARTESIAN_POINT ( 'NONE',  ( 0.1243515176670834943, -80.78259192502341079, -1.268026773355690473 ) ) ;
#20739=CARTESIAN_POINT ( 'NONE',  ( -1.250000000000000000, -77.71666666666666856, 0.000000000000000000 ) ) ;
#20768=CARTESIAN_POINT ( 'NONE',  ( -1.471932811527529195, -79.01769483858601006, -0.3335056313496183034 ) ) ;
#20796=CARTESIAN_POINT ( 'NONE',  ( -0.9218200799623716968, -80.07291666666667140, -1.199500263597270910 ) ) ;
#20842=CARTESIAN_POINT ( 'NONE',  ( 0.000000000000000000, -77.40000000000736691, 0.000000000000000000 ) ) ;
#20859=CARTESIAN_POINT ( 'NONE',  ( -0.09713983013762964025, -79.11964965042942310, -1.537455523586755080 ) ) ;
#20868=CARTESIAN_POINT ( 'NONE',  ( 0.000000000000000000, -76.00000000000000000, 0.000000000000000000 ) ) ;
#20869=CARTESIAN_POINT ( 'NONE',  ( -1.137100204128000058, -81.28336096009799405, -0.6517852884778999600 ) ) ;
#20876=ORIENTED_EDGE ( 'NONE', *, *, #50835, .F. ) ;
#20902=CARTESIAN_POINT ( 'NONE',  ( 1.199500263597268246, -78.20208333333333428, 0.9218200799623752495 ) ) ;
#20928=CARTESIAN_POINT ( 'NONE',  ( -0.9052918118899000444, -78.30676310382339977, -0.9596938812619000281 ) ) ;
#20943=CARTESIAN_POINT ( 'NONE',  ( -1.499934128473817241, -81.90004407876089942, 2.109063419893342596E-06 ) ) ;
#20973=ADVANCED_FACE ( 'NONE', ( #27846 ), #41733, .T. ) ;
#20976=EDGE_LOOP ( 'NONE', ( #42411, #50167, #3741, #41092 ) ) ;
#20979=CARTESIAN_POINT ( 'NONE',  ( 0.9925657212695000453, -80.48402853000399659, -1.012359935335999994 ) ) ;
#20983=CARTESIAN_POINT ( 'NONE',  ( -1.232249204661999942, -77.57215499870638098, 0.4974159524616000305 ) ) ;
#21000=CARTESIAN_POINT ( 'NONE',  ( -1.140431633367790853, -79.21314104385653820, 0.5695704127092841018 ) ) ;
#21006=CARTESIAN_POINT ( 'NONE',  ( -0.4619891075108225054, -82.05471047325586653, 1.187616552076537602 ) ) ;
#21035=AXIS2_PLACEMENT_3D ( 'NONE', #2892, #2613, #3752 ) ;
#21079=CARTESIAN_POINT ( 'NONE',  ( -1.500000000000000000, -77.50000000000000000, 0.000000000000000000 ) ) ;
#21084=CARTESIAN_POINT ( 'NONE',  ( -0.7554284705563480973, -80.08333333333332860, -1.310679582531387277 ) ) ;
#21144=CARTESIAN_POINT ( 'NONE',  ( -0.5935892672256000147, -82.08982011648200228, 1.194249225580000129 ) ) ;
#21161=CARTESIAN_POINT ( 'NONE',  ( 0.3985939703966000502, -79.13679175127299459, -1.564707112294000169 ) ) ;
#21187=DIRECTION ( 'NONE',  ( 0.000000000000000000, 1.000000000000000000, 0.000000000000000000 ) ) ;
#21188=CARTESIAN_POINT ( 'NONE',  ( 1.460959015002472494, -78.17083333333334849, 0.3926218265389232465 ) ) ;
#21204=CARTESIAN_POINT ( 'NONE',  ( 1.603441158369999897, -79.16745489434200067, 0.1902368389766999901 ) ) ;
#21208=CARTESIAN_POINT ( 'NONE',  ( 1.500000000000000000, -80.75000000000000000, 0.000000000000000000 ) ) ;
#21251=CARTESIAN_POINT ( 'NONE',  ( 0.000000000000000000, -75.67500000000001137, 0.000000000000000000 ) ) ;
#21261=CARTESIAN_POINT ( 'NONE',  ( -1.196791375131569746, -82.25000000000000000, -0.4167097060225089522 ) ) ;
#21262=ORIENTED_EDGE ( 'NONE', *, *, #2042, .T. ) ;
#21265=CARTESIAN_POINT ( 'NONE',  ( -0.8374915928969000056, -80.80902028819700433, -0.9453856285906999668 ) ) ;
#21268=CARTESIAN_POINT ( 'NONE',  ( -1.391953914337000109, -78.11789385589818835, -0.2693022098514999962 ) ) ;
#21285=CARTESIAN_POINT ( 'NONE',  ( -1.271334513670838939, -79.24494429262146866, 0.08715925150112330266 ) ) ;
#21292=CARTESIAN_POINT ( 'NONE',  ( -1.273526288746646973, -81.14832600764039228, 0.03013355673499748880 ) ) ;
#21324=FACE_OUTER_BOUND ( 'NONE', #58208, .T. ) ;
#21363=DIRECTION ( 'NONE',  ( 0.000000000000000000, 0.7071067811866525998, -0.7071067811864425456 ) ) ;
#21389=DIRECTION ( 'NONE',  ( 0.000000000000000000, 0.000000000000000000, -1.000000000000000000 ) ) ;
#21394=ORIENTED_EDGE ( 'NONE', *, *, #26460, .T. ) ;
#21407=AXIS2_PLACEMENT_3D ( 'NONE', #14293, #34532, #49003 ) ;
#21433=CARTESIAN_POINT ( 'NONE',  ( -1.260553452884753955, -79.73788096563870909, 0.1933511446621866969 ) ) ;
#21436=CARTESIAN_POINT ( 'NONE',  ( -0.7068627984950999199, -81.09756764886000724, 1.130893941374999878 ) ) ;
#21446=ADVANCED_FACE ( 'NONE', ( #23360 ), #19603, .F. ) ;
#21454=CARTESIAN_POINT ( 'NONE',  ( -1.034826241750000264, -80.48209164690899797, 1.108174957742000144 ) ) ;
#21457=CARTESIAN_POINT ( 'NONE',  ( 1.097898070916953239, -82.12630208333071380, 0.8448041534256599538 ) ) ;
#21476=CARTESIAN_POINT ( 'NONE',  ( 0.4727252345235593567, -79.49457189493710985, 1.183769161397306258 ) ) ;
#21497=CARTESIAN_POINT ( 'NONE',  ( -0.7259747304966001069, -78.82016653067499590, 1.442281046339000117 ) ) ;
#21501=CARTESIAN_POINT ( 'NONE',  ( 0.3926218265389159190, -80.85416666666667140, 1.460959015002474715 ) ) ;
#21503=CARTESIAN_POINT ( 'NONE',  ( -0.9509180703096998810, -78.80288933763399939, -0.9145055679095001056 ) ) ;
#21532=( LENGTH_UNIT ( ) NAMED_UNIT ( * ) SI_UNIT ( .MILLI., .METRE. ) );
#21541=DIRECTION ( 'NONE',  ( -1.000000000000000000, 0.000000000000000000, 0.000000000000000000 ) ) ;
#21551=CARTESIAN_POINT ( 'NONE',  ( -0.8502109015516584600, -82.25000000000000000, -0.9397329394915318046 ) ) ;
#21557=CARTESIAN_POINT ( 'NONE',  ( -1.100846539600000007, -79.19859309350199794, -0.6190985795237999856 ) ) ;
#21568=EDGE_CURVE ( 'NONE', #54597, #33739, #31841, .T. ) ;
#21612=ORIENTED_EDGE ( 'NONE', *, *, #40072, .T. ) ;
#21627=CARTESIAN_POINT ( 'NONE',  ( -1.199500263597274685, -77.94791666666668561, 0.9218200799623673669 ) ) ;
#21698=CARTESIAN_POINT ( 'NONE',  ( -1.319155384867000125, -80.21015088913199520, 0.1959724986398999891 ) ) ;
#21721=CARTESIAN_POINT ( 'NONE',  ( -1.234140985588999984, -81.19095428981999873, 0.5054425604136000283 ) ) ;
#21735=CARTESIAN_POINT ( 'NONE',  ( -1.499766830043999910, -80.03557803647899505, 0.2228039671692000068 ) ) ;
#21744=ORIENTED_EDGE ( 'NONE', *, *, #50835, .T. ) ;
#21754=CARTESIAN_POINT ( 'NONE',  ( -8.022734517049746273E-06, -82.01564364893640402, -1.484164386985079798 ) ) ;
#21756=EDGE_CURVE ( 'NONE', #42409, #27527, #44484, .T. ) ;
#21757=CARTESIAN_POINT ( 'NONE',  ( -1.193476013507506650, -79.62178374976105033, 0.4454124431937202533 ) ) ;
#21780=CARTESIAN_POINT ( 'NONE',  ( -1.308462286196999891, -79.31053370013900405, 0.7661340681064999769 ) ) ;
#21815=ORIENTED_EDGE ( 'NONE', *, *, #29875, .F. ) ;
#21834=( GEOMETRIC_REPRESENTATION_CONTEXT ( 3 ) GLOBAL_UNCERTAINTY_ASSIGNED_CONTEXT ( ( #33682 ) ) GLOBAL_UNIT_ASSIGNED_CONTEXT ( ( #11401, #38245, #47428 ) ) REPRESENTATION_CONTEXT ( 'NONE', 'WORKASPACE' ) );
#21838=CARTESIAN_POINT ( 'NONE',  ( -0.2315393795184000070, -80.13098110198900770, 1.298828366650000010 ) ) ;
#21841=CARTESIAN_POINT ( 'NONE',  ( -1.112867702664867675, -80.60286633726140337, -0.8764124957829881879 ) ) ;
#21867=CARTESIAN_POINT ( 'NONE',  ( -1.310679582531389276, -79.35833333333332007, 0.7554284705563443225 ) ) ;
#21915=VECTOR ( 'NONE', #42008, 1000.000000000000000 ) ;
#21928=CARTESIAN_POINT ( 'NONE',  ( -0.6878299077642000547, -82.24743426901200394, -1.043738481606000024 ) ) ;
#21953=CARTESIAN_POINT ( 'NONE',  ( 2.799999999999999822, -76.00000000000000000, 0.000000000000000000 ) ) ;
#21957=CIRCLE ( 'NONE', #15365, 1.500000000000000000 ) ;
#21959=CARTESIAN_POINT ( 'NONE',  ( -1.047413957980333654, -80.85330312658089724, -0.8248344856773377476 ) ) ;
#21966=CARTESIAN_POINT ( 'NONE',  ( -1.364447001127000014, -80.56986782673699565, -0.3974066121187999623 ) ) ;
#21984=EDGE_CURVE ( 'NONE', #5753, #34724, #33626, .T. ) ;
#21985=CARTESIAN_POINT ( 'NONE',  ( 0.9788970803261000109, -79.95624916642501034, -0.9057243817226000582 ) ) ;
#22003=CARTESIAN_POINT ( 'NONE',  ( 1.274727678800788633, -79.49935659990086378, -0.01038921198208550382 ) ) ;
#22008=CARTESIAN_POINT ( 'NONE',  ( -0.7068627984950999199, -81.14134166643898993, 1.130893941374999878 ) ) ;
#22018=CARTESIAN_POINT ( 'NONE',  ( -0.2109498265882999990, -82.12980651837901291, 1.293563445978999971 ) ) ;
#22023=CARTESIAN_POINT ( 'NONE',  ( -0.6219878248318000402, -79.63867704943100989, -1.382777385570999940 ) ) ;
#22024=ORIENTED_EDGE ( 'NONE', *, *, #31524, .T. ) ;
#22043=CARTESIAN_POINT ( 'NONE',  ( 1.461448385607039491, -81.67104446236695026, 0.3928510776231207702 ) ) ;
#22050=CIRCLE ( 'NONE', #16437, 0.6999999999999999556 ) ;
#22054=CARTESIAN_POINT ( 'NONE',  ( -1.500000000000000000, -79.90000000000000568, 0.000000000000000000 ) ) ;
#22062=CARTESIAN_POINT ( 'NONE',  ( 1.281522546595510681, -81.47967980706110325, -0.3373344656957449339 ) ) ;
#22074=CARTESIAN_POINT ( 'NONE',  ( -0.1190996060027000036, -77.91562118112170765, -1.412746526842000083 ) ) ;
#22079=EDGE_CURVE ( 'NONE', #17474, #41507, #31693, .T. ) ;
#22098=EDGE_LOOP ( 'NONE', ( #33962, #20611, #42835, #20876, #16759, #41356, #9637, #50462, #31883, #455 ) ) ;
#22104=VERTEX_POINT ( 'NONE', #57553 ) ;
#22129=CARTESIAN_POINT ( 'NONE',  ( -1.606812318740999945, -79.90019517812399386, 0.1592736582230999953 ) ) ;
#22131=CARTESIAN_POINT ( 'NONE',  ( 0.8816674349947000167, -77.97481505010179603, 0.9814419191067000892 ) ) ;
#22132=EDGE_CURVE ( 'NONE', #16033, #18435, #42286, .T. ) ;
#22141=FACE_OUTER_BOUND ( 'NONE', #54725, .T. ) ;
#22181=DIRECTION ( 'NONE',  ( 0.000000000000000000, -1.000000000000000000, 0.000000000000000000 ) ) ;
#22185=EDGE_LOOP ( 'NONE', ( #22776, #32556, #32355, #47660, #54660 ) ) ;
#22204=CARTESIAN_POINT ( 'NONE',  ( -1.460959015002474937, -77.97916666666665719, 0.3926218265389144757 ) ) ;
#22227=CARTESIAN_POINT ( 'NONE',  ( 0.000000000000000000, -77.40000000000736691, 0.000000000000000000 ) ) ;
#22233=DIRECTION ( 'NONE',  ( 1.000000000000000000, 0.000000000000000000, 0.000000000000000000 ) ) ;
#22260=ORIENTED_EDGE ( 'NONE', *, *, #15752, .T. ) ;
#22261=CARTESIAN_POINT ( 'NONE',  ( 0.1045857360044000067, -80.86178450267699702, 1.611296339591000049 ) ) ;
#22277=CARTESIAN_POINT ( 'NONE',  ( -0.9820397338569999413, -80.70308451575900222, -0.7733679338621000099 ) ) ;
#22279=CARTESIAN_POINT ( 'NONE',  ( 0.9336649615752000697, -80.45237540023499889, -0.9522845488933000535 ) ) ;
#22299=CARTESIAN_POINT ( 'NONE',  ( -1.258250795308458070, -80.26263457026050219, -0.2016572651531162164 ) ) ;
#22304=CARTESIAN_POINT ( 'NONE',  ( -1.127489577578000057, -80.71720420293900133, -0.5989559841152000130 ) ) ;
#22312=CARTESIAN_POINT ( 'NONE',  ( 0.8666632585819999957, -81.42443521981201116, -0.9832170324100000247 ) ) ;
#22318=CARTESIAN_POINT ( 'NONE',  ( 0.2296925013217000211, -80.18441590662199303, -1.498727297740999775 ) ) ;
#22323=CARTESIAN_POINT ( 'NONE',  ( 1.460959015002474493, -79.12916666666669130, -0.3926218265389176953 ) ) ;
#22329=DIRECTION ( 'NONE',  ( -1.000000000000000000, 7.077902766859999560E-11, 7.077871680614999346E-11 ) ) ;
#22343=CARTESIAN_POINT ( 'NONE',  ( -1.203536965665374270, -80.62357710649452258, 0.4181554378093583768 ) ) ;
#22352=EDGE_CURVE ( 'NONE', #39723, #17474, #15900, .T. ) ;
#22354=CARTESIAN_POINT ( 'NONE',  ( -1.178447680628000205, -80.55308451575899653, -0.9280415206345000723 ) ) ;
#22370=CARTESIAN_POINT ( 'NONE',  ( -1.431457626485999945, -78.86977915405600470, 0.7470896798747000966 ) ) ;
#22379=CARTESIAN_POINT ( 'NONE',  ( -0.2558648464975999959, -78.90787364874299215, -1.394486488214999875 ) ) ;
#22393=VERTEX_POINT ( 'NONE', #38041 ) ;
#22394=CARTESIAN_POINT ( 'NONE',  ( 0.7833523767573993268, -80.66795188156623908, -1.316067733153899688 ) ) ;
#22405=ORIENTED_EDGE ( 'NONE', *, *, #48848, .F. ) ;
#22427=EDGE_CURVE ( 'NONE', #38110, #5279, #44352, .T. ) ;
#22429=CARTESIAN_POINT ( 'NONE',  ( 0.6980205241115000625, -80.24748354179199339, 1.456015547280999911 ) ) ;
#22430=CARTESIAN_POINT ( 'NONE',  ( 0.6216730717741000278, -78.32210341376939766, -1.163652956044999964 ) ) ;
#22468=VECTOR ( 'NONE', #31570, 1000.000000000000000 ) ;
#22470=CARTESIAN_POINT ( 'NONE',  ( -1.115376533724000030, -80.69714874331999965, -0.5925211750962999790 ) ) ;
#22519=EDGE_CURVE ( 'NONE', #24789, #12731, #56280, .T. ) ;
#22564=CARTESIAN_POINT ( 'NONE',  ( -0.9343553003753000130, -80.61948045011800446, -1.194030576736000215 ) ) ;
#22565=ORIENTED_EDGE ( 'NONE', *, *, #9953, .T. ) ;
#22580=CARTESIAN_POINT ( 'NONE',  ( -0.6211595220380999871, -80.84927638728399302, -1.084739991049000096 ) ) ;
#22597=CARTESIAN_POINT ( 'NONE',  ( -1.256362333281000110, -77.75166772233730228, 0.2270125678640999844 ) ) ;
#22601=CARTESIAN_POINT ( 'NONE',  ( 1.041570653413430803, -80.54886380914602739, 0.7342313532027737732 ) ) ;
#22615=CARTESIAN_POINT ( 'NONE',  ( -0.5811420367779999152, -81.33038571333599975, -1.174774391002999963 ) ) ;
#22622=CARTESIAN_POINT ( 'NONE',  ( -1.137653363949000074, -79.48983917928698872, 1.002340751266999952 ) ) ;
#22678=CARTESIAN_POINT ( 'NONE',  ( -0.1877060973040000080, -78.41174741493239253, -1.405284953735000064 ) ) ;
#22684=CARTESIAN_POINT ( 'NONE',  ( 1.199500263597271799, -81.69791666666667140, -0.9218200799623701425 ) ) ;
#22692=CARTESIAN_POINT ( 'NONE',  ( 1.500000000000000222, -80.73359037631325918, -0.3093141193355201102 ) ) ;
#22705=PRESENTATION_STYLE_ASSIGNMENT (( #8834 ) ) ;
#22725=CARTESIAN_POINT ( 'NONE',  ( 1.602460118848999970, -80.14825829503000421, -0.1983317763271000012 ) ) ;
#22736=VERTEX_POINT ( 'NONE', #21953 ) ;
#22758=CARTESIAN_POINT ( 'NONE',  ( 0.000000000000000000, -76.79999999999999716, -3.999999999999249045 ) ) ;
#22776=ORIENTED_EDGE ( 'NONE', *, *, #36838, .T. ) ;
#22795=CARTESIAN_POINT ( 'NONE',  ( 1.460959015002472494, -77.77083333333335702, 0.3926218265389233020 ) ) ;
#22796=DIRECTION ( 'NONE',  ( 0.000000000000000000, 0.7071067811866525998, -0.7071067811864425456 ) ) ;
#22822=ORIENTED_EDGE ( 'NONE', *, *, #22132, .F. ) ;
#22845=CARTESIAN_POINT ( 'NONE',  ( 0.3993207018968132904, -77.99983260076393776, 1.209697183087648620 ) ) ;
#22847=B_SPLINE_CURVE_WITH_KNOTS ( 'NONE', 3,
 ( #16596, #26013, #56464, #7732 ),
 .UNSPECIFIED., .F., .F.,
 ( 4, 4 ),
 ( 0.000000000000000000, 1.000000000000000000 ),
 .UNSPECIFIED. ) ;
#22855=CARTESIAN_POINT ( 'NONE',  ( 1.593618269839000012, -81.75481172353600812, 0.2599901540301000069 ) ) ;
#22868=VERTEX_POINT ( 'NONE', #1022 ) ;
#22871=CARTESIAN_POINT ( 'NONE',  ( -0.9565643533716999825, -80.16053826575100061, 0.9292797142584000580 ) ) ;
#22882=AXIS2_PLACEMENT_3D ( 'NONE', #51003, #37395, #15847 ) ;
#22886=CARTESIAN_POINT ( 'NONE',  ( 0.6284244718204999858, -78.38593289096679939, -1.176290284212999859 ) ) ;
#22903=ORIENTED_EDGE ( 'NONE', *, *, #35705, .F. ) ;
#22907=CARTESIAN_POINT ( 'NONE',  ( 0.4476906417931999504, -81.89468275219000759, -1.231825476718000134 ) ) ;
#22914=ORIENTED_EDGE ( 'NONE', *, *, #49486, .F. ) ;
#22932=B_SPLINE_SURFACE_WITH_KNOTS ( 'NONE', 3, 3, ( 
 ( #39359, #11642, #24917, #12206 ),
 ( #16061, #57366, #6909, #29900 ),
 ( #24629, #3066, #7489, #38198 ),
 ( #12489, #11922, #15767, #29619 ) ),
 .UNSPECIFIED., .F., .F., .F.,
 ( 4, 4 ),
 ( 4, 4 ),
 ( 0.7425508590987000002, 1.053716877278999986 ),
 ( -0.0006517983049530999724, 0.01399779397395000020 ),
 .UNSPECIFIED. ) ;
#22936=CARTESIAN_POINT ( 'NONE',  ( 1.062151845517925741, -80.35325191499507014, -0.7033190988423592138 ) ) ;
#22949=CARTESIAN_POINT ( 'NONE',  ( -0.1963495408493606265, -80.01458333333334849, -1.500000000000000222 ) ) ;
#22955=DIRECTION ( 'NONE',  ( 0.000000000000000000, -1.000000000000000000, 0.000000000000000000 ) ) ;
#22957=CARTESIAN_POINT ( 'NONE',  ( 0.7980979214679511102, -81.57372931353624779, 1.057891434376452500 ) ) ;
#22971=CARTESIAN_POINT ( 'NONE',  ( -1.411465571349000081, -79.30477463579200048, -0.1328074485833999896 ) ) ;
#22990=CARTESIAN_POINT ( 'NONE',  ( -0.1120320062231000002, -77.75264599861779402, -1.328911429676000067 ) ) ;
#22992=DIRECTION ( 'NONE',  ( 0.000000000000000000, 0.000000000000000000, -1.000000000000000000 ) ) ;
#23003=CARTESIAN_POINT ( 'NONE',  ( 0.000000000000000000, -77.50000000000000000, 0.000000000000000000 ) ) ;
#23017=CARTESIAN_POINT ( 'NONE',  ( -0.9624967649451999785, -80.91976366365300066, -1.086495216026000188 ) ) ;
#23125=CARTESIAN_POINT ( 'NONE',  ( -0.9218200799623775810, -80.42708333333334281, 1.199500263597266247 ) ) ;
#23145=CARTESIAN_POINT ( 'NONE',  ( -1.427657462233000052, -81.95326221706000069, 0.7543074114907001304 ) ) ;
#23160=DIRECTION ( 'NONE',  ( -1.000000000000000000, 0.000000000000000000, 0.000000000000000000 ) ) ;
#23180=CARTESIAN_POINT ( 'NONE',  ( -0.9151233253627000241, -78.33048166178321026, -0.9701162038759999495 ) ) ;
#23198=CARTESIAN_POINT ( 'NONE',  ( 1.137028337533999789, -81.99707919315601146, -0.8312398915222000140 ) ) ;
#23204=CARTESIAN_POINT ( 'NONE',  ( 1.157603047269999852, -79.94787091841099880, 0.6328671228825999417 ) ) ;
#23240=CARTESIAN_POINT ( 'NONE',  ( -1.327128730425999992, -79.62647662016500760, 0.1315503032697999675 ) ) ;
#23252=EDGE_CURVE ( 'NONE', #52412, #33741, #45516, .T. ) ;
#23261=CARTESIAN_POINT ( 'NONE',  ( -1.310679582531389276, -79.85833333333332007, 0.7554284705563443225 ) ) ;
#23262=CARTESIAN_POINT ( 'NONE',  ( -0.2007418666109000160, -78.46711910266039069, -1.502878855747000086 ) ) ;
#23284=ORIENTED_EDGE ( 'NONE', *, *, #38556, .T. ) ;
#23311=CARTESIAN_POINT ( 'NONE',  ( 1.112922243992000126, -80.04327398392099724, -1.029731144982999780 ) ) ;
#23356=CARTESIAN_POINT ( 'NONE',  ( 0.3926218265389220807, -81.14583333333335702, -1.460959015002473382 ) ) ;
#23360=FACE_OUTER_BOUND ( 'NONE', #9577, .T. ) ;
#23381=CARTESIAN_POINT ( 'NONE',  ( -1.598336519864000049, -78.50327671425300480, -0.2292036100155999956 ) ) ;
#23436=CARTESIAN_POINT ( 'NONE',  ( 0.2448185669109000095, -81.90940865802599546, 1.496330837606000053 ) ) ;
#23465=CARTESIAN_POINT ( 'NONE',  ( 0.9834589317531000630, -78.98712297734201115, 0.9007689179829999615 ) ) ;
#23483=CARTESIAN_POINT ( 'NONE',  ( -1.444291512224999963, -80.93220373766600062, -0.4522057381387999953 ) ) ;
#23490=CARTESIAN_POINT ( 'NONE',  ( -1.312870888196999930, -79.65019517812399386, 0.1301370089704000088 ) ) ;
#23498=B_SPLINE_CURVE_WITH_KNOTS ( 'NONE', 3,
 ( #49544, #8791, #54555, #40379, #9090, #45116 ),
 .UNSPECIFIED., .F., .F.,
 ( 4, 2, 4 ),
 ( 0.000000000000000000, 0.5000000000000000000, 1.000000000000000000 ),
 .UNSPECIFIED. ) ;
#23510=VERTEX_POINT ( 'NONE', #29060 ) ;
#23526=CARTESIAN_POINT ( 'NONE',  ( 1.199918086393000127, -80.42027859426200109, 0.5820416783086000967 ) ) ;
#23533=CARTESIAN_POINT ( 'NONE',  ( -0.3180038526339120097, -81.85587783296324460, -1.286455647724569884 ) ) ;
#23534=CARTESIAN_POINT ( 'NONE',  ( -0.1554435011324208915, -82.01041666286585041, -1.489583319316136745 ) ) ;
#23539=FACE_OUTER_BOUND ( 'NONE', #19604, .T. ) ;
#23544=CARTESIAN_POINT ( 'NONE',  ( -1.500000000000000000, -80.00000000000000000, 0.000000000000000000 ) ) ;
#23560=ORIENTED_EDGE ( 'NONE', *, *, #22079, .F. ) ;
#23601=LINE ( 'NONE', #27440, #8173 ) ;
#23645=DIRECTION ( 'NONE',  ( -1.000000000000000000, 0.000000000000000000, 0.000000000000000000 ) ) ;
#23666=CARTESIAN_POINT ( 'NONE',  ( -1.466115278491000096, -77.95753785706131112, 0.6765500100044000709 ) ) ;
#23673=EDGE_CURVE ( 'NONE', #47577, #43330, #26083, .T. ) ;
#23701=DIRECTION ( 'NONE',  ( 0.000000000000000000, 0.7071067811865475727, 0.7071067811865475727 ) ) ;
#23721=DIRECTION ( 'NONE',  ( -1.000000000000000000, 0.000000000000000000, 0.000000000000000000 ) ) ;
#23724=CARTESIAN_POINT ( 'NONE',  ( 0.7804898537227999977, -80.77407738460799180, -1.183584831557000117 ) ) ;
#23756=CARTESIAN_POINT ( 'NONE',  ( 0.2725326480772000126, -79.03673560072299153, 1.305490477442999842 ) ) ;
#23774=CARTESIAN_POINT ( 'NONE',  ( 0.9660827079681000296, -81.73162454270899957, 1.280557929256000094 ) ) ;
#23781=CARTESIAN_POINT ( 'NONE',  ( 0.5703284788033999853, -79.99748354179199339, 1.189660050829999927 ) ) ;
#23832=CARTESIAN_POINT ( 'NONE',  ( 0.000000000000000000, -77.50000000000000000, 0.000000000000000000 ) ) ;
#23841=ADVANCED_FACE ( 'NONE', ( #41127 ), #722, .T. ) ;
#23843=CARTESIAN_POINT ( 'NONE',  ( -1.500000000000000222, -81.51041666666667140, -0.1963495408493622085 ) ) ;
#23850=ORIENTED_EDGE ( 'NONE', *, *, #22132, .T. ) ;
#23855=CARTESIAN_POINT ( 'NONE',  ( 0.6284244718204999858, -78.29838485580960139, -1.176290284212999859 ) ) ;
#23911=CARTESIAN_POINT ( 'NONE',  ( 3.999999999993000266, -77.30000000000720206, -8.632702228606999814E-11 ) ) ;
#23942=CARTESIAN_POINT ( 'NONE',  ( -1.500000000000000444, -80.38958333333332007, 0.1963495408493560745 ) ) ;
#23953=CARTESIAN_POINT ( 'NONE',  ( -1.317826160292999926, -77.51678331097843966, 0.5319603796220000458 ) ) ;
#23981=CARTESIAN_POINT ( 'NONE',  ( -0.05395919428434999693, -80.88743994373099611, -1.332567581519000122 ) ) ;
#23995=CARTESIAN_POINT ( 'NONE',  ( 1.500000000000000000, -79.75000000000000000, 0.000000000000000000 ) ) ;
#24015=CARTESIAN_POINT ( 'NONE',  ( 1.269301140243999759, -81.81594247561099564, -0.6316121951705000459 ) ) ;
#24029=EDGE_LOOP ( 'NONE', ( #27918, #5501, #9048, #30810 ) ) ;
#24033=CARTESIAN_POINT ( 'NONE',  ( 0.1963495408493571015, -79.36458333333330017, 1.500000000000000444 ) ) ;
#24036=CARTESIAN_POINT ( 'NONE',  ( -1.500000000000000000, -79.50000000000000000, 0.000000000000000000 ) ) ;
#24048=CARTESIAN_POINT ( 'NONE',  ( -1.150888948972000003, -79.22350888264300295, 0.6738713386821000295 ) ) ;
#24068=CARTESIAN_POINT ( 'NONE',  ( 0.4053230381024000017, -81.20600532260299076, 1.450728874481000075 ) ) ;
#24083=ORIENTED_EDGE ( 'NONE', *, *, #15421, .F. ) ;
#24101=CARTESIAN_POINT ( 'NONE',  ( -1.500000000000000000, -81.00000000000000000, 0.000000000000000000 ) ) ;
#24124=CARTESIAN_POINT ( 'NONE',  ( 0.08638142328466999476, -81.00418100790099629, 1.330832257483999914 ) ) ;
#24153=CARTESIAN_POINT ( 'NONE',  ( 0.9834589317531000630, -78.94334895976399480, 0.9007689179829999615 ) ) ;
#24222=CARTESIAN_POINT ( 'NONE',  ( -1.500410155940665735, -81.91674653272079354, -0.3141412879893631382 ) ) ;
#24224=CARTESIAN_POINT ( 'NONE',  ( 0.1494146964801000010, -81.52402579967099427, 1.310816866976999950 ) ) ;
#24226=CARTESIAN_POINT ( 'NONE',  ( 1.270896956543958733, -78.90621706637968202, 0.09642097433307661447 ) ) ;
#24253=ORIENTED_EDGE ( 'NONE', *, *, #24776, .T. ) ;
#24282=CARTESIAN_POINT ( 'NONE',  ( -0.7068627984950999199, -81.18511568401699208, 1.130893941374999878 ) ) ;
#24297=CARTESIAN_POINT ( 'NONE',  ( 0.1963495408493638184, -79.63541666666667140, -1.499999999999999778 ) ) ;
#24316=CARTESIAN_POINT ( 'NONE',  ( -0.1350024095750999853, -81.16521930730999657, -1.510204125836999811 ) ) ;
#24350=CARTESIAN_POINT ( 'NONE',  ( -0.7022187824378000043, -82.19906693409399168, -1.095132696781000003 ) ) ;
#24369=CARTESIAN_POINT ( 'NONE',  ( 0.08881464945738999639, -81.77864929594699106, 1.601641772328999958 ) ) ;
#24376=CARTESIAN_POINT ( 'NONE',  ( 0.1963495408493571015, -81.36458333333332860, 1.500000000000000444 ) ) ;
#24411=CARTESIAN_POINT ( 'NONE',  ( 0.6343572851480000496, -80.51366523522099783, 1.173101423079000005 ) ) ;
#24444=DIRECTION ( 'NONE',  ( 0.000000000000000000, -1.000000000000000000, 0.000000000000000000 ) ) ;
#24450=CARTESIAN_POINT ( 'NONE',  ( -1.309352690804000074, -78.14954698566639024, -0.2533212985548999874 ) ) ;
#24453=EDGE_LOOP ( 'NONE', ( #30349, #34743, #651 ) ) ;
#24485=ORIENTED_EDGE ( 'NONE', *, *, #29875, .T. ) ;
#24514=CARTESIAN_POINT ( 'NONE',  ( -0.9554212428760000542, -82.21860252700599858, -0.9097111415877999763 ) ) ;
#24518=CARTESIAN_POINT ( 'NONE',  ( 0.7733564461248794153, -78.82670965711476185, -1.012296451130571873 ) ) ;
#24563=CARTESIAN_POINT ( 'NONE',  ( 0.1450192808573305958, -78.11592896146416365, 1.266846556839069216 ) ) ;
#24571=CARTESIAN_POINT ( 'NONE',  ( -1.034480412912579972, -81.10062156208175566, 0.7433832837861729104 ) ) ;
#24573=CARTESIAN_POINT ( 'NONE',  ( -0.1187445621502999926, -81.38356617754199362, -1.328335755224000048 ) ) ;
#24602=DIRECTION ( 'NONE',  ( 0.000000000000000000, -1.000000000000000000, 0.000000000000000000 ) ) ;
#24604=ORIENTED_EDGE ( 'NONE', *, *, #40012, .F. ) ;
#24606=CARTESIAN_POINT ( 'NONE',  ( 0.09820828907688000653, -80.91715619040499519, 1.513042435352000004 ) ) ;
#24613=B_SPLINE_CURVE_WITH_KNOTS ( 'NONE', 3,
 ( #11786, #47241, #39504, #52513, #29759, #33908, #52797, #25921, #33627, #47538, #43944, #56371, #6772, #51949, #7063, #38641, #7347, #25347 ),
 .UNSPECIFIED., .F., .F.,
 ( 4, 2, 2, 2, 2, 2, 2, 2, 4 ),
 ( 0.000000000000000000, 0.1250000000000000000, 0.2500000000000000000, 0.3750000000000000000, 0.5000000000000000000, 0.6250000000000000000, 0.7500000000000000000, 0.8750000000000000000, 1.000000000000000000 ),
 .UNSPECIFIED. ) ;
#24618=ORIENTED_EDGE ( 'NONE', *, *, #43881, .F. ) ;
#24621=CARTESIAN_POINT ( 'NONE',  ( -1.500000000000000000, -79.00000000000000000, 0.000000000000000000 ) ) ;
#24622=EDGE_CURVE ( 'NONE', #1594, #39914, #12564, .T. ) ;
#24626=DIRECTION ( 'NONE',  ( 0.000000000000000000, -0.5547001962253867990, -0.8320502943377385829 ) ) ;
#24629=CARTESIAN_POINT ( 'NONE',  ( -0.6947089123876000194, -82.22113100666500429, -1.054176937042999862 ) ) ;
#24648=EDGE_CURVE ( 'NONE', #5425, #9344, #13812, .T. ) ;
#24658=CARTESIAN_POINT ( 'NONE',  ( 1.367042039058000036, -82.20187207508699601, 0.8392497673348999765 ) ) ;
#24682=ORIENTED_EDGE ( 'NONE', *, *, #56544, .T. ) ;
#24701=AXIS2_PLACEMENT_3D ( 'NONE', #50553, #41394, #45840 ) ;
#24703=FACE_OUTER_BOUND ( 'NONE', #12607, .T. ) ;
#24716=CARTESIAN_POINT ( 'NONE',  ( 0.6224761083686999319, -81.79798298199800399, -1.179448874982999884 ) ) ;
#24733=CARTESIAN_POINT ( 'NONE',  ( -0.2056945464814999847, -80.37710733580000522, 1.601533168507999871 ) ) ;
#24738=CARTESIAN_POINT ( 'NONE',  ( 0.6849175148897999055, -77.84603263957740182, -1.144319635748999975 ) ) ;
#24760=CARTESIAN_POINT ( 'NONE',  ( -1.310679582531389276, -81.35833333333332007, 0.7554284705563443225 ) ) ;
#24776=EDGE_CURVE ( 'NONE', #10831, #54597, #23601, .T. ) ;
#24789=VERTEX_POINT ( 'NONE', #45773 ) ;
#24799=ORIENTED_EDGE ( 'NONE', *, *, #57608, .F. ) ;
#24807=B_SPLINE_CURVE_WITH_KNOTS ( 'NONE', 3,
 ( #5525, #51300, #23534, #843 ),
 .UNSPECIFIED., .F., .F.,
 ( 4, 4 ),
 ( 0.000000000000000000, 0.1666666058611807055 ),
 .UNSPECIFIED. ) ;
#24808=CARTESIAN_POINT ( 'NONE',  ( -0.3252833033496160819, -78.25425631041045449, -1.232823141656065102 ) ) ;
#24837=CARTESIAN_POINT ( 'NONE',  ( -1.500872881732000064, -78.55864840198100296, -0.2152271930174000092 ) ) ;
#24839=CARTESIAN_POINT ( 'NONE',  ( 0.000000000000000000, -76.15000000005198899, 0.000000000000000000 ) ) ;
#24854=CARTESIAN_POINT ( 'NONE',  ( -1.250000000000000000, -77.75000000000000000, 0.000000000000000000 ) ) ;
#24862=CARTESIAN_POINT ( 'NONE',  ( 0.8920022376942984277, -81.46635564469825397, 0.9829159123015102084 ) ) ;
#24863=ORIENTED_EDGE ( 'NONE', *, *, #4833, .F. ) ;
#24871=EDGE_CURVE ( 'NONE', #50394, #5279, #25340, .T. ) ;
#24886=CARTESIAN_POINT ( 'NONE',  ( -0.3926218265389189721, -78.00416666666666288, -1.460959015002473604 ) ) ;
#24917=CARTESIAN_POINT ( 'NONE',  ( -0.5080623288857000208, -82.20492321929599200, -1.218433453902000085 ) ) ;
#24924=CARTESIAN_POINT ( 'NONE',  ( -0.5995968343850351934, -82.21604462272937042, -1.140767552750202807 ) ) ;
#24929=DIRECTION ( 'NONE',  ( 1.000000000000000000, 0.000000000000000000, 0.000000000000000000 ) ) ;
#24942=VECTOR ( 'NONE', #14900, 1000.000000000000114 ) ;
#24949=CARTESIAN_POINT ( 'NONE',  ( 1.310679582531385279, -81.29166666666668561, 0.7554284705563519831 ) ) ;
#24983=CARTESIAN_POINT ( 'NONE',  ( -1.120379678216000041, -79.22373702731300682, -0.7232983489183999470 ) ) ;
#24998=CARTESIAN_POINT ( 'NONE',  ( 0.8471236057751000414, -80.95456838452000170, 1.030027924806000028 ) ) ;
#25014=CARTESIAN_POINT ( 'NONE',  ( 1.377412799619999850, -79.28562962141599257, 0.8425838727997000399 ) ) ;
#25019=ORIENTED_EDGE ( 'NONE', *, *, #28832, .F. ) ;
#25038=CARTESIAN_POINT ( 'NONE',  ( -1.181111693982000110, -79.17654225787899236, -0.4092372983238000139 ) ) ;
#25042=CARTESIAN_POINT ( 'NONE',  ( 1.310679582531385501, -78.19166666666669130, 0.7554284705563518720 ) ) ;
#25074=ORIENTED_EDGE ( 'NONE', *, *, #30799, .F. ) ;
#25087=EDGE_CURVE ( 'NONE', #9344, #35383, #39498, .T. ) ;
#25089=CARTESIAN_POINT ( 'NONE',  ( 0.06739144895349272191, -78.77900521155609681, -1.272095446073437053 ) ) ;
#25101=B_SPLINE_CURVE_WITH_KNOTS ( 'NONE', 3,
 ( #765, #14590, #14296, #32290 ),
 .UNSPECIFIED., .F., .F.,
 ( 4, 4 ),
 ( 0.000000000000000000, 1.000000000000000000 ),
 .UNSPECIFIED. ) ;
#25116=EDGE_LOOP ( 'NONE', ( #9282, #17323, #47064, #27572 ) ) ;
#25118=CARTESIAN_POINT ( 'NONE',  ( -0.9462876233756999378, -80.18059372536998808, 0.9192961133846000443 ) ) ;
#25121=CARTESIAN_POINT ( 'NONE',  ( -1.308462286196999891, -79.00516201241099168, 0.7661340681064999769 ) ) ;
#25136=CARTESIAN_POINT ( 'NONE',  ( 0.8344599933502094835, -78.06822408831668270, 0.9640149690932605653 ) ) ;
#25145=CARTESIAN_POINT ( 'NONE',  ( 1.226743013016005523, -80.87800081614069825, -0.3449182370377862905 ) ) ;
#25224=CARTESIAN_POINT ( 'NONE',  ( 1.500000000000000888, -80.23958333333334281, -0.1963495408493590444 ) ) ;
#25227=EDGE_CURVE ( 'NONE', #51104, #46629, #1189, .T. ) ;
#25236=CARTESIAN_POINT ( 'NONE',  ( -1.460959015002474937, -78.97916666666664298, 0.3926218265389144757 ) ) ;
#25239=VECTOR ( 'NONE', #37083, 1000.000000000000000 ) ;
#25272=CARTESIAN_POINT ( 'NONE',  ( -0.6211595220380999871, -80.76172835212699397, -1.084739991049000096 ) ) ;
#25286=CARTESIAN_POINT ( 'NONE',  ( -1.066991882994506424, -79.06378521489916977, -1.111185832896742998 ) ) ;
#25294=DIRECTION ( 'NONE',  ( 1.000000000000000000, 0.000000000000000000, 0.000000000000000000 ) ) ;
#25303=CARTESIAN_POINT ( 'NONE',  ( -0.6623784515263000383, -79.58330536170299752, -1.472572141918999877 ) ) ;
#25317=B_SPLINE_CURVE_WITH_KNOTS ( 'NONE', 3,
 ( #43716, #26842, #21261, #44570, #21551, #7975 ),
 .UNSPECIFIED., .F., .F.,
 ( 4, 2, 4 ),
 ( 0.000000000000000000, 0.5000000000000000000, 1.000000000000000000 ),
 .UNSPECIFIED. ) ;
#25340=LINE ( 'NONE', #34185, #49703 ) ;
#25347=CARTESIAN_POINT ( 'NONE',  ( -1.500000000000000000, -78.50000000000000000, 0.000000000000000000 ) ) ;
#25356=EDGE_LOOP ( 'NONE', ( #1790, #49516, #37590, #36628, #32160, #43201, #43851, #24485, #3823, #40864 ) ) ;
#25383=ORIENTED_EDGE ( 'NONE', *, *, #51117, .F. ) ;
#25392=CARTESIAN_POINT ( 'NONE',  ( -0.6929804918870210440, -82.20905653057849349, -1.080747793140661717 ) ) ;
#25405=CARTESIAN_POINT ( 'NONE',  ( 0.9683804214594998738, -79.93253060846500091, -0.8959938446301999315 ) ) ;
#25409=CARTESIAN_POINT ( 'NONE',  ( -1.403409243600000300, -78.61402008970900113, -0.2012507760191999950 ) ) ;
#25420=CARTESIAN_POINT ( 'NONE',  ( 3.799999999999999822, -77.50000000000000000, 0.000000000000000000 ) ) ;
#25422=ORIENTED_EDGE ( 'NONE', *, *, #44602, .F. ) ;
#25435=CARTESIAN_POINT ( 'NONE',  ( -0.1360927073799415854, -80.76669044317051771, -1.267130688116418824 ) ) ;
#25447=ORIENTED_EDGE ( 'NONE', *, *, #16747, .T. ) ;
#25451=B_SPLINE_CURVE_WITH_KNOTS ( 'NONE', 3,
 ( #12440, #3581, #53459, #35142, #48190, #17746, #26297, #34571, #3867, #49338, #3302, #49039, #26005, #39015, #21867, #39875, #53763, #13002 ),
 .UNSPECIFIED., .F., .F.,
 ( 4, 2, 2, 2, 2, 2, 2, 2, 4 ),
 ( 0.000000000000000000, 0.1249999999999999722, 0.2499999999999999445, 0.3749999999999998890, 0.4999999999999998890, 0.6249999999999998890, 0.7499999999999997780, 0.8749999999999998890, 1.000000000000000000 ),
 .UNSPECIFIED. ) ;
#25498=CARTESIAN_POINT ( 'NONE',  ( 0.000000000000000000, -75.67500000000001137, 0.000000000000000000 ) ) ;
#25517=AXIS2_PLACEMENT_3D ( 'NONE', #27685, #54854, #36555 ) ;
#25525=EDGE_CURVE ( 'NONE', #49361, #19498, #17357, .T. ) ;
#25555=EDGE_CURVE ( 'NONE', #22104, #12731, #54863, .T. ) ;
#25560=CARTESIAN_POINT ( 'NONE',  ( -0.2976639488673999967, -79.61479940856000326, 1.299989344602000108 ) ) ;
#25570=EDGE_CURVE ( 'NONE', #37791, #5068, #44147, .T. ) ;
#25572=CARTESIAN_POINT ( 'NONE',  ( 1.221474390223999951, -81.39524338914699797, -0.5353283698298000326 ) ) ;
#25573=CARTESIAN_POINT ( 'NONE',  ( -0.9218200799623714747, -80.47291666666669130, -1.199500263597270466 ) ) ;
#25583=CARTESIAN_POINT ( 'NONE',  ( 0.3526813275444999896, -81.09526194714700864, 1.262314098292000031 ) ) ;
#25589=CARTESIAN_POINT ( 'NONE',  ( -0.7520647764090000464, -80.57555782932399779, -1.313341758254999991 ) ) ;
#25610=CARTESIAN_POINT ( 'NONE',  ( 0.8763811889879414840, -79.33555707640819321, -0.9249508082997421887 ) ) ;
#25621=ADVANCED_FACE ( 'NONE', ( #301 ), #36121, .F. ) ;
#25639=CARTESIAN_POINT ( 'NONE',  ( -1.100846539600000007, -79.28247803031800345, -0.6190985795237999856 ) ) ;
#25665=EDGE_CURVE ( 'NONE', #30464, #16033, #15285, .T. ) ;
#25683=CARTESIAN_POINT ( 'NONE',  ( 1.500000000000000000, -79.75000000000000000, 0.000000000000000000 ) ) ;
#25691=CARTESIAN_POINT ( 'NONE',  ( -0.2488193260981999833, -80.18635278971700586, 1.395760840247999957 ) ) ;
#25694=CARTESIAN_POINT ( 'NONE',  ( 0.6485435286463999693, -78.70748627212400095, -1.370523042014000215 ) ) ;
#25698=CARTESIAN_POINT ( 'NONE',  ( 0.000000000000000000, -76.00000000000000000, 0.000000000000000000 ) ) ;
#25703=DIRECTION ( 'NONE',  ( -1.000000000000000000, 0.000000000000000000, 0.000000000000000000 ) ) ;
#25720=DIRECTION ( 'NONE',  ( 0.000000000000000000, 1.000000000000000000, 0.000000000000000000 ) ) ;
#25722=CARTESIAN_POINT ( 'NONE',  ( 0.5071878057841813225, -81.30734082616947944, -1.169795988924593022 ) ) ;
#25754=ORIENTED_EDGE ( 'NONE', *, *, #25525, .F. ) ;
#25755=B_SPLINE_CURVE_WITH_KNOTS ( 'NONE', 3,
 ( #7615, #25902, #21188, #25042, #20902, #43926, #47515, #48361, #48084, #52210, #20332, #56924, #7043, #39190, #43064, #38620, #3474, #12050 ),
 .UNSPECIFIED., .F., .F.,
 ( 4, 2, 2, 2, 2, 2, 2, 2, 4 ),
 ( 0.000000000000000000, 0.1249999999999999722, 0.2499999999999999445, 0.3749999999999998890, 0.4999999999999998890, 0.6249999999999998890, 0.7499999999999997780, 0.8749999999999998890, 1.000000000000000000 ),
 .UNSPECIFIED. ) ;
#25819=CARTESIAN_POINT ( 'NONE',  ( 1.250000000000000000, -76.50000000000000000, 0.000000000000000000 ) ) ;
#25856=CARTESIAN_POINT ( 'NONE',  ( -0.7579940186957824233, -80.67607680420574923, 1.024633870185459816 ) ) ;
#25860=CARTESIAN_POINT ( 'NONE',  ( -0.05395919428434999693, -80.79989190857401127, -1.332567581519000122 ) ) ;
#25877=CARTESIAN_POINT ( 'NONE',  ( -0.2488193260981999833, -79.99172447744500403, 1.395760840247999957 ) ) ;
#25887=ORIENTED_EDGE ( 'NONE', *, *, #22519, .T. ) ;
#25902=CARTESIAN_POINT ( 'NONE',  ( 1.499999999999999778, -78.16041666666670551, 0.1963495408493654004 ) ) ;
#25915=CARTESIAN_POINT ( 'NONE',  ( -1.999999999936000084, -76.30000000006400285, 2.601307828485999989E-10 ) ) ;
#25920=CARTESIAN_POINT ( 'NONE',  ( 0.000000000000000000, -77.29999999999999716, 0.000000000000000000 ) ) ;
#25921=CARTESIAN_POINT ( 'NONE',  ( 0.3926218265389220807, -78.64583333333334281, -1.460959015002473382 ) ) ;
#25926=CARTESIAN_POINT ( 'NONE',  ( -1.305945605467999870, -78.75327671425300480, -0.1872743590209999809 ) ) ;
#25975=CARTESIAN_POINT ( 'NONE',  ( -1.260178996155999931, -80.33519065986000385, -0.6496216418182000352 ) ) ;
#25979=CARTESIAN_POINT ( 'NONE',  ( 1.398095685538000010, -78.36595697280360184, 0.2353462009024000212 ) ) ;
#26005=CARTESIAN_POINT ( 'NONE',  ( -0.9218200799623778030, -79.32708333333336270, 1.199500263597266914 ) ) ;
#26013=CARTESIAN_POINT ( 'NONE',  ( -1.333333333333333259, -77.79999999999999716, 0.000000000000000000 ) ) ;
#26034=DIRECTION ( 'NONE',  ( -1.000000000000000000, 0.000000000000000000, 0.000000000000000000 ) ) ;
#26083=LINE ( 'NONE', #8085, #27083 ) ;
#26095=CARTESIAN_POINT ( 'NONE',  ( 0.1963495408493571015, -78.86458333333331439, 1.500000000000000444 ) ) ;
#26131=EDGE_CURVE ( 'NONE', #34809, #22868, #26879, .T. ) ;
#26151=CARTESIAN_POINT ( 'NONE',  ( -0.1832406609208000192, -81.79214437619499734, -1.320984106490000087 ) ) ;
#26163=CARTESIAN_POINT ( 'NONE',  ( 0.6345915023811000699, -80.90716293419500005, -1.146778027003000133 ) ) ;
#26166=AXIS2_PLACEMENT_3D ( 'NONE', #22227, #27525, #17216 ) ;
#26169=CARTESIAN_POINT ( 'NONE',  ( 1.061497194196000082, -80.23402853000399659, -1.082666072229000020 ) ) ;
#26183=FACE_OUTER_BOUND ( 'NONE', #57131, .T. ) ;
#26187=CARTESIAN_POINT ( 'NONE',  ( -0.9215901096570091600, -81.82721060988042439, 1.199517572493949524 ) ) ;
#26217=DIRECTION ( 'NONE',  ( 1.000000000000000000, 0.000000000000000000, 0.000000000000000000 ) ) ;
#26220=ORIENTED_EDGE ( 'NONE', *, *, #40283, .T. ) ;
#26227=DIRECTION ( 'NONE',  ( 0.000000000000000000, 1.000000000000000000, -1.646830819861000174E-14 ) ) ;
#26233=CARTESIAN_POINT ( 'NONE',  ( -1.500000000000000000, -78.50000000000000000, 0.000000000000000000 ) ) ;
#26238=ORIENTED_EDGE ( 'NONE', *, *, #28627, .T. ) ;
#26248=ORIENTED_EDGE ( 'NONE', *, *, #36092, .T. ) ;
#26255=FACE_OUTER_BOUND ( 'NONE', #45603, .T. ) ;
#26268=CARTESIAN_POINT ( 'NONE',  ( -0.5815971981373999622, -79.88867704943100989, -1.292982629223000002 ) ) ;
#26297=CARTESIAN_POINT ( 'NONE',  ( 0.7554284705563452107, -79.23333333333330586, 1.310679582531388609 ) ) ;
#26384=CARTESIAN_POINT ( 'NONE',  ( -1.178447680628000205, -80.95308451575900222, -0.9280415206345000723 ) ) ;
#26390=CARTESIAN_POINT ( 'NONE',  ( -0.2806432552994999607, -82.10210008720301289, -1.487181012905000044 ) ) ;
#26393=ORIENTED_EDGE ( 'NONE', *, *, #31524, .F. ) ;
#26396=CARTESIAN_POINT ( 'NONE',  ( 1.199500263597268246, -78.30208333333331439, 0.9218200799623752495 ) ) ;
#26407=CARTESIAN_POINT ( 'NONE',  ( -0.8465867926663999121, -80.78896482857800265, -0.9556525628790000226 ) ) ;
#26415=CARTESIAN_POINT ( 'NONE',  ( -2.000000000000000000, -76.29999999999999716, 0.000000000000000000 ) ) ;
#26425=CARTESIAN_POINT ( 'NONE',  ( -0.6380817373966316541, -79.83329071193379889, -1.104274488347721794 ) ) ;
#26430=CARTESIAN_POINT ( 'NONE',  ( 0.1510373474112000070, -81.58785527686900707, 1.325052402434999888 ) ) ;
#26438=CARTESIAN_POINT ( 'NONE',  ( -1.335058897431999902, -82.31057754807500260, -0.2280211375632000270 ) ) ;
#26444=CARTESIAN_POINT ( 'NONE',  ( 1.396889377938999921, -80.33901284111300356, -0.2424037069397000088 ) ) ;
#26448=EDGE_CURVE ( 'NONE', #2323, #10831, #17646, .T. ) ;
#26460=EDGE_CURVE ( 'NONE', #39760, #16765, #24807, .T. ) ;
#26464=CARTESIAN_POINT ( 'NONE',  ( 1.199237972082057846, -81.70227769186961098, 0.9216820448048951286 ) ) ;
#26476=CARTESIAN_POINT ( 'NONE',  ( 0.3926218265389221362, -80.04583333333334849, -1.460959015002473160 ) ) ;
#26477=CIRCLE ( 'NONE', #1082, 0.5000000000000000000 ) ;
#26497=CARTESIAN_POINT ( 'NONE',  ( 1.013266355313000133, -78.16944336237389734, 1.127933319133000101 ) ) ;
#26548=CARTESIAN_POINT ( 'NONE',  ( 1.377412799619999850, -79.70174468460000128, 0.8425838727997000399 ) ) ;
#26596=EDGE_CURVE ( 'NONE', #22868, #51104, #9958, .T. ) ;
#26700=CARTESIAN_POINT ( 'NONE',  ( -0.5470841013496000604, -79.85702391966199798, -1.216254552179000026 ) ) ;
#26719=CARTESIAN_POINT ( 'NONE',  ( -1.152722609229902551, -80.21492969711312071, 0.5434249559639973137 ) ) ;
#26721=ORIENTED_EDGE ( 'NONE', *, *, #37977, .F. ) ;
#26724=CARTESIAN_POINT ( 'NONE',  ( 0.6791306551168999617, -81.34563076576598917, -1.147762040996999966 ) ) ;
#26732=CARTESIAN_POINT ( 'NONE',  ( -1.272578778811999989, -80.89250696768399962, -0.6917752173717000019 ) ) ;
#26738=CARTESIAN_POINT ( 'NONE',  ( -0.2660992726780999629, -79.93635278971700586, 1.492693313845999903 ) ) ;
#26741=CARTESIAN_POINT ( 'NONE',  ( -0.7554284705563483193, -78.98333333333333428, -1.310679582531387721 ) ) ;
#26759=CARTESIAN_POINT ( 'NONE',  ( 1.251843065520180875, -82.06770833143092148, -0.7205419773649445192 ) ) ;
#26762=CARTESIAN_POINT ( 'NONE',  ( -0.9248060758160334682, -80.21013857831869132, -0.8761209355067355320 ) ) ;
#26786=CARTESIAN_POINT ( 'NONE',  ( -1.509488703453999880, -79.36014632351999865, -0.1420306293263000064 ) ) ;
#26793=CARTESIAN_POINT ( 'NONE',  ( -1.287313221243000072, -78.26290954478920980, 0.5940404451740000091 ) ) ;
#26831=EDGE_CURVE ( 'NONE', #28437, #12549, #45874, .T. ) ;
#26842=CARTESIAN_POINT ( 'NONE',  ( -1.250000000013809398, -82.25000000000000000, -0.2084624058389335510 ) ) ;
#26846=CARTESIAN_POINT ( 'NONE',  ( -1.379800422845999908, -80.88668858139899953, -0.6283944928419999965 ) ) ;
#26847=CARTESIAN_POINT ( 'NONE',  ( -0.8575312565364999751, -77.72675193319649622, -1.002634541711000082 ) ) ;
#26877=DIRECTION ( 'NONE',  ( 0.000000000000000000, -1.000000000000000000, 0.000000000000000000 ) ) ;
#26879=B_SPLINE_CURVE_WITH_KNOTS ( 'NONE', 3,
 ( #24854, #41991, #42870, #20430, #20145, #7135, #55866, #29556, #1559, #46440, #55272, #38425, #15115, #15998, #25136, #43162, #24563, #10408, #19851, #6555, #51154, #19551, #10709, #28393, #37258, #47024, #28687, #37846, #38132, #42580, #15416, #56443, #2718, #33699, #51738, #5968, #11287, #6258, #42290, #33409, #2144, #51447, #56155, #29267, #47315, #17435, #30991, #44302, #7713, #53450, #56736, #39865, #47893, #3293, #43443, #44597, #3004, #57014, #16296, #12995, #57585, #21000, #21285, #34273, #49030 ),
 .UNSPECIFIED., .F., .F.,
 ( 4, 2, 2, 2, 2, 2, 2, 2, 2, 2, 2, 2, 2, 2, 2, 2, 1, 2, 2, 2, 2, 2, 2, 2, 2, 2, 2, 2, 2, 2, 2, 2, 4 ),
 ( 0.000000000000000000, 0.03125000000000000000, 0.06250000000000000000, 0.09375000000000000000, 0.1250000000000000000, 0.1562500000000000000, 0.1875000000000000000, 0.2187500000000000000, 0.2500000000000000000, 0.2812500000000000000, 0.3125000000000000000, 0.3437500000000000000, 0.3750000000000000000, 0.4062500000000000000, 0.4375000000000000000, 0.4687500000000000000, 0.5000000000000000000, 0.5312500000000000000, 0.5625000000000000000, 0.5937500000000000000, 0.6250000000000000000, 0.6562500000000000000, 0.6875000000000000000, 0.7187500000000000000, 0.7500000000000000000, 0.7812500000000000000, 0.8125000000000000000, 0.8437500000000000000, 0.8750000000000000000, 0.9062500000000000000, 0.9375000000000000000, 0.9687500000000000000, 1.000000000000000000 ),
 .UNSPECIFIED. ) ;
#26890=CARTESIAN_POINT ( 'NONE',  ( -3.999999999993000266, -77.30000000000720206, 8.632643823722999667E-11 ) ) ;
#26937=CARTESIAN_POINT ( 'NONE',  ( -0.4831833036036000117, -82.27957484316098657, -1.158768654956999988 ) ) ;
#26981=CARTESIAN_POINT ( 'NONE',  ( -0.3926218265389255779, -78.39583333333334281, 1.460959015002472494 ) ) ;
#26993=CARTESIAN_POINT ( 'NONE',  ( 1.199918086393000127, -80.50782662941900014, 0.5820416783086000967 ) ) ;
#27003=VECTOR ( 'NONE', #27882, 1000.000000000000000 ) ;
#27014=CARTESIAN_POINT ( 'NONE',  ( 0.8977011673350683285, -80.43755243846868552, -0.9055672397132533691 ) ) ;
#27015=ORIENTED_EDGE ( 'NONE', *, *, #36838, .F. ) ;
#27019=CARTESIAN_POINT ( 'NONE',  ( 1.193978368322000216, -81.97891765811500875, -0.5941311122250999555 ) ) ;
#27027=CARTESIAN_POINT ( 'NONE',  ( 1.496078468352999957, -81.11195581612699357, 0.1750711238899000100 ) ) ;
#27033=CARTESIAN_POINT ( 'NONE',  ( 0.6554565090088000368, -79.88674016633599706, 1.367230381797000183 ) ) ;
#27038=ORIENTED_EDGE ( 'NONE', *, *, #12268, .F. ) ;
#27043=ORIENTED_EDGE ( 'NONE', *, *, #43151, .T. ) ;
#27047=ORIENTED_EDGE ( 'NONE', *, *, #34546, .T. ) ;
#27053=CARTESIAN_POINT ( 'NONE',  ( -1.311000177045137827, -81.85844383938299984, 0.7555961656110528057 ) ) ;
#27055=CARTESIAN_POINT ( 'NONE',  ( 0.6791567373625641002, -80.48046376981821481, 1.078384872319655186 ) ) ;
#27065=CARTESIAN_POINT ( 'NONE',  ( 1.500000000000001110, -80.13958333333334849, -0.1963495408493590721 ) ) ;
#27083=VECTOR ( 'NONE', #44107, 1000.000000000000114 ) ;
#27090=CARTESIAN_POINT ( 'NONE',  ( 1.391768007815999963, -78.07021811561179447, -0.6016011292324999760 ) ) ;
#27138=CARTESIAN_POINT ( 'NONE',  ( -1.158153954042000056, -80.34670878855399678, 1.125119257983999921 ) ) ;
#27151=CARTESIAN_POINT ( 'NONE',  ( -1.500000000000000000, -80.51769483858633691, -0.3335398494528040159 ) ) ;
#27241=CARTESIAN_POINT ( 'NONE',  ( 1.500000000000001110, -79.63137852148993545, -0.3510066005171248449 ) ) ;
#27245=DIRECTION ( 'NONE',  ( 0.000000000000000000, 1.000000000000000000, 0.000000000000000000 ) ) ;
#27259=CARTESIAN_POINT ( 'NONE',  ( 1.272221273747917714, -77.90442370964647978, 0.06754771032932266328 ) ) ;
#27271=CARTESIAN_POINT ( 'NONE',  ( -0.8558294506340999863, -80.91139712605799161, 1.369222347861999811 ) ) ;
#27272=ORIENTED_EDGE ( 'NONE', *, *, #57608, .T. ) ;
#27274=ORIENTED_EDGE ( 'NONE', *, *, #54253, .F. ) ;
#27287=CARTESIAN_POINT ( 'NONE',  ( -1.308081345731999967, -80.70627712294299272, 0.2599445073669000017 ) ) ;
#27289=AXIS2_PLACEMENT_3D ( 'NONE', #23832, #33560, #32672 ) ;
#27307=CARTESIAN_POINT ( 'NONE',  ( 0.2725326480772000126, -79.08050961830200265, 1.305490477442999842 ) ) ;
#27325=CARTESIAN_POINT ( 'NONE',  ( 1.407325970645999957, -82.04410394639400295, -0.05680320185105999786 ) ) ;
#27331=CARTESIAN_POINT ( 'NONE',  ( -1.235017835984000056, -79.15406894431399110, 0.06195353447049999768 ) ) ;
#27350=CARTESIAN_POINT ( 'NONE',  ( 0.000000000000000000, -76.00000000000000000, 0.000000000000000000 ) ) ;
#27354=CARTESIAN_POINT ( 'NONE',  ( -0.04771499852550991488, -80.52816821537712144, 1.273416777469591477 ) ) ;
#27360=EDGE_CURVE ( 'NONE', #32930, #27527, #3565, .T. ) ;
#27371=FACE_OUTER_BOUND ( 'NONE', #29663, .T. ) ;
#27385=CARTESIAN_POINT ( 'NONE',  ( 1.199500263597268246, -79.70208333333333428, 0.9218200799623752495 ) ) ;
#27386=CARTESIAN_POINT ( 'NONE',  ( 1.301389418711000223, -78.01484642788379631, -0.5625343731648000389 ) ) ;
#27406=CARTESIAN_POINT ( 'NONE',  ( 1.500000000000001110, -81.63958333333334849, -0.1963495408493590721 ) ) ;
#27408=CARTESIAN_POINT ( 'NONE',  ( -1.250000000000000000, -77.10000000000000853, 0.000000000000000000 ) ) ;
#27409=ORIENTED_EDGE ( 'NONE', *, *, #22352, .T. ) ;
#27435=CARTESIAN_POINT ( 'NONE',  ( -0.1931516691869999969, -80.73785071125600155, 1.503874604587000174 ) ) ;
#27440=CARTESIAN_POINT ( 'NONE',  ( -2.799999999997999645, -75.99999999999799627, -5.978147109672000789E-11 ) ) ;
#27476=CARTESIAN_POINT ( 'NONE',  ( -0.1963495408493605987, -81.11458333333332860, -1.500000000000000444 ) ) ;
#27498=VERTEX_POINT ( 'NONE', #2229 ) ;
#27525=DIRECTION ( 'NONE',  ( 0.000000000000000000, 1.000000000000000000, 0.000000000000000000 ) ) ;
#27527=VERTEX_POINT ( 'NONE', #12228 ) ;
#27537=EDGE_CURVE ( 'NONE', #39723, #42409, #9217, .T. ) ;
#27559=CARTESIAN_POINT ( 'NONE',  ( 1.560799078659000028, -80.76255925591399887, 0.4136666654166999413 ) ) ;
#27572=ORIENTED_EDGE ( 'NONE', *, *, #22427, .T. ) ;
#27576=CARTESIAN_POINT ( 'NONE',  ( 0.000000000000000000, -75.67500000000001137, 0.000000000000000000 ) ) ;
#27578=CARTESIAN_POINT ( 'NONE',  ( 1.021809889922000059, -79.46012293261399861, -0.8570204080543000202 ) ) ;
#27592=CARTESIAN_POINT ( 'NONE',  ( 0.6849175148897999055, -77.88980665715600082, -1.144319635748999975 ) ) ;
#27603=CARTESIAN_POINT ( 'NONE',  ( -1.127489577578000057, -80.80475223809600038, -0.5989559841152000130 ) ) ;
#27614=CARTESIAN_POINT ( 'NONE',  ( 0.9313429465132000429, -81.47980690754000932, -1.056595210376000127 ) ) ;
#27620=CARTESIAN_POINT ( 'NONE',  ( -1.500000000000000000, -81.50000000000000000, 0.000000000000000000 ) ) ;
#27623=CARTESIAN_POINT ( 'NONE',  ( -1.500000000000000000, -79.39999999999999147, 0.000000000000000000 ) ) ;
#27640=CARTESIAN_POINT ( 'NONE',  ( -1.500000000000000000, -80.50000000000000000, 0.000000000000000000 ) ) ;
#27642=CARTESIAN_POINT ( 'NONE',  ( -1.152422862266062609, -80.11472968720097754, 0.5432694035117214826 ) ) ;
#27674=CARTESIAN_POINT ( 'NONE',  ( 0.9474668951539000350, -78.11407167464599866, 1.054687619119999864 ) ) ;
#27683=CARTESIAN_POINT ( 'NONE',  ( 1.500000000000000888, -81.73958333333332860, -0.1963495408493590444 ) ) ;
#27685=CARTESIAN_POINT ( 'NONE',  ( 0.000000000000000000, -76.29999999999999716, 0.000000000000000000 ) ) ;
#27696=CARTESIAN_POINT ( 'NONE',  ( -1.500000000000000000, -81.40000000000000568, 0.000000000000000000 ) ) ;
#27698=DIRECTION ( 'NONE',  ( 0.000000000000000000, 0.000000000000000000, -1.000000000000000000 ) ) ;
#27723=CARTESIAN_POINT ( 'NONE',  ( -0.6885369103866999518, -80.44017497096899660, -1.350873448928000098 ) ) ;
#27764=CARTESIAN_POINT ( 'NONE',  ( -0.8130050274896999385, -80.73022382557400078, -1.038954733251000073 ) ) ;
#27770=CARTESIAN_POINT ( 'NONE',  ( -1.500000000000000222, -81.01041666666667140, -0.1963495408493622085 ) ) ;
#27794=CARTESIAN_POINT ( 'NONE',  ( 0.8292593438864999111, -77.65986211677478934, -1.385477418387000004 ) ) ;
#27818=ADVANCED_FACE ( 'NONE', ( #54998 ), #14547, .T. ) ;
#27825=CARTESIAN_POINT ( 'NONE',  ( 0.000000000000000000, -75.67500000000001137, 0.000000000000000000 ) ) ;
#27829=CARTESIAN_POINT ( 'NONE',  ( 0.9218200799623694763, -80.32291666666667140, 1.199500263597272465 ) ) ;
#27846=FACE_OUTER_BOUND ( 'NONE', #11046, .T. ) ;
#27849=CARTESIAN_POINT ( 'NONE',  ( -0.9913219194069000650, -81.11560668392900197, -1.147267625202000207 ) ) ;
#27874=DIRECTION ( 'NONE',  ( 1.000000000000000000, 0.000000000000000000, 0.000000000000000000 ) ) ;
#27881=CARTESIAN_POINT ( 'NONE',  ( 0.6284244718204999858, -78.42970690854529892, -1.176290284212999859 ) ) ;
#27882=DIRECTION ( 'NONE',  ( -9.562128866322998892E-12, 1.000000000000000000, -3.007558296593999951E-10 ) ) ;
#27899=CARTESIAN_POINT ( 'NONE',  ( 0.5145135761085000148, -82.00542612764600392, -1.415689478406999990 ) ) ;
#27918=ORIENTED_EDGE ( 'NONE', *, *, #35705, .T. ) ;
#27942=CARTESIAN_POINT ( 'NONE',  ( 0.2020314717676000016, -80.27144072411900311, -1.318241039644999946 ) ) ;
#28019=ADVANCED_FACE ( 'NONE', ( #28630 ), #19793, .T. ) ;
#28027=ORIENTED_EDGE ( 'NONE', *, *, #11013, .T. ) ;
#28138=CARTESIAN_POINT ( 'NONE',  ( 0.7219739802542000096, -81.27020361841898932, -1.220169230883999978 ) ) ;
#28146=EDGE_CURVE ( 'NONE', #35842, #32930, #37489, .T. ) ;
#28154=CARTESIAN_POINT ( 'NONE',  ( 1.500000000000000000, -79.25000000000000000, 0.000000000000000000 ) ) ;
#28158=DIRECTION ( 'NONE',  ( 0.000000000000000000, 1.000000000000000000, -1.093719250013000041E-14 ) ) ;
#28171=CARTESIAN_POINT ( 'NONE',  ( 1.166929042523999982, -78.93167174815900466, -0.6456414311070999279 ) ) ;
#28186=CARTESIAN_POINT ( 'NONE',  ( -1.562814397797999799, -82.38997108803900460, 0.3613598533091000320 ) ) ;
#28192=CARTESIAN_POINT ( 'NONE',  ( -1.250000000000000000, -77.10000000000000853, 0.000000000000000000 ) ) ;
#28193=CARTESIAN_POINT ( 'NONE',  ( -0.5991125319583999742, -80.24554665869699477, -1.175427489992000085 ) ) ;
#28205=EDGE_LOOP ( 'NONE', ( #45539, #24682, #34376, #23284, #37895 ) ) ;
#28244=CARTESIAN_POINT ( 'NONE',  ( 1.500000000000000000, -81.65000000000000568, 0.000000000000000000 ) ) ;
#28274=CARTESIAN_POINT ( 'NONE',  ( 1.166929042523999982, -78.88789773057999355, -0.6456414311070000078 ) ) ;
#28281=ORIENTED_EDGE ( 'NONE', *, *, #31123, .F. ) ;
#28282=EDGE_LOOP ( 'NONE', ( #17549, #16831, #28027, #40622 ) ) ;
#28302=CIRCLE ( 'NONE', #43405, 4.000000000000000000 ) ;
#28324=CARTESIAN_POINT ( 'NONE',  ( 1.401388975520860170, -81.11718075262649563, -0.6178868534844423888 ) ) ;
#28342=CARTESIAN_POINT ( 'NONE',  ( 1.302090486218000054, -81.92092678672000261, 0.2124289815698000017 ) ) ;
#28357=ORIENTED_EDGE ( 'NONE', *, *, #28832, .T. ) ;
#28365=B_SPLINE_CURVE_WITH_KNOTS ( 'NONE', 3,
 ( #36486, #5206, #8751, #14052, #32047, #36776, #26741, #50091, #9636, #4322, #41214, #9050, #54795, #13463, #32334, #22323, #50381, #31459 ),
 .UNSPECIFIED., .F., .F.,
 ( 4, 2, 2, 2, 2, 2, 2, 2, 4 ),
 ( 0.000000000000000000, 0.1250000000000000000, 0.2500000000000000000, 0.3750000000000000000, 0.5000000000000000000, 0.6250000000000000000, 0.7500000000000000000, 0.8750000000000000000, 1.000000000000000000 ),
 .UNSPECIFIED. ) ;
#28376=CARTESIAN_POINT ( 'NONE',  ( 1.190716386653000169, -78.80095245453999553, 1.090600000265000036 ) ) ;
#28393=CARTESIAN_POINT ( 'NONE',  ( -1.113300763112903935, -78.29084682967156539, -0.6200230202612950769 ) ) ;
#28412=CARTESIAN_POINT ( 'NONE',  ( -1.500000000000000000, -80.50000000000000000, 0.000000000000000000 ) ) ;
#28434=CARTESIAN_POINT ( 'NONE',  ( -0.2464170302977999882, -82.21284346265900922, -1.305809855734000102 ) ) ;
#28437=VERTEX_POINT ( 'NONE', #28882 ) ;
#28438=AXIS2_PLACEMENT_3D ( 'NONE', #47420, #55379, #46256 ) ;
#28441=SHAPE_DEFINITION_REPRESENTATION ( #11610, #4074 ) ;
#28465=CARTESIAN_POINT ( 'NONE',  ( -1.199500263597274241, -78.84791666666667709, 0.9218200799623669228 ) ) ;
#28466=CARTESIAN_POINT ( 'NONE',  ( 0.9834589317531000630, -79.07467101249899599, 0.9007689179829999615 ) ) ;
#28468=CARTESIAN_POINT ( 'NONE',  ( 1.500000000000000000, -77.75000000000000000, 0.000000000000000000 ) ) ;
#28485=CARTESIAN_POINT ( 'NONE',  ( 0.9960226344442998370, -81.53517859526800748, -1.129973388342000007 ) ) ;
#28500=EDGE_CURVE ( 'NONE', #23510, #49361, #25755, .T. ) ;
#28507=ORIENTED_EDGE ( 'NONE', *, *, #25555, .T. ) ;
#28529=CARTESIAN_POINT ( 'NONE',  ( 0.2659376973789999710, -79.77531449030800559, -1.306848610430999980 ) ) ;
#28557=CARTESIAN_POINT ( 'NONE',  ( -1.500000000000000000, -81.50000000000000000, 0.000000000000000000 ) ) ;
#28570=CARTESIAN_POINT ( 'NONE',  ( -0.1765672563250000049, -78.24877223242859259, -1.321892640673999919 ) ) ;
#28598=CARTESIAN_POINT ( 'NONE',  ( -1.024999350969000078, -80.97513535138099883, -1.157050009743000096 ) ) ;
#28615=CARTESIAN_POINT ( 'NONE',  ( -1.500000000000000000, -79.50000000000000000, 0.000000000000000000 ) ) ;
#28627=EDGE_CURVE ( 'NONE', #57022, #37791, #32738, .T. ) ;
#28630=FACE_OUTER_BOUND ( 'NONE', #14355, .T. ) ;
#28656=CLOSED_SHELL ( 'NONE', ( #3963, #56165, #47598, #16034, #11345, #48640, #11754, #16727, #19934, #8294, #49705, #906, #46031, #41844, #15104, #12248, #49212, #25621, #33808, #48368, #50981, #858, #18126, #16155, #56348, #28019, #44155, #48889, #4788, #12486, #11782, #46635, #11377, #23841, #6249, #19369, #8176, #53206, #20973, #8665, #11907, #48032, #14875, #35397, #33668, #27818, #46428, #40592, #51176, #21446, #56823, #48414, #19382, #41269, #51972, #31674, #54591, #17789, #47077 ) ) ;
#28687=CARTESIAN_POINT ( 'NONE',  ( -0.3253823571070225129, -78.35445332720156841, -1.233148206733681862 ) ) ;
#28696=CARTESIAN_POINT ( 'NONE',  ( -0.9200108141794000050, -81.78630577039299965, -0.9654823929056000065 ) ) ;
#28709=CARTESIAN_POINT ( 'NONE',  ( 0.1963495408493571015, -80.36458333333331439, 1.500000000000000444 ) ) ;
#28727=CARTESIAN_POINT ( 'NONE',  ( 0.7077020876660000681, -81.71095816450198868, -1.340932479011999856 ) ) ;
#28742=CARTESIAN_POINT ( 'NONE',  ( -0.6747260877994001316, -82.25000000000000000, -1.052256958371999840 ) ) ;
#28757=CARTESIAN_POINT ( 'NONE',  ( -1.500000000000000444, -78.88958333333333428, 0.1963495408493560745 ) ) ;
#28764=EDGE_LOOP ( 'NONE', ( #52886, #17261, #8247, #21744 ) ) ;
#28775=CIRCLE ( 'NONE', #18430, 4.000000000000000000 ) ;
#28780=CARTESIAN_POINT ( 'NONE',  ( 1.060702322374999840, -81.59055028299499668, -1.203351566307999887 ) ) ;
#28820=CARTESIAN_POINT ( 'NONE',  ( -1.248430190247999949, -79.21789842151099492, 0.06262635289305999720 ) ) ;
#28832=EDGE_CURVE ( 'NONE', #2323, #43690, #2773, .T. ) ;
#28860=CARTESIAN_POINT ( 'NONE',  ( 0.2086861075963999945, -78.49683534933389240, 1.317203954600000060 ) ) ;
#28882=CARTESIAN_POINT ( 'NONE',  ( 0.000000000000000000, -77.29999999999999716, -4.000000000000341949 ) ) ;
#28920=CARTESIAN_POINT ( 'NONE',  ( 0.000000000000000000, -75.67500000000001137, 0.000000000000000000 ) ) ;
#28933=CARTESIAN_POINT ( 'NONE',  ( 0.9331017648476999105, -81.97053941010099720, 0.9326770562470999559 ) ) ;
#28935=CARTESIAN_POINT ( 'NONE',  ( -0.3806779964142781858, -79.04933040305580505, 1.216001660871532275 ) ) ;
#28956=CARTESIAN_POINT ( 'NONE',  ( 1.310679582531385279, -79.79166666666667140, 0.7554284705563519831 ) ) ;
#28971=CARTESIAN_POINT ( 'NONE',  ( 1.500000000000000000, -80.75000000000000000, 0.000000000000000000 ) ) ;
#28992=CARTESIAN_POINT ( 'NONE',  ( 0.2579617086353386823, -81.29143934431662899, -1.247668167079378110 ) ) ;
#28994=CARTESIAN_POINT ( 'NONE',  ( 1.246077061130999919, -80.98666519049299950, -0.4752592857455000264 ) ) ;
#29019=CARTESIAN_POINT ( 'NONE',  ( 0.1963495408493637351, -78.03541666666667709, -1.499999999999999778 ) ) ;
#29027=CARTESIAN_POINT ( 'NONE',  ( -1.275842582732999997, -80.62523951446499382, -0.3715998334726999808 ) ) ;
#29028=ORIENTED_EDGE ( 'NONE', *, *, #30024, .F. ) ;
#29056=CARTESIAN_POINT ( 'NONE',  ( -0.9612450871864000046, -78.82660789559399461, -0.9244371432244999909 ) ) ;
#29059=DIRECTION ( 'NONE',  ( -1.000000000000000000, 0.000000000000000000, 0.000000000000000000 ) ) ;
#29060=CARTESIAN_POINT ( 'NONE',  ( 1.500000000000000000, -78.14999999999999147, 0.000000000000000000 ) ) ;
#29075=CARTESIAN_POINT ( 'NONE',  ( 1.144839767925999841, -81.15898056936499927, 0.9788987191686998601 ) ) ;
#29094=EDGE_LOOP ( 'NONE', ( #50962, #52055 ) ) ;
#29115=CARTESIAN_POINT ( 'NONE',  ( -0.9565643533716999825, -80.11676424817299846, 0.9292797142584000580 ) ) ;
#29127=CARTESIAN_POINT ( 'NONE',  ( 0.7554284705563509839, -77.66666666666667140, -1.310679582531385945 ) ) ;
#29128=CARTESIAN_POINT ( 'NONE',  ( 1.500000000000000000, -79.25000000000000000, 0.000000000000000000 ) ) ;
#29141=CARTESIAN_POINT ( 'NONE',  ( -0.9218200799623716968, -81.57291666666667140, -1.199500263597270910 ) ) ;
#29147=CARTESIAN_POINT ( 'NONE',  ( 1.610212697858000030, -79.23601699803499798, -0.1201205297940999978 ) ) ;
#29152=ORIENTED_EDGE ( 'NONE', *, *, #39362, .T. ) ;
#29154=CARTESIAN_POINT ( 'NONE',  ( 1.302799686710000016, -77.94525788633960417, 0.2851120931344000020 ) ) ;
#29173=PLANE ( 'NONE',  #45156 ) ;
#29197=AXIS2_PLACEMENT_3D ( 'NONE', #53401, #58129, #48699 ) ;
#29219=AXIS2_PLACEMENT_3D ( 'NONE', #41545, #22955, #19115 ) ;
#29242=CARTESIAN_POINT ( 'NONE',  ( -1.500000000000000888, -79.98958333333334281, 0.1963495408493559080 ) ) ;
#29251=CARTESIAN_POINT ( 'NONE',  ( 0.6064284284549000814, -78.76285795985199911, -1.281524057860000010 ) ) ;
#29267=CARTESIAN_POINT ( 'NONE',  ( -1.160984792064531756, -78.78379718552881172, -0.5251923553234724151 ) ) ;
#29275=CARTESIAN_POINT ( 'NONE',  ( -0.2413114649954342938, -81.25963638061078598, -1.251987394859889413 ) ) ;
#29318=VERTEX_POINT ( 'NONE', #19400 ) ;
#29332=CARTESIAN_POINT ( 'NONE',  ( 0.000000000000000000, -75.67500000000001137, 0.000000000000000000 ) ) ;
#29346=EDGE_LOOP ( 'NONE', ( #14700, #8925, #2083, #4996 ) ) ;
#29355=CARTESIAN_POINT ( 'NONE',  ( 1.500000000000000000, -78.75000000000000000, 0.000000000000000000 ) ) ;
#29367=CARTESIAN_POINT ( 'NONE',  ( 0.9218200799623694763, -81.32291666666668561, 1.199500263597272465 ) ) ;
#29401=CARTESIAN_POINT ( 'NONE',  ( -0.6056189234361001317, -80.26560211831599645, -1.188192690176999911 ) ) ;
#29417=CARTESIAN_POINT ( 'NONE',  ( -1.310679582531386611, -77.54166666666667140, -0.7554284705563495406 ) ) ;
#29428=CARTESIAN_POINT ( 'NONE',  ( 1.165893053700000070, -80.95418768743299154, -0.5987630157190000357 ) ) ;
#29439=CARTESIAN_POINT ( 'NONE',  ( -1.250000000000000000, -76.29999999999999716, -0.6999999999999999556 ) ) ;
#29452=ORIENTED_EDGE ( 'NONE', *, *, #26831, .F. ) ;
#29535=FACE_OUTER_BOUND ( 'NONE', #50961, .T. ) ;
#29538=CARTESIAN_POINT ( 'NONE',  ( 0.7786926255480000059, -77.71523380450280172, -1.300993539011999989 ) ) ;
#29556=CARTESIAN_POINT ( 'NONE',  ( 0.5253929667144483506, -77.90920784449171776, -1.161211157036742048 ) ) ;
#29563=CARTESIAN_POINT ( 'NONE',  ( 1.233875498716631158, -81.87979417287398576, -0.3168210084591759346 ) ) ;
#29566=CARTESIAN_POINT ( 'NONE',  ( -0.9816856958575284064, -80.76975118242557983, -0.7730884388065356605 ) ) ;
#29614=CARTESIAN_POINT ( 'NONE',  ( 0.000000000000000000, -76.39999999999899671, -3.399999999997999733 ) ) ;
#29618=CIRCLE ( 'NONE', #46640, 3.799999999999999822 ) ;
#29619=CARTESIAN_POINT ( 'NONE',  ( -0.3673871636652999983, -82.25905252924800948, -1.180734503437000038 ) ) ;
#29653=CARTESIAN_POINT ( 'NONE',  ( 1.500000000000000000, -81.25000000000000000, 0.000000000000000000 ) ) ;
#29654=CARTESIAN_POINT ( 'NONE',  ( -1.384806900013862530, -80.93538967717266530, -0.6660020126448532585 ) ) ;
#29663=EDGE_LOOP ( 'NONE', ( #38098, #28357, #13551, #50677 ) ) ;
#29674=ORIENTED_EDGE ( 'NONE', *, *, #19298, .T. ) ;
#29688=CARTESIAN_POINT ( 'NONE',  ( -0.1698911186725000078, -80.56327785860300139, 1.322768475116000042 ) ) ;
#29704=CARTESIAN_POINT ( 'NONE',  ( -1.460959015002473826, -80.42083333333334849, -0.3926218265389207485 ) ) ;
#29718=CARTESIAN_POINT ( 'NONE',  ( 1.237149555198000073, -79.18640437465400339, -1.037631781681999987 ) ) ;
#29724=B_SPLINE_CURVE_WITH_KNOTS ( 'NONE', 3,
 ( #27623, #58347, #49799, #1090 ),
 .UNSPECIFIED., .F., .F.,
 ( 4, 4 ),
 ( 0.000000000000000000, 1.000000000000000000 ),
 .UNSPECIFIED. ) ;
#29729=ORIENTED_EDGE ( 'NONE', *, *, #42988, .T. ) ;
#29738=CARTESIAN_POINT ( 'NONE',  ( 0.7032092222470416321, -79.47867041308421676, 1.062278989215700742 ) ) ;
#29741=CARTESIAN_POINT ( 'NONE',  ( 1.310679582531385501, -80.69166666666669130, 0.7554284705563518720 ) ) ;
#29751=CARTESIAN_POINT ( 'NONE',  ( -1.500000000000000000, -81.50000000000000000, 0.000000000000000000 ) ) ;
#29759=CARTESIAN_POINT ( 'NONE',  ( 1.199500263597271799, -78.69791666666667140, -0.9218200799623701425 ) ) ;
#29766=CARTESIAN_POINT ( 'NONE',  ( 0.9728932632037999850, -79.05095245453999553, 0.8910916192982000217 ) ) ;
#29789=CARTESIAN_POINT ( 'NONE',  ( -1.184185271002474060, -78.61999039302729386, 0.4726615109851249885 ) ) ;
#29812=CARTESIAN_POINT ( 'NONE',  ( -0.3926218265389255779, -79.89583333333337123, 1.460959015002472494 ) ) ;
#29822=CARTESIAN_POINT ( 'NONE',  ( -1.063776463958000074, -79.73983917928698872, 0.9372507776557998938 ) ) ;
#29825=CARTESIAN_POINT ( 'NONE',  ( 0.9976655664682999580, -78.41556959618471012, 1.007334501387000092 ) ) ;
#29847=CARTESIAN_POINT ( 'NONE',  ( 1.500000000000000000, -81.25000000000000000, 0.000000000000000000 ) ) ;
#29849=CARTESIAN_POINT ( 'NONE',  ( -0.1075386183112145844, -81.76848379990374838, -1.270412146854431379 ) ) ;
#29871=AXIS2_PLACEMENT_3D ( 'NONE', #28192, #10508, #14627 ) ;
#29875=EDGE_CURVE ( 'NONE', #38477, #5068, #43940, .T. ) ;
#29884=CARTESIAN_POINT ( 'NONE',  ( -1.460959015002473382, -78.02083333333337123, -0.3926218265389205819 ) ) ;
#29892=VECTOR ( 'NONE', #24626, 1000.000000000000000 ) ;
#29900=CARTESIAN_POINT ( 'NONE',  ( -0.3827951509036000011, -82.22793592742999635, -1.230253768017000038 ) ) ;
#29906=EDGE_CURVE ( 'NONE', #16765, #10750, #12261, .T. ) ;
#29917=ORIENTED_EDGE ( 'NONE', *, *, #35484, .F. ) ;
#29936=CARTESIAN_POINT ( 'NONE',  ( 1.199500263597268246, -78.80208333333334281, 0.9218200799623752495 ) ) ;
#29945=AXIS2_PLACEMENT_3D ( 'NONE', #667, #51118, #23645 ) ;
#29975=CARTESIAN_POINT ( 'NONE',  ( 1.021809889922000059, -79.41634891503500171, -0.8570204080543000202 ) ) ;
#29987=CARTESIAN_POINT ( 'NONE',  ( -1.127489577578000057, -80.67343018535999022, -0.5989559841152000130 ) ) ;
#29992=CONICAL_SURFACE ( 'NONE', #43261, 1.203124999988000043, 0.7853981633972997312 ) ;
#29997=DIRECTION ( 'NONE',  ( 0.000000000000000000, -1.000000000000000000, 0.000000000000000000 ) ) ;
#30005=CARTESIAN_POINT ( 'NONE',  ( 0.7680438806649999561, -80.32749471241899641, 1.420324776730000238 ) ) ;
#30008=CARTESIAN_POINT ( 'NONE',  ( 1.205681127563965394, -82.11979166666397134, 0.6958864542683118604 ) ) ;
#30014=ORIENTED_EDGE ( 'NONE', *, *, #23673, .F. ) ;
#30024=EDGE_CURVE ( 'NONE', #30255, #41507, #14354, .T. ) ;
#30025=EDGE_LOOP ( 'NONE', ( #58052, #2617, #18228 ) ) ;
#30026=CARTESIAN_POINT ( 'NONE',  ( 0.2017117102288683017, -79.28785263084954238, -1.258247021708098545 ) ) ;
#30056=CARTESIAN_POINT ( 'NONE',  ( -1.232249204661999942, -77.76678331097849650, 0.4974159524616000305 ) ) ;
#30094=DIRECTION ( 'NONE',  ( -1.000000000000000000, 0.000000000000000000, 0.000000000000000000 ) ) ;
#30108=CARTESIAN_POINT ( 'NONE',  ( 1.157603047269999852, -80.03175585522699009, 0.6328671228825999417 ) ) ;
#30112=CARTESIAN_POINT ( 'NONE',  ( 1.495190308928000089, -78.31058528507570315, 0.2516904690231000497 ) ) ;
#30113=CARTESIAN_POINT ( 'NONE',  ( -1.249999992656000147, -76.50000000027618796, 0.4999999997238000482 ) ) ;
#30137=CARTESIAN_POINT ( 'NONE',  ( 0.4184574958520561605, -81.49815860840411119, 1.203822021099241857 ) ) ;
#30150=CARTESIAN_POINT ( 'NONE',  ( -3.799999999999999822, -77.50000000000000000, 0.000000000000000000 ) ) ;
#30180=ORIENTED_EDGE ( 'NONE', *, *, #14756, .F. ) ;
#30218=CARTESIAN_POINT ( 'NONE',  ( -1.460959015002473382, -80.02083333333335702, -0.3926218265389205819 ) ) ;
#30255=VERTEX_POINT ( 'NONE', #11066 ) ;
#30275=CARTESIAN_POINT ( 'NONE',  ( -1.203848874799230195, -80.72378167735320176, 0.4182774650447538822 ) ) ;
#30279=CARTESIAN_POINT ( 'NONE',  ( 1.289124607492999841, -80.99250379629599195, 0.3416633729347999804 ) ) ;
#30297=CARTESIAN_POINT ( 'NONE',  ( 1.364204221418999774, -80.33325377676599999, 0.6617315995101000770 ) ) ;
#30299=CARTESIAN_POINT ( 'NONE',  ( 0.3502547437541005948, -82.15885416666446872, 1.306565524318783700 ) ) ;
#30339=CARTESIAN_POINT ( 'NONE',  ( 1.136236858042999787, -78.72094128391299250, 1.147248764840999913 ) ) ;
#30346=CARTESIAN_POINT ( 'NONE',  ( -1.281518013001000211, -77.76102424663160662, -0.3132342491214999969 ) ) ;
#30349=ORIENTED_EDGE ( 'NONE', *, *, #46328, .T. ) ;
#30391=DIRECTION ( 'NONE',  ( 0.000000000000000000, -1.000000000000000000, 0.000000000000000000 ) ) ;
#30400=CARTESIAN_POINT ( 'NONE',  ( -0.8999941789210000875, -80.86439197592500250, -1.015940422307999969 ) ) ;
#30404=CARTESIAN_POINT ( 'NONE',  ( 0.2372582530112999910, -78.40981053183779181, 1.497548220759000071 ) ) ;
#30406=CARTESIAN_POINT ( 'NONE',  ( -0.9820397338569999413, -80.70308451575900222, -0.7733679338621000099 ) ) ;
#30464=VERTEX_POINT ( 'NONE', #4213 ) ;
#30480=DIRECTION ( 'NONE',  ( 0.000000000000000000, 0.000000000000000000, -1.000000000000000000 ) ) ;
#30535=ORIENTED_EDGE ( 'NONE', *, *, #41461, .F. ) ;
#30547=ORIENTED_EDGE ( 'NONE', *, *, #50242, .F. ) ;
#30568=CARTESIAN_POINT ( 'NONE',  ( 1.245667655356138326, -79.48345497551839856, -0.2692737754160527408 ) ) ;
#30573=CARTESIAN_POINT ( 'NONE',  ( 1.246077061130999919, -80.94289117291501157, -0.4752592857455000264 ) ) ;
#30577=CARTESIAN_POINT ( 'NONE',  ( 0.5951337072741887946, -79.55689260744961189, -1.420922764992056386 ) ) ;
#30589=CARTESIAN_POINT ( 'NONE',  ( 0.3499829075702999837, -79.24753512672899092, -1.373881155581999858 ) ) ;
#30607=CARTESIAN_POINT ( 'NONE',  ( 0.3926156672727783015, -81.75433307437405972, 1.500698096577291363 ) ) ;
#30626=CARTESIAN_POINT ( 'NONE',  ( 1.178809752479577311, -80.96240752144423425, -0.6053965928639025718 ) ) ;
#30631=CARTESIAN_POINT ( 'NONE',  ( -1.521132372192000037, -77.89406422756130155, 0.2748539626865999508 ) ) ;
#30651=ORIENTED_EDGE ( 'NONE', *, *, #40072, .F. ) ;
#30655=CARTESIAN_POINT ( 'NONE',  ( -0.7554284705563483193, -78.48333333333333428, -1.310679582531387721 ) ) ;
#30661=ORIENTED_EDGE ( 'NONE', *, *, #22519, .F. ) ;
#30676=FACE_OUTER_BOUND ( 'NONE', #50980, .T. ) ;
#30679=VECTOR ( 'NONE', #16217, 1000.000000000000114 ) ;
#30686=CARTESIAN_POINT ( 'NONE',  ( -1.410851365044999861, -79.78945180266799753, 0.1398492253880000147 ) ) ;
#30724=ORIENTED_EDGE ( 'NONE', *, *, #55841, .T. ) ;
#30746=ORIENTED_EDGE ( 'NONE', *, *, #5812, .F. ) ;
#30799=EDGE_CURVE ( 'NONE', #44267, #33739, #4812, .T. ) ;
#30810=ORIENTED_EDGE ( 'NONE', *, *, #42658, .T. ) ;
#30816=ORIENTED_EDGE ( 'NONE', *, *, #6666, .F. ) ;
#30817=CARTESIAN_POINT ( 'NONE',  ( 0.2607165876585000319, -81.85403697029799730, 1.593499524613000151 ) ) ;
#30836=CARTESIAN_POINT ( 'NONE',  ( -0.2340539085346999837, -80.15469965994898871, 1.312933706406000267 ) ) ;
#30851=CARTESIAN_POINT ( 'NONE',  ( -0.3056428120159084827, -80.64427355544083298, 1.237341845012493557 ) ) ;
#30856=CARTESIAN_POINT ( 'NONE',  ( 1.304222966381000104, -81.48863003010599471, 0.2785293583740000023 ) ) ;
#30867=CARTESIAN_POINT ( 'NONE',  ( 0.7893528373467999515, -81.56550947952499087, 1.046299686877999902 ) ) ;
#30873=CARTESIAN_POINT ( 'NONE',  ( 0.2827145210274000231, -79.74366136053998844, -1.389291862697999980 ) ) ;
#30876=CARTESIAN_POINT ( 'NONE',  ( -0.7967926909478446618, -82.20442708333173698, 1.035424098837760098 ) ) ;
#30884=ORIENTED_EDGE ( 'NONE', *, *, #6448, .F. ) ;
#30893=CARTESIAN_POINT ( 'NONE',  ( 1.382657135218546385, -82.08072916571396149, -0.3707038244580741493 ) ) ;
#30895=CARTESIAN_POINT ( 'NONE',  ( -0.5175321235027776634, -80.24194154202476170, -1.165191863362585512 ) ) ;
#30910=CARTESIAN_POINT ( 'NONE',  ( 0.1738177897059751675, -81.38563030058524816, -1.313728265332345657 ) ) ;
#30915=CARTESIAN_POINT ( 'NONE',  ( 1.449215700157000075, -78.62171603714999435, -0.7120307440141999678 ) ) ;
#30921=CARTESIAN_POINT ( 'NONE',  ( 1.288803220532000138, -78.00908736353699169, 0.2820490268708999437 ) ) ;
#30937=CIRCLE ( 'NONE', #38515, 2.299999999999999822 ) ;
#30971=CARTESIAN_POINT ( 'NONE',  ( -1.499766830043999910, -80.34094972420699321, 0.2228039671692000068 ) ) ;
#30972=CARTESIAN_POINT ( 'NONE',  ( -1.242864761025999965, -77.64406422756130155, 0.2245736866142999943 ) ) ;
#30983=LINE ( 'NONE', #31275, #18730 ) ;
#30991=CARTESIAN_POINT ( 'NONE',  ( -0.1931105070826031334, -78.86330530744118050, -1.260507006898233806 ) ) ;
#31022=CARTESIAN_POINT ( 'NONE',  ( -1.460959015002473382, -81.02083333333331439, -0.3926218265389205819 ) ) ;
#31065=CARTESIAN_POINT ( 'NONE',  ( -0.4831833036036000117, -82.24511132376299827, -1.158768654956999988 ) ) ;
#31104=CARTESIAN_POINT ( 'NONE',  ( 0.1963495408493571015, -78.36458333333328596, 1.500000000000000444 ) ) ;
#31116=CARTESIAN_POINT ( 'NONE',  ( -0.9102058945833000347, -80.70043851714099503, 0.9747214924314999696 ) ) ;
#31123=EDGE_CURVE ( 'NONE', #18435, #30464, #10816, .T. ) ;
#31134=CARTESIAN_POINT ( 'NONE',  ( -1.274005267229903593, -80.24673294587803696, 0.05895105347379184929 ) ) ;
#31138=CARTESIAN_POINT ( 'NONE',  ( -0.5935892672256000147, -82.04604609890299116, 1.194249225580000129 ) ) ;
#31149=CARTESIAN_POINT ( 'NONE',  ( -0.9700586308955000403, -81.80063324571399619, -0.8813666596095000028 ) ) ;
#31157=CARTESIAN_POINT ( 'NONE',  ( -1.290198984414000050, -80.63668858139899953, -0.5875878301326999953 ) ) ;
#31179=CARTESIAN_POINT ( 'NONE',  ( -0.7340933969682582605, -79.57407930420207265, 1.041093327151733305 ) ) ;
#31197=CARTESIAN_POINT ( 'NONE',  ( 1.252145818528037857, -81.52670456029824209, 0.4338495457226560492 ) ) ;
#31208=CARTESIAN_POINT ( 'NONE',  ( 1.310679582531385279, -80.79166666666667140, 0.7554284705563519831 ) ) ;
#31211=CARTESIAN_POINT ( 'NONE',  ( 1.240545393080999981, -79.00709889550499554, -0.6863720704128000172 ) ) ;
#31219=CARTESIAN_POINT ( 'NONE',  ( -1.750000000000000000, -76.29999999999999716, 0.5000000000000000000 ) ) ;
#31223=CARTESIAN_POINT ( 'NONE',  ( 1.500000000000000000, -79.75000000000000000, 0.000000000000000000 ) ) ;
#31230=LINE ( 'NONE', #49271, #15818 ) ;
#31260=EDGE_LOOP ( 'NONE', ( #27272, #37339, #18802, #16333 ) ) ;
#31263=CARTESIAN_POINT ( 'NONE',  ( -1.527286180810999872, -79.42060648544099877, -0.2382966983378000114 ) ) ;
#31275=CARTESIAN_POINT ( 'NONE',  ( 1.249999996278000181, -76.50000000037098857, 0.4999999996289999915 ) ) ;
#31279=CARTESIAN_POINT ( 'NONE',  ( -1.384806900013862530, -80.53538967717265962, -0.6660020126448532585 ) ) ;
#31337=( NAMED_UNIT ( * ) SI_UNIT ( $, .STERADIAN. ) SOLID_ANGLE_UNIT ( ) );
#31338=CARTESIAN_POINT ( 'NONE',  ( 0.000000000000000000, -77.40000000000736691, -3.899999999992999733 ) ) ;
#31351=ORIENTED_EDGE ( 'NONE', *, *, #21756, .F. ) ;
#31367=DIRECTION ( 'NONE',  ( 0.000000000000000000, 1.000000000000000000, 0.000000000000000000 ) ) ;
#31370=AXIS2_PLACEMENT_3D ( 'NONE', #25498, #11079, #29059 ) ;
#31400=CARTESIAN_POINT ( 'NONE',  ( 0.7536588245869000335, -81.65558647677399051, -1.428009912074000187 ) ) ;
#31436=CARTESIAN_POINT ( 'NONE',  ( 1.500000000000000000, -79.75000000000000000, 0.000000000000000000 ) ) ;
#31437=CARTESIAN_POINT ( 'NONE',  ( 0.2017531936662588510, -79.38804522922356455, -1.258586820450570798 ) ) ;
#31442=CARTESIAN_POINT ( 'NONE',  ( 0.9432352957733999288, -81.99059486971999888, 0.9428059748164999698 ) ) ;
#31450=CARTESIAN_POINT ( 'NONE',  ( -0.3145193548456999832, -81.84765799895200189, -1.272359429009000120 ) ) ;
#31457=EDGE_CURVE ( 'NONE', #12549, #44267, #12708, .T. ) ;
#31459=CARTESIAN_POINT ( 'NONE',  ( 1.500000000000000000, -79.14999999999999147, 0.000000000000000000 ) ) ;
#31473=ORIENTED_EDGE ( 'NONE', *, *, #31457, .F. ) ;
#31494=CARTESIAN_POINT ( 'NONE',  ( -0.6826850050872016462, -80.83097677460143871, -1.092173985590070506 ) ) ;
#31510=CARTESIAN_POINT ( 'NONE',  ( 0.2218511837006999776, -78.65981053183800498, 1.400300479361000106 ) ) ;
#31516=CARTESIAN_POINT ( 'NONE',  ( 0.3926218265389220807, -81.64583333333334281, -1.460959015002473382 ) ) ;
#31524=EDGE_CURVE ( 'NONE', #56598, #13233, #20400, .T. ) ;
#31529=CARTESIAN_POINT ( 'NONE',  ( -1.199500263597270244, -81.45208333333334849, -0.9218200799623728070 ) ) ;
#31531=AXIS2_PLACEMENT_3D ( 'NONE', #35195, #3636, #12493 ) ;
#31556=ORIENTED_EDGE ( 'NONE', *, *, #56491, .T. ) ;
#31559=CARTESIAN_POINT ( 'NONE',  ( -1.034826241750000264, -80.78746333463699614, 1.108174957742000144 ) ) ;
#31570=DIRECTION ( 'NONE',  ( 0.000000000000000000, -1.000000000000000000, 0.000000000000000000 ) ) ;
#31604=CARTESIAN_POINT ( 'NONE',  ( -1.187238164339999846, -80.68061120219299198, -0.3457930548265999993 ) ) ;
#31609=CARTESIAN_POINT ( 'NONE',  ( -1.500000000000000000, -81.00000000000000000, 0.000000000000000000 ) ) ;
#31621=ORIENTED_EDGE ( 'NONE', *, *, #27360, .F. ) ;
#31624=B_SPLINE_CURVE_WITH_KNOTS ( 'NONE', 3,
 ( #2450, #6576, #20739, #38737 ),
 .UNSPECIFIED., .F., .F.,
 ( 4, 4 ),
 ( 0.000000000000000000, 1.000000000000000000 ),
 .UNSPECIFIED. ) ;
#31645=ORIENTED_EDGE ( 'NONE', *, *, #53837, .T. ) ;
#31651=DIRECTION ( 'NONE',  ( 0.000000000000000000, 0.000000000000000000, -1.000000000000000000 ) ) ;
#31673=VECTOR ( 'NONE', #57610, 1000.000000000000000 ) ;
#31674=ADVANCED_FACE ( 'NONE', ( #30676 ), #40432, .T. ) ;
#31684=CARTESIAN_POINT ( 'NONE',  ( 1.088575500396492979, -77.85671926408777210, -0.6620644299734026461 ) ) ;
#31692=CARTESIAN_POINT ( 'NONE',  ( 1.416683027186000254, -80.76831832026100244, -0.5403291534934999696 ) ) ;
#31693=B_SPLINE_CURVE_WITH_KNOTS ( 'NONE', 3,
 ( #15671, #33669, #51707, #37518, #1826, #45019, #55536, #5645, #41667, #31702, #19235, #19822, #37227, #55243, #15085, #32785, #23942, #37813 ),
 .UNSPECIFIED., .F., .F.,
 ( 4, 2, 2, 2, 2, 2, 2, 2, 4 ),
 ( 0.000000000000000000, 0.1249999999999999722, 0.2499999999999999445, 0.3749999999999998890, 0.4999999999999998890, 0.6249999999999998890, 0.7499999999999997780, 0.8749999999999998890, 1.000000000000000000 ),
 .UNSPECIFIED. ) ;
#31702=CARTESIAN_POINT ( 'NONE',  ( -0.1963495408493673156, -80.28541666666667709, 1.499999999999999556 ) ) ;
#31705=VERTEX_POINT ( 'NONE', #37456 ) ;
#31709=CARTESIAN_POINT ( 'NONE',  ( 1.199918086393000127, -80.55160064699700229, 0.5820416783086000967 ) ) ;
#31721=AXIS2_PLACEMENT_3D ( 'NONE', #27350, #45386, #14352 ) ;
#31726=CARTESIAN_POINT ( 'NONE',  ( 1.196963559360000096, -78.43554551434779398, -0.5880938590690999446 ) ) ;
#31734=CARTESIAN_POINT ( 'NONE',  ( -1.297058042903999953, -81.28434093078000444, -0.3101879797029999941 ) ) ;
#31745=CARTESIAN_POINT ( 'NONE',  ( 0.07798313963709001262, -81.66790592049099473, 1.406311399563000109 ) ) ;
#31768=ORIENTED_EDGE ( 'NONE', *, *, #21568, .T. ) ;
#31776=CARTESIAN_POINT ( 'NONE',  ( -0.2692648470245010972, -80.25784302387772584, -1.245099868093910933 ) ) ;
#31808=AXIS2_PLACEMENT_3D ( 'NONE', #17381, #17979, #44539 ) ;
#31809=CARTESIAN_POINT ( 'NONE',  ( -0.1963495408493673156, -79.78541666666667709, 1.499999999999999556 ) ) ;
#31810=CARTESIAN_POINT ( 'NONE',  ( -1.335620631414000004, -77.78332085210550417, 0.2413337786383999983 ) ) ;
#31812=EDGE_LOOP ( 'NONE', ( #2467, #26238, #44426, #3226 ) ) ;
#31830=CARTESIAN_POINT ( 'NONE',  ( -0.8668440880359000733, -77.70303337523669995, -1.013523202003999923 ) ) ;
#31832=FACE_OUTER_BOUND ( 'NONE', #54526, .T. ) ;
#31841=CIRCLE ( 'NONE', #29945, 4.000000000000000000 ) ;
#31859=CARTESIAN_POINT ( 'NONE',  ( -0.2660992726780999629, -80.24172447744500403, 1.492693313845999903 ) ) ;
#31860=CARTESIAN_POINT ( 'NONE',  ( 1.288803220532000138, -77.92520242672080144, 0.2820490268708999437 ) ) ;
#31883=ORIENTED_EDGE ( 'NONE', *, *, #49680, .F. ) ;
#31897=CARTESIAN_POINT ( 'NONE',  ( 0.08545339522192001158, -81.02789956585999676, 1.316534626873000047 ) ) ;
#31904=CARTESIAN_POINT ( 'NONE',  ( 0.1963495408493638184, -81.13541666666668561, -1.499999999999999778 ) ) ;
#32001=CARTESIAN_POINT ( 'NONE',  ( -4.000000000000000000, -77.29999999999999716, 0.000000000000000000 ) ) ;
#32003=CYLINDRICAL_SURFACE ( 'NONE', #11068, 1.500000000000000000 ) ;
#32004=CARTESIAN_POINT ( 'NONE',  ( -1.248430190247999949, -79.26167243909000604, 0.06262635289305999720 ) ) ;
#32018=CIRCLE ( 'NONE', #29197, 2.000000000000000000 ) ;
#32019=CARTESIAN_POINT ( 'NONE',  ( -1.256362333281000110, -77.70789370475868907, 0.2270125678640999844 ) ) ;
#32034=ORIENTED_EDGE ( 'NONE', *, *, #16089, .F. ) ;
#32037=CARTESIAN_POINT ( 'NONE',  ( -0.6245130753102998700, -81.38575740106399792, -1.262448629235000119 ) ) ;
#32047=CARTESIAN_POINT ( 'NONE',  ( -1.199500263597270244, -78.95208333333333428, -0.9218200799623728070 ) ) ;
#32054=VERTEX_POINT ( 'NONE', #57780 ) ;
#32065=B_SPLINE_CURVE_WITH_KNOTS ( 'NONE', 3,
 ( #15677, #29242, #10977, #7682, #33674, #7393, #15967, #29812, #48151, #51711, #12115, #47289, #43136, #42551, #28956, #39262, #6817, #25683 ),
 .UNSPECIFIED., .F., .F.,
 ( 4, 2, 2, 2, 2, 2, 2, 2, 4 ),
 ( 0.000000000000000000, 0.1250000000000000833, 0.2500000000000001665, 0.3750000000000001665, 0.5000000000000002220, 0.6250000000000002220, 0.7500000000000001110, 0.8750000000000001110, 1.000000000000000000 ),
 .UNSPECIFIED. ) ;
#32069=CARTESIAN_POINT ( 'NONE',  ( -0.6379005857648086808, -79.73309412273128771, -1.103986640637640848 ) ) ;
#32082=CARTESIAN_POINT ( 'NONE',  ( -1.319155384867000125, -80.12260285397499615, 0.1959724986398999891 ) ) ;
#32103=CARTESIAN_POINT ( 'NONE',  ( 0.6064284284549000814, -78.95748627212400095, -1.281524057860000010 ) ) ;
#32120=DIRECTION ( 'NONE',  ( 0.000000000000000000, 0.000000000000000000, 1.000000000000000000 ) ) ;
#32121=CARTESIAN_POINT ( 'NONE',  ( 0.8912423865758999364, -77.95109649214209924, 0.9921004264782997684 ) ) ;
#32150=CARTESIAN_POINT ( 'NONE',  ( 0.3985939703966000502, -79.55290681445698908, -1.564707112294000169 ) ) ;
#32160=ORIENTED_EDGE ( 'NONE', *, *, #29906, .F. ) ;
#32171=ORIENTED_EDGE ( 'NONE', *, *, #45223, .F. ) ;
#32192=CARTESIAN_POINT ( 'NONE',  ( -0.9218200799623716968, -81.07291666666667140, -1.199500263597270910 ) ) ;
#32217=CARTESIAN_POINT ( 'NONE',  ( -8.022734517049746273E-06, -82.01564364893640402, -1.484164386985079798 ) ) ;
#32250=CARTESIAN_POINT ( 'NONE',  ( -1.249999996278000181, -76.50000000037098857, -0.4999999996289999915 ) ) ;
#32254=CARTESIAN_POINT ( 'NONE',  ( 0.7554284705563509839, -79.66666666666668561, -1.310679582531385945 ) ) ;
#32274=CARTESIAN_POINT ( 'NONE',  ( -0.1262356271553999876, -81.22059099503800894, -1.412134535654999912 ) ) ;
#32290=CARTESIAN_POINT ( 'NONE',  ( -1.181111693982000110, -79.27654225787900089, -0.4092372983238000139 ) ) ;
#32302=CARTESIAN_POINT ( 'NONE',  ( -1.295435361468000091, -77.78474280459130341, -0.3166359884281000348 ) ) ;
#32324=CARTESIAN_POINT ( 'NONE',  ( -0.7112551523747999704, -81.49650077651999425, -1.437797105698000122 ) ) ;
#32331=CARTESIAN_POINT ( 'NONE',  ( -0.3926218265389255779, -81.39583333333337123, 1.460959015002472494 ) ) ;
#32334=CARTESIAN_POINT ( 'NONE',  ( 1.310679582531388387, -79.10833333333333428, -0.7554284705563470981 ) ) ;
#32335=EDGE_LOOP ( 'NONE', ( #55646, #15306, #12759 ) ) ;
#32341=VERTEX_POINT ( 'NONE', #20270 ) ;
#32355=ORIENTED_EDGE ( 'NONE', *, *, #2068, .T. ) ;
#32369=CARTESIAN_POINT ( 'NONE',  ( -0.6056189234361001317, -80.22182810073799430, -1.188192690176999911 ) ) ;
#32377=CARTESIAN_POINT ( 'NONE',  ( -1.196500474958131388, -81.71480357325025068, 0.5696325066958111139 ) ) ;
#32388=CARTESIAN_POINT ( 'NONE',  ( -0.3926218265389256890, -79.79583333333334849, 1.460959015002472050 ) ) ;
#32389=CARTESIAN_POINT ( 'NONE',  ( 0.2372582530112999910, -78.71518221956600314, 1.497548220759000071 ) ) ;
#32396=CARTESIAN_POINT ( 'NONE',  ( 0.7554284705563509839, -81.66666666666669983, -1.310679582531385945 ) ) ;
#32451=CARTESIAN_POINT ( 'NONE',  ( -1.500000000000000000, -80.00000000000000000, 0.000000000000000000 ) ) ;
#32475=B_SPLINE_CURVE_WITH_KNOTS ( 'NONE', 3,
 ( #432, #17015, #12012, #40546, #57454, #30577, #3438, #16730, #27241, #4828 ),
 .UNSPECIFIED., .F., .F.,
 ( 4, 2, 2, 2, 4 ),
 ( 0.000000000000000000, 0.2500000000000000000, 0.5000000000000000000, 0.7500000000000000000, 1.000000000000000000 ),
 .UNSPECIFIED. ) ;
#32498=VECTOR ( 'NONE', #2668, 1000.000000000000000 ) ;
#32506=CARTESIAN_POINT ( 'NONE',  ( -0.1356420093736999954, -77.61024949339380896, -1.608970710047999964 ) ) ;
#32523=DIRECTION ( 'NONE',  ( 0.000000000000000000, 1.000000000000000000, 0.000000000000000000 ) ) ;
#32556=ORIENTED_EDGE ( 'NONE', *, *, #28146, .F. ) ;
#32563=CARTESIAN_POINT ( 'NONE',  ( -1.403112730325000168, -81.01638143716699858, 0.5746449548680000463 ) ) ;
#32579=CARTESIAN_POINT ( 'NONE',  ( -1.500000000000000000, -79.50000000000000000, 0.000000000000000000 ) ) ;
#32587=VECTOR ( 'NONE', #32599, 1000.000000000000000 ) ;
#32597=CARTESIAN_POINT ( 'NONE',  ( -1.210921577777000158, -78.18748239744249418, 0.5587889421650999999 ) ) ;
#32599=DIRECTION ( 'NONE',  ( 0.000000000000000000, 1.000000000000000000, 0.000000000000000000 ) ) ;
#32613=CARTESIAN_POINT ( 'NONE',  ( -1.467516833711000057, -82.33459940031100643, 0.3393247902666000071 ) ) ;
#32620=CARTESIAN_POINT ( 'NONE',  ( 0.9683804214594998738, -79.84864567164899540, -0.8959938446301999315 ) ) ;
#32635=ORIENTED_EDGE ( 'NONE', *, *, #26596, .T. ) ;
#32672=DIRECTION ( 'NONE',  ( 1.000000000000000000, 0.000000000000000000, 0.000000000000000000 ) ) ;
#32708=SHAPE_REPRESENTATION_RELATIONSHIP ( 'NONE' , 'NONE' ,  #4074, #463 ) ;
#32726=CARTESIAN_POINT ( 'NONE',  ( -0.7520647764090000464, -80.99167289250799229, -1.313341758254999991 ) ) ;
#32738=B_SPLINE_CURVE_WITH_KNOTS ( 'NONE', 3,
 ( #2623, #47221, #57203, #12333, #16196, #51928, #16771, #34752, #34173, #33887, #6753, #11765, #52779, #7326, #24760, #42775, #11487, #47794 ),
 .UNSPECIFIED., .F., .F.,
 ( 4, 2, 2, 2, 2, 2, 2, 2, 4 ),
 ( 0.000000000000000000, 0.1249999999999999722, 0.2499999999999999445, 0.3749999999999998890, 0.4999999999999998890, 0.6249999999999998890, 0.7499999999999997780, 0.8749999999999998890, 1.000000000000000000 ),
 .UNSPECIFIED. ) ;
#32768=CARTESIAN_POINT ( 'NONE',  ( -1.195105308512000031, -81.62325104643299767, 0.5588281594584000311 ) ) ;
#32785=CARTESIAN_POINT ( 'NONE',  ( -1.460959015002474493, -80.37916666666664867, 0.3926218265389144757 ) ) ;
#32794=CARTESIAN_POINT ( 'NONE',  ( 1.125436458607999901, -79.53562962141599257, 0.6884462015638999066 ) ) ;
#32796=CARTESIAN_POINT ( 'NONE',  ( -0.2914033309752999679, -78.60250196101499398, -1.588174433604999880 ) ) ;
#32816=VECTOR ( 'NONE', #25720, 1000.000000000000000 ) ;
#32836=CARTESIAN_POINT ( 'NONE',  ( -1.460959015002474937, -80.47916666666665719, 0.3926218265389144757 ) ) ;
#32854=CARTESIAN_POINT ( 'NONE',  ( 1.298531763578000264, -81.31981624179999812, -0.5690998499286999968 ) ) ;
#32858=CARTESIAN_POINT ( 'NONE',  ( 0.1963495408493571015, -81.86458333333975190, 1.500000000000000444 ) ) ;
#32861=PRODUCT_CONTEXT ( 'NONE', #39066, 'mechanical' ) ;
#32871=CARTESIAN_POINT ( 'NONE',  ( 0.9218200799623694763, -79.32291666666667140, 1.199500263597272465 ) ) ;
#32889=CARTESIAN_POINT ( 'NONE',  ( -1.112801787005999854, -79.21864855312099962, -0.6258220204580999813 ) ) ;
#32907=CARTESIAN_POINT ( 'NONE',  ( 1.505061616724999940, -82.09947563412200111, -0.06074805737713000198 ) ) ;
#32912=CARTESIAN_POINT ( 'NONE',  ( 0.3926218265389159745, -80.75416666666666288, 1.460959015002474493 ) ) ;
#32913=CARTESIAN_POINT ( 'NONE',  ( -1.141857967141000074, -79.69980780150500266, -0.6608524743567000259 ) ) ;
#32930=VERTEX_POINT ( 'NONE', #44343 ) ;
#32953=CARTESIAN_POINT ( 'NONE',  ( -0.2976639488673999967, -79.52725137340199524, 1.299989344602000108 ) ) ;
#32993=CARTESIAN_POINT ( 'NONE',  ( -1.320128238786999919, -78.64567321947700407, -0.1893081677438999966 ) ) ;
#33009=ORIENTED_EDGE ( 'NONE', *, *, #48848, .T. ) ;
#33022=CARTESIAN_POINT ( 'NONE',  ( -1.469401861277999988, -80.94206026912699770, -0.6692011555514000287 ) ) ;
#33078=ORIENTED_EDGE ( 'NONE', *, *, #25555, .F. ) ;
#33095=CARTESIAN_POINT ( 'NONE',  ( -0.7259747304966001069, -78.40405146749098719, 1.442281046339000117 ) ) ;
#33112=VECTOR ( 'NONE', #34305, 1000.000000000000000 ) ;
#33122=CARTESIAN_POINT ( 'NONE',  ( -0.2317941695893000198, -82.33204462758500597, -1.228320586388000013 ) ) ;
#33151=CARTESIAN_POINT ( 'NONE',  ( 1.465624405047999845, -80.81793094364199703, 0.3884420286245000575 ) ) ;
#33200=CARTESIAN_POINT ( 'NONE',  ( -1.600123231380999878, -81.40245127004399706, 0.1129161299330000007 ) ) ;
#33207=CARTESIAN_POINT ( 'NONE',  ( 1.500000000000000000, -81.26041666666668561, 0.1963495408493652339 ) ) ;
#33210=AXIS2_PLACEMENT_3D ( 'NONE', #3809, #4400, #17096 ) ;
#33218=ORIENTED_EDGE ( 'NONE', *, *, #33569, .F. ) ;
#33256=CARTESIAN_POINT ( 'NONE',  ( 0.000000000000000000, -75.67500000000001137, 0.000000000000000000 ) ) ;
#33262=CARTESIAN_POINT ( 'NONE',  ( -1.297058042903999953, -81.15301887804400849, -0.3101879797029999941 ) ) ;
#33264=CARTESIAN_POINT ( 'NONE',  ( 1.500000000000001110, -80.63958333333333428, -0.1963495408493590721 ) ) ;
#33282=CARTESIAN_POINT ( 'NONE',  ( -1.211530263941000163, -79.43446749155899056, 1.067430724879000037 ) ) ;
#33288=CARTESIAN_POINT ( 'NONE',  ( 0.5704417986824000808, -78.79451108962000205, -1.205475954488999912 ) ) ;
#33364=CARTESIAN_POINT ( 'NONE',  ( -1.127487306198333927, -78.11114297373420357, 0.5952175666624754946 ) ) ;
#33392=CARTESIAN_POINT ( 'NONE',  ( 1.079065815471999867, -77.80869998691809997, 1.201179019145000026 ) ) ;
#33409=CARTESIAN_POINT ( 'NONE',  ( -0.9112835142866211324, -78.68838743923397772, 0.8908661252871045155 ) ) ;
#33419=CARTESIAN_POINT ( 'NONE',  ( -0.8218343019581000330, -80.83782732035000151, -1.050237832603999832 ) ) ;
#33432=CARTESIAN_POINT ( 'NONE',  ( 1.199500263597271799, -79.69791666666667140, -0.9218200799623701425 ) ) ;
#33449=CARTESIAN_POINT ( 'NONE',  ( -1.198617868132000108, -80.64177705559200149, -0.6367414467165999348 ) ) ;
#33456=CARTESIAN_POINT ( 'NONE',  ( 0.7554284705563509839, -78.16666666666668561, -1.310679582531385945 ) ) ;
#33465=FILL_AREA_STYLE_COLOUR ( '', #8309 ) ;
#33502=CARTESIAN_POINT ( 'NONE',  ( -1.391687965710999952, -81.44947602328198855, -0.7977148706058000416 ) ) ;
#33544=CARTESIAN_POINT ( 'NONE',  ( -1.261445002938999860, -79.19066194505900569, -0.1968185027220000216 ) ) ;
#33559=CARTESIAN_POINT ( 'NONE',  ( 1.460959015002474493, -80.62916666666664867, -0.3926218265389176953 ) ) ;
#33560=DIRECTION ( 'NONE',  ( 0.000000000000000000, -1.000000000000000000, 0.000000000000000000 ) ) ;
#33569=EDGE_CURVE ( 'NONE', #14133, #52412, #22050, .T. ) ;
#33577=CARTESIAN_POINT ( 'NONE',  ( -1.102025757167999886, -80.42671995918099981, 1.180137589876000037 ) ) ;
#33580=DIRECTION ( 'NONE',  ( 0.000000000000000000, 1.000000000000000000, 0.000000000000000000 ) ) ;
#33584=CARTESIAN_POINT ( 'NONE',  ( 1.224162466603000210, -77.89564526295849589, -0.5291525010897000225 ) ) ;
#33612=CARTESIAN_POINT ( 'NONE',  ( 0.7680438806649999561, -80.74360977560299091, 1.420324776730000238 ) ) ;
#33626=CIRCLE ( 'NONE', #31721, 2.299999999999999822 ) ;
#33627=CARTESIAN_POINT ( 'NONE',  ( 0.1963495408493638184, -78.63541666666668561, -1.499999999999999778 ) ) ;
#33652=CARTESIAN_POINT ( 'NONE',  ( 0.8118302357295669180, -78.96982299379136805, 0.9819661897715911136 ) ) ;
#33668=ADVANCED_FACE ( 'NONE', ( #43283 ), #3415, .F. ) ;
#33669=CARTESIAN_POINT ( 'NONE',  ( 1.499999999999999778, -80.16041666666669130, 0.1963495408493654004 ) ) ;
#33674=CARTESIAN_POINT ( 'NONE',  ( -1.199500263597274685, -79.94791666666668561, 0.9218200799623673669 ) ) ;
#33682=UNCERTAINTY_MEASURE_WITH_UNIT (LENGTH_MEASURE( 1.000000000000000082E-05 ), #11401, 'distance_accuracy_value', 'NONE');
#33683=CARTESIAN_POINT ( 'NONE',  ( -0.6374375075192000306, -78.51479484294699773, 1.266385724874999896 ) ) ;
#33699=CARTESIAN_POINT ( 'NONE',  ( 1.073843316271627879, -78.54527281979174802, 0.6870350484321460227 ) ) ;
#33706=CARTESIAN_POINT ( 'NONE',  ( -1.068511653377071102, -81.19603045319907153, -0.6936404097926303081 ) ) ;
#33739=VERTEX_POINT ( 'NONE', #47729 ) ;
#33741=VERTEX_POINT ( 'NONE', #35859 ) ;
#33767=DIRECTION ( 'NONE',  ( -1.000000000000000000, 0.000000000000000000, 0.000000000000000000 ) ) ;
#33794=CARTESIAN_POINT ( 'NONE',  ( 1.199500263597268246, -81.30208333333334281, 0.9218200799623752495 ) ) ;
#33800=LINE ( 'NONE', #1096, #5757 ) ;
#33808=ADVANCED_FACE ( 'NONE', ( #46133 ), #7916, .F. ) ;
#33830=CARTESIAN_POINT ( 'NONE',  ( 1.021809889922000059, -79.37257489745699957, -0.8570204080543000202 ) ) ;
#33843=CARTESIAN_POINT ( 'NONE',  ( 0.9432352957733999288, -81.94682085214100198, 0.9428059748164999698 ) ) ;
#33859=CARTESIAN_POINT ( 'NONE',  ( 0.000000000000000000, -75.67500000000001137, 0.000000000000000000 ) ) ;
#33865=CARTESIAN_POINT ( 'NONE',  ( 0.1443438050804999873, -78.00070911552320752, 1.325798245762999983 ) ) ;
#33884=CARTESIAN_POINT ( 'NONE',  ( -0.2976406553997369420, -79.25604966714371358, -1.238856423539541840 ) ) ;
#33887=CARTESIAN_POINT ( 'NONE',  ( -0.1963495408493673156, -81.28541666666667709, 1.499999999999999556 ) ) ;
#33897=DIRECTION ( 'NONE',  ( 0.000000000000000000, 1.000000000000000000, 1.740029764579000277E-14 ) ) ;
#33908=CARTESIAN_POINT ( 'NONE',  ( 0.9218200799623742503, -78.67708333333332860, -1.199500263597268912 ) ) ;
#33933=CARTESIAN_POINT ( 'NONE',  ( -1.499934128473817241, -81.90004407876089942, 2.109063419893342596E-06 ) ) ;
#33934=CARTESIAN_POINT ( 'NONE',  ( -0.1812720377017000006, -81.77208891657700462, -1.306792278262000062 ) ) ;
#33945=ORIENTED_EDGE ( 'NONE', *, *, #51117, .T. ) ;
#33962=ORIENTED_EDGE ( 'NONE', *, *, #280, .F. ) ;
#33969=CARTESIAN_POINT ( 'NONE',  ( -0.2558648464975999959, -78.71324533647100452, -1.394486488214999875 ) ) ;
#33979=ORIENTED_EDGE ( 'NONE', *, *, #39957, .F. ) ;
#33992=DIRECTION ( 'NONE',  ( 1.000000000000000000, 0.000000000000000000, 0.000000000000000000 ) ) ;
#33993=CARTESIAN_POINT ( 'NONE',  ( 1.256367437124104258, -81.38684823543385960, -0.2130951737473960883 ) ) ;
#34021=EDGE_LOOP ( 'NONE', ( #30746, #29674, #18727, #50544 ) ) ;
#34051=CARTESIAN_POINT ( 'NONE',  ( 0.1963495408493571848, -78.76458333333334849, 1.500000000000000666 ) ) ;
#34056=CARTESIAN_POINT ( 'NONE',  ( -0.3713770062794000126, -82.23533397128800004, -1.193557338046999927 ) ) ;
#34068=CARTESIAN_POINT ( 'NONE',  ( -1.500000000000000222, -80.01041666666669983, -0.1963495408493622085 ) ) ;
#34126=FACE_OUTER_BOUND ( 'NONE', #48602, .T. ) ;
#34135=EDGE_CURVE ( 'NONE', #43690, #54597, #2368, .T. ) ;
#34145=CARTESIAN_POINT ( 'NONE',  ( 0.2446082660763000405, -80.12904421889498963, -1.596051606003999979 ) ) ;
#34173=CARTESIAN_POINT ( 'NONE',  ( 0.1963495408493571848, -81.26458333333333428, 1.500000000000000666 ) ) ;
#34183=LINE ( 'NONE', #29751, #7573 ) ;
#34185=CARTESIAN_POINT ( 'NONE',  ( -1.500000000000000000, -81.00000000000000000, 0.000000000000000000 ) ) ;
#34223=CARTESIAN_POINT ( 'NONE',  ( 0.01019144981830593689, -78.52458150190987851, 1.274912689113979924 ) ) ;
#34250=CARTESIAN_POINT ( 'NONE',  ( 0.2827145210274000231, -79.93828967281199027, -1.389291862697999980 ) ) ;
#34251=DIRECTION ( 'NONE',  ( 0.000000000000000000, -1.000000000000000000, 0.000000000000000000 ) ) ;
#34254=CARTESIAN_POINT ( 'NONE',  ( -0.5750548074078000171, -79.01092107675799525, 1.295897153995000162 ) ) ;
#34273=CARTESIAN_POINT ( 'NONE',  ( -1.263074648639895603, -79.26084591700393389, -0.1732096211842467925 ) ) ;
#34280=CARTESIAN_POINT ( 'NONE',  ( -0.6937200964320594521, -82.07061195510875962, 1.068798584389240691 ) ) ;
#34284=CARTESIAN_POINT ( 'NONE',  ( -0.9816856958575284064, -80.73641784909243313, -0.7730884388065356605 ) ) ;
#34305=DIRECTION ( 'NONE',  ( -2.250403632142151042E-08, -0.7071067811865473507, -0.7071067811865473507 ) ) ;
#34318=CARTESIAN_POINT ( 'NONE',  ( -0.3926218265389190276, -78.10416666666667140, -1.460959015002473826 ) ) ;
#34350=DIRECTION ( 'NONE',  ( -0.3090169943750110115, 0.000000000000000000, -0.9510565162951328810 ) ) ;
#34351=CARTESIAN_POINT ( 'NONE',  ( -1.250000000000000000, -77.64999999999999147, 0.000000000000000000 ) ) ;
#34371=CARTESIAN_POINT ( 'NONE',  ( 1.500000000000000000, -78.75000000000000000, 0.000000000000000000 ) ) ;
#34376=ORIENTED_EDGE ( 'NONE', *, *, #17899, .F. ) ;
#34384=VERTEX_POINT ( 'NONE', #1780 ) ;
#34421=CARTESIAN_POINT ( 'NONE',  ( -0.9218200799623716968, -77.57291666666667140, -1.199500263597270910 ) ) ;
#34422=CARTESIAN_POINT ( 'NONE',  ( 1.500000000000000000, -80.65000000000000568, 0.000000000000000000 ) ) ;
#34437=CARTESIAN_POINT ( 'NONE',  ( -1.435212230719999926, -80.02981897213200568, -0.7398511866349000154 ) ) ;
#34441=ORIENTED_EDGE ( 'NONE', *, *, #25087, .T. ) ;
#34450=EDGE_CURVE ( 'NONE', #51480, #56774, #35343, .T. ) ;
#34488=CARTESIAN_POINT ( 'NONE',  ( 0.2696047275149000555, -79.10056507792100433, 1.291465103089999955 ) ) ;
#34497=CARTESIAN_POINT ( 'NONE',  ( -0.6747260877994001316, -82.25000000000000000, -1.052256958371999840 ) ) ;
#34509=CARTESIAN_POINT ( 'NONE',  ( -1.140137907013035523, -79.11293633046733476, 0.5694093068792435153 ) ) ;
#34532=DIRECTION ( 'NONE',  ( 0.000000000000000000, -1.000000000000000000, 0.000000000000000000 ) ) ;
#34533=VECTOR ( 'NONE', #9315, 1000.000000000000000 ) ;
#34539=CARTESIAN_POINT ( 'NONE',  ( 0.5703284788033999853, -80.08136847860799890, 1.189660050829999927 ) ) ;
#34542=CARTESIAN_POINT ( 'NONE',  ( 0.7281259072094999896, -77.77060549223068620, -1.216509659635999885 ) ) ;
#34546=EDGE_CURVE ( 'NONE', #43155, #4192, #38170, .T. ) ;
#34568=CARTESIAN_POINT ( 'NONE',  ( 0.2886757222754123275, -82.00700602769721570, 1.241303401317177979 ) ) ;
#34571=CARTESIAN_POINT ( 'NONE',  ( 0.3926218265389159745, -79.25416666666666288, 1.460959015002474493 ) ) ;
#34587=VECTOR ( 'NONE', #50162, 1000.000000000000000 ) ;
#34588=VECTOR ( 'NONE', #56971, 1000.000000000000000 ) ;
#34608=EDGE_CURVE ( 'NONE', #43155, #16765, #52958, .T. ) ;
#34633=CIRCLE ( 'NONE', #31808, 3.799999999999999822 ) ;
#34651=DIRECTION ( 'NONE',  ( 0.000000000000000000, -1.000000000000000000, 0.000000000000000000 ) ) ;
#34696=CARTESIAN_POINT ( 'NONE',  ( -0.5470841013496000604, -79.76947588450499893, -1.216254552179000026 ) ) ;
#34707=CARTESIAN_POINT ( 'NONE',  ( -0.8218343019581000330, -80.79405330277099040, -1.050237832603999832 ) ) ;
#34723=CARTESIAN_POINT ( 'NONE',  ( 0.7212099693301999848, -80.38286640014699458, 1.333715969168000059 ) ) ;
#34724=VERTEX_POINT ( 'NONE', #50577 ) ;
#34727=CARTESIAN_POINT ( 'NONE',  ( 0.8355970340055913770, -82.13932291666422714, 1.088690951272730523 ) ) ;
#34743=ORIENTED_EDGE ( 'NONE', *, *, #7202, .T. ) ;
#34752=CARTESIAN_POINT ( 'NONE',  ( 0.3926218265389159745, -81.25416666666667709, 1.460959015002474493 ) ) ;
#34772=CARTESIAN_POINT ( 'NONE',  ( 1.577356090230000119, -78.17520242672080144, 0.3451975780249000314 ) ) ;
#34777=AXIS2_PLACEMENT_3D ( 'NONE', #57090, #38505, #16657 ) ;
#34809=VERTEX_POINT ( 'NONE', #13521 ) ;
#34828=CARTESIAN_POINT ( 'NONE',  ( -1.390602365772999782, -80.78170427028999256, 0.2763432473779000587 ) ) ;
#34829=CARTESIAN_POINT ( 'NONE',  ( -0.9728543758959999899, -78.16750647927929663, -1.031316509929999903 ) ) ;
#34899=PRESENTATION_STYLE_ASSIGNMENT (( #35475 ) ) ;
#34937=VECTOR ( 'NONE', #22329, 1000.000000000000000 ) ;
#34986=FACE_OUTER_BOUND ( 'NONE', #13056, .T. ) ;
#34989=CARTESIAN_POINT ( 'NONE',  ( -0.04771467012325169427, -80.62837193105833933, 1.273752274804522244 ) ) ;
#34993=CARTESIAN_POINT ( 'NONE',  ( -1.321095329625999959, -82.18904536324399146, -0.1826337427822999904 ) ) ;
#35000=VERTEX_POINT ( 'NONE', #40916 ) ;
#35010=CARTESIAN_POINT ( 'NONE',  ( -1.347695613438000040, -80.08519065986000385, -0.6947364142266000409 ) ) ;
#35024=CYLINDRICAL_SURFACE ( 'NONE', #21035, 0.5000000000000000000 ) ;
#35044=DIRECTION ( 'NONE',  ( -1.000000000000000000, 0.000000000000000000, 0.000000000000000000 ) ) ;
#35047=DIRECTION ( 'NONE',  ( 0.000000000000000000, 0.000000000000000000, -1.000000000000000000 ) ) ;
#35050=CARTESIAN_POINT ( 'NONE',  ( -1.347317391812999920, -79.44859309350199794, -0.7577098654840999092 ) ) ;
#35057=CARTESIAN_POINT ( 'NONE',  ( 1.154392285689999742, -78.95172720777699737, -0.6387050628028000387 ) ) ;
#35078=AXIS2_PLACEMENT_3D ( 'NONE', #24839, #38988, #43724 ) ;
#35086=CIRCLE ( 'NONE', #33210, 1.000000000000000000 ) ;
#35109=CARTESIAN_POINT ( 'NONE',  ( -1.327188084842999993, -79.29332556885799477, 0.06657717027841000834 ) ) ;
#35113=CARTESIAN_POINT ( 'NONE',  ( -1.146672249030999957, -77.62752668643429388, 0.4628715253012000153 ) ) ;
#35118=DIRECTION ( 'NONE',  ( 1.000000000000000000, 0.000000000000000000, 0.000000000000000000 ) ) ;
#35142=CARTESIAN_POINT ( 'NONE',  ( 1.310679582531385501, -79.19166666666669130, 0.7554284705563518720 ) ) ;
#35183=CARTESIAN_POINT ( 'NONE',  ( -0.1963495408493673433, -77.88541666666668561, 1.499999999999999334 ) ) ;
#35195=CARTESIAN_POINT ( 'NONE',  ( 0.000000000000000000, -76.79999999999999716, 0.000000000000000000 ) ) ;
#35239=CARTESIAN_POINT ( 'NONE',  ( -1.113896998616000111, -81.55636123001200133, -1.168951411329999912 ) ) ;
#35259=CARTESIAN_POINT ( 'NONE',  ( -1.120379678216000041, -79.31128506247100063, -0.7232983489183999470 ) ) ;
#35275=CARTESIAN_POINT ( 'NONE',  ( 0.7969900020161251319, -79.92870045822861869, -0.9955794363004618619 ) ) ;
#35282=CARTESIAN_POINT ( 'NONE',  ( 0.6791306551168999617, -81.38940478334400552, -1.147762040996999966 ) ) ;
#35290=CARTESIAN_POINT ( 'NONE',  ( 1.309590324566999975, -81.98873225866600478, -0.05285834632500000657 ) ) ;
#35295=CARTESIAN_POINT ( 'NONE',  ( -1.487176594838000021, -80.53170427028999256, 0.2955346688291999868 ) ) ;
#35299=CARTESIAN_POINT ( 'NONE',  ( 1.399739583348414529, -82.10026041666372976, 0.1840776944558860095 ) ) ;
#35309=B_SPLINE_SURFACE_WITH_KNOTS ( 'NONE', 3, 3, ( 
 ( #38282, #29987, #6411, #48041, #20576, #47470, #6994, #24998, #24124, #51880, #43018, #33262, #1711, #37702, #55722, #42440, #15268, #51303, #10861, #2007, #15564, #11153, #47174, #6705, #24716, #56302, #15857, #33843, #48894, #31138, #57451, #48321, #43889, #43592, #40319 ),
 ( #7861, #22304, #58328, #25860, #44752, #7572, #4303, #53607, #49178, #21436, #12855, #3155, #48605, #17892, #26724, #25572, #44451, #3435, #16725, #17010, #53909, #8152, #39445, #26151, #35881, #13442, #8731, #31442, #58031, #21144, #12576, #34993, #35578, #13146, #53024 ),
 ( #39152, #12289, #34707, #57159, #52738, #30573, #30279, #44171, #3719, #22008, #21721, #39726, #57734, #17293, #35282, #53312, #30856, #8435, #26430, #4003, #40015, #17591, #28696, #37558, #9032, #11010, #19860, #9615, #55575, #38142, #37855, #54199, #55876, #15426, #33122 ),
 ( #2154, #27603, #33419, #23981, #51457, #28994, #47035, #6565, #40908, #24282, #13736, #31734, #15124, #24573, #49779, #42590, #20155, #54494, #51165, #56166, #19560, #36467, #15714, #10719, #49482, #27019, #45055, #46747, #6267, #4607, #42300, #45347, #1865, #18188, #45645 ) ),
 .UNSPECIFIED., .F., .F., .F.,
 ( 4, 4 ),
 ( 4, 1, 1, 1, 1, 1, 1, 1, 1, 1, 1, 1, 1, 1, 1, 1, 1, 1, 1, 1, 1, 1, 1, 1, 1, 1, 1, 1, 1, 1, 1, 1, 4 ),
 ( -0.1566102636784000024, 1.156610263678000017 ),
 ( -0.02000000000000000042, 0.01250000000000000069, 0.04499999999999999833, 0.07749999999999999944, 0.1100000000000000006, 0.1424999999999999878, 0.1749999999999999889, 0.2074999999999999900, 0.2399999999999999911, 0.2725000000000000200, 0.3049999999999999933, 0.3375000000000000222, 0.3699999999999999956, 0.4025000000000000244, 0.4349999999999999978, 0.4675000000000000266, 0.5000000000000000000, 0.5324999999999999734, 0.5649999999999999467, 0.5975000000000000311, 0.6300000000000000044, 0.6624999999999999778, 0.6949999999999999512, 0.7275000000000000355, 0.7600000000000000089, 0.7924999999999999822, 0.8249999999999999556, 0.8575000000000000400, 0.8900000000000000133, 0.9224999999999999867, 0.9549999999999999600, 0.9875000000000000444, 1.020000000000000018 ),
 .UNSPECIFIED. ) ;
#35315=CARTESIAN_POINT ( 'NONE',  ( 0.1943040786466343206, -82.02213541144035958, -1.477864610832026804 ) ) ;
#35316=B_SPLINE_CURVE_WITH_KNOTS ( 'NONE', 3,
 ( #32579, #50626, #46499, #14586, #41754, #42347, #42046, #760, #1616, #24033, #37314, #1046, #32871, #19608, #37607, #1329, #5731, #28154 ),
 .UNSPECIFIED., .F., .F.,
 ( 4, 2, 2, 2, 2, 2, 2, 2, 4 ),
 ( 0.000000000000000000, 0.1250000000000000833, 0.2500000000000001665, 0.3750000000000001665, 0.5000000000000002220, 0.6250000000000002220, 0.7500000000000001110, 0.8750000000000001110, 1.000000000000000000 ),
 .UNSPECIFIED. ) ;
#35318=CARTESIAN_POINT ( 'NONE',  ( 0.4456039955205827185, -80.49636525167119316, 1.193634369761791492 ) ) ;
#35319=AXIS2_PLACEMENT_3D ( 'NONE', #7257, #2831, #38835 ) ;
#35331=CARTESIAN_POINT ( 'NONE',  ( 0.1963495408493637351, -80.03541666666670551, -1.499999999999999778 ) ) ;
#35343=LINE ( 'NONE', #40076, #24942 ) ;
#35344=CARTESIAN_POINT ( 'NONE',  ( 0.2526653223220000632, -78.77055390729400131, 1.594795962155999947 ) ) ;
#35350=CARTESIAN_POINT ( 'NONE',  ( 0.8816674349947000167, -78.05869998691809997, 0.9814419191067000892 ) ) ;
#35366=LINE ( 'NONE', #7654, #4094 ) ;
#35379=ORIENTED_EDGE ( 'NONE', *, *, #58202, .T. ) ;
#35383=VERTEX_POINT ( 'NONE', #43532 ) ;
#35388=DIRECTION ( 'NONE',  ( -1.000000000000000000, 0.000000000000000000, 0.000000000000000000 ) ) ;
#35397=ADVANCED_FACE ( 'NONE', ( #57102 ), #35745, .F. ) ;
#35399=CARTESIAN_POINT ( 'NONE',  ( 0.2630806288481999933, -79.88291798508399211, -1.292808645144999824 ) ) ;
#35401=CARTESIAN_POINT ( 'NONE',  ( -1.001490227998000027, -79.15975894690099324, -0.8734289068823000157 ) ) ;
#35475=SURFACE_STYLE_USAGE ( .BOTH. , #7768 ) ;
#35484=EDGE_CURVE ( 'NONE', #12549, #43416, #40182, .T. ) ;
#35528=CARTESIAN_POINT ( 'NONE',  ( -1.172432707911829297, -77.68180296370584870, -0.4984351444782006424 ) ) ;
#35558=CARTESIAN_POINT ( 'NONE',  ( -1.185397549814999785, -80.30353753009200091, -0.6110718436566999756 ) ) ;
#35574=CARTESIAN_POINT ( 'NONE',  ( 0.4728636598485260745, -79.59476634619571200, 1.184081205126365388 ) ) ;
#35578=CARTESIAN_POINT ( 'NONE',  ( -0.9657971644277000278, -82.23865798662500026, -0.9195906491977999808 ) ) ;
#35582=EDGE_CURVE ( 'NONE', #35000, #24789, #6208, .T. ) ;
#35588=CARTESIAN_POINT ( 'NONE',  ( -1.356221256960000066, -80.87683204993798824, -0.4246310591675999668 ) ) ;
#35594=CARTESIAN_POINT ( 'NONE',  ( 1.413837046361000160, -79.34676037349100852, -0.1054710693050000120 ) ) ;
#35602=EDGE_CURVE ( 'NONE', #39760, #38477, #57901, .T. ) ;
#35608=ORIENTED_EDGE ( 'NONE', *, *, #54253, .T. ) ;
#35613=DIRECTION ( 'NONE',  ( 0.000000000000000000, 1.000000000000000000, -1.868195065453000187E-14 ) ) ;
#35627=CARTESIAN_POINT ( 'NONE',  ( 1.310679582531388387, -80.10833333333333428, -0.7554284705563470981 ) ) ;
#35641=CARTESIAN_POINT ( 'NONE',  ( -1.598336519864000049, -78.91939177743699929, -0.2292036100155999956 ) ) ;
#35648=CARTESIAN_POINT ( 'NONE',  ( -1.500000000000000444, -79.88958333333333428, 0.1963495408493560745 ) ) ;
#35649=CARTESIAN_POINT ( 'NONE',  ( 1.384987510431000102, -78.06445905126490459, 0.3030985439221999811 ) ) ;
#35683=( NAMED_UNIT ( * ) SI_UNIT ( $, .STERADIAN. ) SOLID_ANGLE_UNIT ( ) );
#35704=CARTESIAN_POINT ( 'NONE',  ( -1.434155062425999994, -79.36523479771300060, -0.2237658014421000097 ) ) ;
#35705=EDGE_CURVE ( 'NONE', #36029, #49361, #58117, .T. ) ;
#35706=CARTESIAN_POINT ( 'NONE',  ( 0.9283799206808001081, -78.47094128391260881, 0.9373773696604000838 ) ) ;
#35711=CARTESIAN_POINT ( 'NONE',  ( -1.338465391571669771, -79.07632407938210406, -0.4637712603925426835 ) ) ;
#35745=CYLINDRICAL_SURFACE ( 'NONE', #56130, 0.5000000000000000000 ) ;
#35838=CARTESIAN_POINT ( 'NONE',  ( -0.7186842730350999631, -81.90364959367900610, 1.445929338514000184 ) ) ;
#35842=VERTEX_POINT ( 'NONE', #31436 ) ;
#35845=CARTESIAN_POINT ( 'NONE',  ( 0.3926218265389159190, -78.35416666666667140, 1.460959015002474715 ) ) ;
#35859=CARTESIAN_POINT ( 'NONE',  ( 1.250000000000000000, -76.50000000000000000, 0.5000000000000000000 ) ) ;
#35876=CARTESIAN_POINT ( 'NONE',  ( 1.117654118288571752, -79.96050370699357757, -0.6128475875778812698 ) ) ;
#35881=CARTESIAN_POINT ( 'NONE',  ( 0.6224761083686999319, -81.84175699957599193, -1.179448874982999884 ) ) ;
#35887=ORIENTED_EDGE ( 'NONE', *, *, #2068, .F. ) ;
#35889=CARTESIAN_POINT ( 'NONE',  ( -1.276921705536999907, -82.22385602485501011, 0.2952546641816000128 ) ) ;
#35896=CARTESIAN_POINT ( 'NONE',  ( 0.6128924939060999000, -79.94211185406399522, 1.278445216313999877 ) ) ;
#35897=ORIENTED_EDGE ( 'NONE', *, *, #21984, .T. ) ;
#35918=CARTESIAN_POINT ( 'NONE',  ( 1.117363022987682308, -79.86030597755448923, -0.6126732938519671157 ) ) ;
#35936=CARTESIAN_POINT ( 'NONE',  ( 1.007188805101713047, -81.05645702792023144, 0.8611998455131303354 ) ) ;
#35944=CARTESIAN_POINT ( 'NONE',  ( 1.079065815471999867, -78.22481505010179603, 1.201179019145000026 ) ) ;
#35951=CARTESIAN_POINT ( 'NONE',  ( 0.7786926255480000059, -78.02060549223070041, -1.300993539011999989 ) ) ;
#35960=DIRECTION ( 'NONE',  ( 1.000000000000000000, 0.000000000000000000, 0.000000000000000000 ) ) ;
#35989=ORIENTED_EDGE ( 'NONE', *, *, #38556, .F. ) ;
#36003=CARTESIAN_POINT ( 'NONE',  ( 0.2446082660763000405, -80.54515928207800357, -1.596051606003999979 ) ) ;
#36004=CARTESIAN_POINT ( 'NONE',  ( -1.313442439244999926, -79.16551801124799681, -0.1235842678404999867 ) ) ;
#36029=VERTEX_POINT ( 'NONE', #37625 ) ;
#36045=CARTESIAN_POINT ( 'NONE',  ( 0.000000000000000000, -76.00000000000000000, -2.799999999999999822 ) ) ;
#36071=AXIS2_PLACEMENT_3D ( 'NONE', #29332, #47379, #25703 ) ;
#36074=ORIENTED_EDGE ( 'NONE', *, *, #23252, .F. ) ;
#36092=EDGE_CURVE ( 'NONE', #22393, #50254, #14604, .T. ) ;
#36102=CARTESIAN_POINT ( 'NONE',  ( -0.6878299077642000547, -82.26466602871199996, -1.043738481606000024 ) ) ;
#36106=ORIENTED_EDGE ( 'NONE', *, *, #39005, .T. ) ;
#36121=B_SPLINE_SURFACE_WITH_KNOTS ( 'NONE', 3, 3, ( 
 ( #36272, #5274, #872, #31830, #22990, #593, #36563, #14125, #32121, #33865, #42464, #56329, #24450, #6144, #28570, #23855, #2030, #19442, #14996, #28860, #51328, #10885, #32993, #20030, #15295, #33288, #15587, #41872, #24153, #1448, #37433, #46909, #42752, #5849, #51905 ),
 ( #51039, #1739, #47201, #38016, #55452, #24738, #33584, #29154, #6436, #56039, #51622, #11177, #6730, #2317, #10586, #42171, #20311, #15880, #11462, #38309, #46617, #19732, #37729, #50749, #55750, #10293, #28274, #46324, #23465, #23756, #55349, #54765, #41769, #32889, #19048 ),
 ( #54191, #32019, #13729, #14601, #40607, #27592, #19338, #5748, #41477, #40898, #41186, #32597, #54485, #50934, #45635, #22886, #31726, #50645, #5175, #487, #14891, #55055, #37332, #50061, #4888, #10192, #28171, #14020, #10481, #27307, #9899, #45338, #18754, #46224, #45045 ),
 ( #4598, #22597, #32302, #205, #9607, #14308, #36458, #36748, #18179, #36174, #50350, #9313, #49771, #23180, #776, #27881, #45928, #5461, #1060, #11649, #2496, #46515, #11362, #29056, #2216, #6335, #20501, #38497, #28466, #1932, #37914, #24048, #6917, #51517, #56514 ) ),
 .UNSPECIFIED., .F., .F., .F.,
 ( 4, 4 ),
 ( 4, 1, 1, 1, 1, 1, 1, 1, 1, 1, 1, 1, 1, 1, 1, 1, 1, 1, 1, 1, 1, 1, 1, 1, 1, 1, 1, 1, 1, 1, 1, 1, 4 ),
 ( -0.1566102636784000024, 1.156610263678000017 ),
 ( -0.02000000000000000042, 0.01250000000000000069, 0.04499999999999999833, 0.07749999999999999944, 0.1100000000000000006, 0.1424999999999999878, 0.1749999999999999889, 0.2074999999999999900, 0.2399999999999999911, 0.2725000000000000200, 0.3049999999999999933, 0.3375000000000000222, 0.3699999999999999956, 0.4025000000000000244, 0.4349999999999999978, 0.4675000000000000266, 0.5000000000000000000, 0.5324999999999999734, 0.5649999999999999467, 0.5975000000000000311, 0.6300000000000000044, 0.6624999999999999778, 0.6949999999999999512, 0.7275000000000000355, 0.7600000000000000089, 0.7924999999999999822, 0.8249999999999999556, 0.8575000000000000400, 0.8900000000000000133, 0.9224999999999999867, 0.9549999999999999600, 0.9875000000000000444, 1.020000000000000018 ),
 .UNSPECIFIED. ) ;
#36139=CARTESIAN_POINT ( 'NONE',  ( -1.586818774941000099, -81.50674860663099253, -0.2986973412923999982 ) ) ;
#36174=CARTESIAN_POINT ( 'NONE',  ( 0.1443438050804999873, -78.13203116825889083, 1.325798245762999983 ) ) ;
#36178=CARTESIAN_POINT ( 'NONE',  ( -0.9505604537480174532, -80.69197842858829972, 0.8492125078390942994 ) ) ;
#36181=DIRECTION ( 'NONE',  ( 0.000000000000000000, 0.000000000000000000, -1.000000000000000000 ) ) ;
#36192=CARTESIAN_POINT ( 'NONE',  ( -0.4410321586598999755, -81.19765838811301251, 1.337641107945999996 ) ) ;
#36198=CARTESIAN_POINT ( 'NONE',  ( 0.2630806288481999933, -79.79903304826800081, -1.292808645144999824 ) ) ;
#36219=CARTESIAN_POINT ( 'NONE',  ( 0.5768166144513863225, -79.81260153199569629, -1.136130408118528390 ) ) ;
#36221=LINE ( 'NONE', #41236, #15175 ) ;
#36237=CARTESIAN_POINT ( 'NONE',  ( -0.6762394706190373306, -81.66777882001223077, 1.139646768752475614 ) ) ;
#36248=EDGE_CURVE ( 'NONE', #10750, #46183, #47542, .T. ) ;
#36253=CARTESIAN_POINT ( 'NONE',  ( 0.2897255177615999933, -79.15593676564900250, 1.387848051154999762 ) ) ;
#36272=CARTESIAN_POINT ( 'NONE',  ( -1.159125165887999964, -77.60380812847459708, 0.4678983327651999868 ) ) ;
#36300=CARTESIAN_POINT ( 'NONE',  ( -0.3384184472371999930, -79.74559824363400651, 1.477976681755000188 ) ) ;
#36343=CARTESIAN_POINT ( 'NONE',  ( 1.460959015002474048, -81.22916666666668561, -0.3926218265389178064 ) ) ;
#36379=ORIENTED_EDGE ( 'NONE', *, *, #3326, .F. ) ;
#36384=EDGE_CURVE ( 'NONE', #50394, #34384, #46531, .T. ) ;
#36418=CARTESIAN_POINT ( 'NONE',  ( -0.5949767217100950800, -78.06343852817556694, 1.127525434812421512 ) ) ;
#36428=CARTESIAN_POINT ( 'NONE',  ( 1.142015885854000157, -81.80442434691700271, 1.141496088348999960 ) ) ;
#36442=CARTESIAN_POINT ( 'NONE',  ( -0.2340539085346999837, -80.11092564237000602, 1.312933706406000267 ) ) ;
#36458=CARTESIAN_POINT ( 'NONE',  ( 1.224162466603000210, -77.98319329811559442, -0.5291525010897000225 ) ) ;
#36463=ORIENTED_EDGE ( 'NONE', *, *, #46258, .F. ) ;
#36467=CARTESIAN_POINT ( 'NONE',  ( -1.310615285706999922, -81.78046716459000720, -0.2467057407436999972 ) ) ;
#36477=CARTESIAN_POINT ( 'NONE',  ( -0.8817537164447001308, -80.86848511544799578, -1.098257200506999931 ) ) ;
#36483=CARTESIAN_POINT ( 'NONE',  ( 1.309314855877999895, -79.89825829503000421, -0.1620500492231000123 ) ) ;
#36486=CARTESIAN_POINT ( 'NONE',  ( -1.500000000000000000, -78.89999999999999147, 0.000000000000000000 ) ) ;
#36492=CARTESIAN_POINT ( 'NONE',  ( 1.249999993052000047, -76.30000000069199473, 0.6999999993075000093 ) ) ;
#36498=VECTOR ( 'NONE', #5629, 1000.000000000000114 ) ;
#36502=B_SPLINE_CURVE_WITH_KNOTS ( 'NONE', 3,
 ( #29128, #11726, #42442, #2009, #43019, #20859, #37990, #25286, #16439, #42728 ),
 .UNSPECIFIED., .F., .F.,
 ( 4, 2, 2, 2, 4 ),
 ( 0.000000000000000000, 0.2500000000000000000, 0.5000000000000000000, 0.7500000000000000000, 1.000000000000000000 ),
 .UNSPECIFIED. ) ;
#36509=CARTESIAN_POINT ( 'NONE',  ( 0.7895151306900345389, -79.97161635052492556, 1.000479881221597367 ) ) ;
#36511=DIRECTION ( 'NONE',  ( 0.000000000000000000, 1.000000000000000000, 1.813364273554000256E-14 ) ) ;
#36520=CARTESIAN_POINT ( 'NONE',  ( -0.9565643533716999825, -80.07299023059400156, 0.9292797142584000580 ) ) ;
#36543=AXIS2_PLACEMENT_3D ( 'NONE', #5847, #13831, #32120 ) ;
#36545=CARTESIAN_POINT ( 'NONE',  ( -1.376714249866999973, -78.31828123251710849, 0.6352952275891999845 ) ) ;
#36552=PLANE ( 'NONE',  #11360 ) ;
#36555=DIRECTION ( 'NONE',  ( 1.000000000000000000, 0.000000000000000000, 0.000000000000000000 ) ) ;
#36560=CARTESIAN_POINT ( 'NONE',  ( 1.042635221160942649, -80.68436150525303674, -1.121867648172004017 ) ) ;
#36563=CARTESIAN_POINT ( 'NONE',  ( 1.224162466603000210, -77.85187124537999637, -0.5291525010897000225 ) ) ;
#36591=CARTESIAN_POINT ( 'NONE',  ( -1.273775855157000203, -79.39830987996700173, -0.8223283506838999779 ) ) ;
#36607=CARTESIAN_POINT ( 'NONE',  ( -0.6747260877994001316, -82.22962677363800310, -1.052256958371999840 ) ) ;
#36628=ORIENTED_EDGE ( 'NONE', *, *, #38818, .F. ) ;
#36641=ORIENTED_EDGE ( 'NONE', *, *, #21756, .T. ) ;
#36657=B_SPLINE_CURVE_WITH_KNOTS ( 'NONE', 3,
 ( #55622, #20768, #7190, #24621 ),
 .UNSPECIFIED., .F., .F.,
 ( 4, 4 ),
 ( 0.000000000000000000, 1.000000000000000000 ),
 .UNSPECIFIED. ) ;
#36660=CARTESIAN_POINT ( 'NONE',  ( 0.7554284705563453217, -77.83333333333335702, 1.310679582531389276 ) ) ;
#36661=CARTESIAN_POINT ( 'NONE',  ( 0.6906586288378000482, -78.65211458439600278, -1.459522026167999975 ) ) ;
#36663=AXIS2_PLACEMENT_3D ( 'NONE', #1328, #19030, #10176 ) ;
#36698=CARTESIAN_POINT ( 'NONE',  ( -0.1963495408493673433, -80.38541666666669983, 1.499999999999999334 ) ) ;
#36719=CARTESIAN_POINT ( 'NONE',  ( 0.9631070755298999364, -80.86754356702299162, 1.171053640356000125 ) ) ;
#36748=CARTESIAN_POINT ( 'NONE',  ( 1.302799686710000016, -78.03280592149668848, 0.2851120931344000020 ) ) ;
#36767=CARTESIAN_POINT ( 'NONE',  ( -0.2581798279218999737, -82.29592158156299320, 1.583182092587000156 ) ) ;
#36773=CARTESIAN_POINT ( 'NONE',  ( -0.7554284705563544255, -81.41666666666668561, 1.310679582531384169 ) ) ;
#36776=CARTESIAN_POINT ( 'NONE',  ( -0.9218200799623714747, -78.97291666666669130, -1.199500263597270466 ) ) ;
#36809=CARTESIAN_POINT ( 'NONE',  ( -0.2340539085346999837, -80.02337760721299276, 1.312933706406000267 ) ) ;
#36832=CARTESIAN_POINT ( 'NONE',  ( -1.183003490338000008, -79.33784971804600161, -0.6653023415106000815 ) ) ;
#36838=EDGE_CURVE ( 'NONE', #17863, #32930, #32475, .T. ) ;
#36847=CARTESIAN_POINT ( 'NONE',  ( -1.178447680628000205, -80.55308451575899653, -0.9280415206345000723 ) ) ;
#36880=CARTESIAN_POINT ( 'NONE',  ( 1.293420685949000060, -79.64637299687198890, 0.7912046490545000532 ) ) ;
#36906=CONICAL_SURFACE ( 'NONE', #44452, 3.899999999992999733, 0.7853981633972997312 ) ;
#36920=CARTESIAN_POINT ( 'NONE',  ( -1.500000000000000000, -79.00000000000000000, 0.000000000000000000 ) ) ;
#36952=CARTESIAN_POINT ( 'NONE',  ( -1.472799192485999997, -77.56639593435953373, -0.3599880333205999761 ) ) ;
#36983=EDGE_CURVE ( 'NONE', #19319, #30464, #43065, .T. ) ;
#37007=CARTESIAN_POINT ( 'NONE',  ( -0.9780501945912999373, -81.66710460546799766, -1.026390372485000091 ) ) ;
#37011=AXIS2_PLACEMENT_3D ( 'NONE', #56609, #33580, #46320 ) ;
#37043=ORIENTED_EDGE ( 'NONE', *, *, #16332, .F. ) ;
#37057=CARTESIAN_POINT ( 'NONE',  ( 0.1975732027802999946, -81.48815384203000178, -1.493273510172999918 ) ) ;
#37063=CARTESIAN_POINT ( 'NONE',  ( -0.2315393795184000070, -80.04709616517300219, 1.298828366650000010 ) ) ;
#37083=DIRECTION ( 'NONE',  ( 0.000000000000000000, 1.000000000000000000, 0.000000000000000000 ) ) ;
#37099=CARTESIAN_POINT ( 'NONE',  ( -0.1698911186725000078, -80.51950384102399028, 1.322768475116000042 ) ) ;
#37107=CARTESIAN_POINT ( 'NONE',  ( -1.212057334841439848, -82.22243190943753177, 0.4356794552377592500 ) ) ;
#37129=CARTESIAN_POINT ( 'NONE',  ( -0.3926218265389190276, -81.60416666666667140, -1.460959015002473826 ) ) ;
#37173=ORIENTED_EDGE ( 'NONE', *, *, #17449, .T. ) ;
#37227=CARTESIAN_POINT ( 'NONE',  ( -0.9218200799623778030, -80.32708333333337691, 1.199500263597266914 ) ) ;
#37258=CARTESIAN_POINT ( 'NONE',  ( -0.9644448879797564711, -78.30674845405408746, -0.8345157321849741017 ) ) ;
#37278=CARTESIAN_POINT ( 'NONE',  ( 1.460959015002472494, -80.27083333333337123, 0.3926218265389233020 ) ) ;
#37280=CARTESIAN_POINT ( 'NONE',  ( -1.250000000000000000, -76.50000000000000000, -0.5000000000000000000 ) ) ;
#37290=CARTESIAN_POINT ( 'NONE',  ( -1.310679582531386389, -77.94166666666667709, -0.7554284705563492075 ) ) ;
#37298=CARTESIAN_POINT ( 'NONE',  ( -1.026725001539000148, -82.16323083927800042, -0.9776035232744000325 ) ) ;
#37302=CARTESIAN_POINT ( 'NONE',  ( -0.3926218265389255779, -81.89583333334149984, 1.460959015002472494 ) ) ;
#37314=CARTESIAN_POINT ( 'NONE',  ( 0.3926218265389159190, -79.35416666666668561, 1.460959015002474715 ) ) ;
#37332=CARTESIAN_POINT ( 'NONE',  ( -1.320128238786999919, -78.73322125463400312, -0.1893081677438999966 ) ) ;
#37339=ORIENTED_EDGE ( 'NONE', *, *, #11017, .T. ) ;
#37350=CARTESIAN_POINT ( 'NONE',  ( -1.427775756650000005, -82.36594923580300076, -0.2438566963919999719 ) ) ;
#37357=CARTESIAN_POINT ( 'NONE',  ( -0.9004272109156999937, -80.59283502236499430, 0.9642496934733999492 ) ) ;
#37395=DIRECTION ( 'NONE',  ( 0.000000000000000000, 1.000000000000000000, 0.000000000000000000 ) ) ;
#37404=DIRECTION ( 'NONE',  ( 0.000000000000000000, 0.7071067811865475727, -0.7071067811865475727 ) ) ;
#37433=CARTESIAN_POINT ( 'NONE',  ( -0.5409299486741000473, -79.04257420652599819, 1.218996123443000013 ) ) ;
#37456=CARTESIAN_POINT ( 'NONE',  ( 1.500000000000000000, -81.25000000000000000, 0.000000000000000000 ) ) ;
#37484=CARTESIAN_POINT ( 'NONE',  ( 1.042635221160942871, -81.08436150525301400, -1.121867648172004017 ) ) ;
#37489=LINE ( 'NONE', #31223, #39254 ) ;
#37505=VECTOR ( 'NONE', #5555, 1000.000000000000000 ) ;
#37511=ORIENTED_EDGE ( 'NONE', *, *, #47202, .F. ) ;
#37518=CARTESIAN_POINT ( 'NONE',  ( 1.310679582531385501, -80.19166666666669130, 0.7554284705563518720 ) ) ;
#37530=CARTESIAN_POINT ( 'NONE',  ( -0.1273708076881999995, -77.66562118112170765, -1.510858618444999912 ) ) ;
#37558=CARTESIAN_POINT ( 'NONE',  ( -0.1832406609208000192, -81.83591839377399424, -1.320984106490000087 ) ) ;
#37583=CARTESIAN_POINT ( 'NONE',  ( -1.460959015002473826, -77.92083333333336270, -0.3926218265389207485 ) ) ;
#37590=ORIENTED_EDGE ( 'NONE', *, *, #25227, .T. ) ;
#37591=CARTESIAN_POINT ( 'NONE',  ( -1.373488406293000175, -81.51250767097698713, 0.6422396358374999892 ) ) ;
#37605=CARTESIAN_POINT ( 'NONE',  ( -1.750000000000000000, -77.10000000000000853, 0.000000000000000000 ) ) ;
#37607=CARTESIAN_POINT ( 'NONE',  ( 1.310679582531385279, -79.29166666666667140, 0.7554284705563519831 ) ) ;
#37625=CARTESIAN_POINT ( 'NONE',  ( -1.500000000000000000, -78.50000000000000000, 0.000000000000000000 ) ) ;
#37645=CARTESIAN_POINT ( 'NONE',  ( 1.219183338402999750, -81.21435225709299743, 1.042466414804000152 ) ) ;
#37702=CARTESIAN_POINT ( 'NONE',  ( -0.1187445621502999926, -81.25224412480599767, -1.328335755224000048 ) ) ;
#37704=CARTESIAN_POINT ( 'NONE',  ( -0.1963495408493606265, -80.51458333333334849, -1.500000000000000222 ) ) ;
#37729=CARTESIAN_POINT ( 'NONE',  ( -1.320128238786999919, -78.68944723705600097, -0.1893081677438999966 ) ) ;
#37791=VERTEX_POINT ( 'NONE', #17236 ) ;
#37813=CARTESIAN_POINT ( 'NONE',  ( -1.500000000000000000, -80.40000000000000568, 0.000000000000000000 ) ) ;
#37828=CARTESIAN_POINT ( 'NONE',  ( -0.2137776359178999996, -78.10637572720449384, -1.600472757759999753 ) ) ;
#37846=CARTESIAN_POINT ( 'NONE',  ( 0.1731036574200994771, -78.38625657596658414, -1.262699286490361894 ) ) ;
#37855=CARTESIAN_POINT ( 'NONE',  ( -1.179157772963000061, -82.18320675744099901, 0.6230118014947999550 ) ) ;
#37867=CARTESIAN_POINT ( 'NONE',  ( -1.500000000000000888, -80.48958333333335702, 0.1963495408493559080 ) ) ;
#37876=CARTESIAN_POINT ( 'NONE',  ( -1.500000000000000000, -77.89999999999999147, 0.000000000000000000 ) ) ;
#37884=CARTESIAN_POINT ( 'NONE',  ( 1.482789947567000111, -81.31405717745300876, 0.3166640546479999596 ) ) ;
#37891=CARTESIAN_POINT ( 'NONE',  ( -1.500000000000000000, -78.00000000000000000, 0.000000000000000000 ) ) ;
#37895=ORIENTED_EDGE ( 'NONE', *, *, #7536, .T. ) ;
#37914=CARTESIAN_POINT ( 'NONE',  ( -0.5409299486741000473, -79.17389625926099939, 1.218996123443000013 ) ) ;
#37921=CARTESIAN_POINT ( 'NONE',  ( -1.181111693982000110, -79.17654225787899236, -0.4092372983238000139 ) ) ;
#37933=CARTESIAN_POINT ( 'NONE',  ( 1.283682315402000063, -82.14650038736000681, 0.7880738512438000276 ) ) ;
#37939=CARTESIAN_POINT ( 'NONE',  ( -1.500000000000000000, -80.90000000000000568, 0.000000000000000000 ) ) ;
#37963=CARTESIAN_POINT ( 'NONE',  ( 1.250000000000000000, -77.10000000000000853, 0.5000000000000000000 ) ) ;
#37977=EDGE_CURVE ( 'NONE', #32341, #34809, #31624, .T. ) ;
#37984=FACE_OUTER_BOUND ( 'NONE', #24029, .T. ) ;
#37990=CARTESIAN_POINT ( 'NONE',  ( -0.4631590389519468220, -79.10102817191933866, -1.469247881823791957 ) ) ;
#38008=CARTESIAN_POINT ( 'NONE',  ( 1.590911073979999868, -80.22826946565700723, -0.2760724992506000119 ) ) ;
#38016=CARTESIAN_POINT ( 'NONE',  ( -0.8668440880359000733, -77.74680739281529895, -1.013523202003999923 ) ) ;
#38018=VECTOR ( 'NONE', #22796, 1000.000000000000000 ) ;
#38031=CIRCLE ( 'NONE', #45596, 1.500000000000000000 ) ;
#38041=CARTESIAN_POINT ( 'NONE',  ( 1.500000000000000000, -77.75000000000000000, 0.000000000000000000 ) ) ;
#38086=CARTESIAN_POINT ( 'NONE',  ( 1.181151010425000036, -81.87131416333899381, -0.5877481386164000732 ) ) ;
#38089=CARTESIAN_POINT ( 'NONE',  ( 0.4987784050544145642, -78.49277853820406392, 1.172641800718043470 ) ) ;
#38098=ORIENTED_EDGE ( 'NONE', *, *, #26448, .F. ) ;
#38110=VERTEX_POINT ( 'NONE', #940 ) ;
#38116=CARTESIAN_POINT ( 'NONE',  ( -0.2736340887363999941, -78.65787364874299215, -1.491330460909999989 ) ) ;
#38132=CARTESIAN_POINT ( 'NONE',  ( 0.4271247780714595432, -78.40215820034904937, -1.201638839774739065 ) ) ;
#38140=CARTESIAN_POINT ( 'NONE',  ( 0.6280001350017426764, -81.81618824546241342, -1.109471376811945298 ) ) ;
#38142=CARTESIAN_POINT ( 'NONE',  ( -0.5935892672256000147, -82.13359413406000442, 1.194249225580000129 ) ) ;
#38164=CARTESIAN_POINT ( 'NONE',  ( 0.9218200799623741393, -78.07708333333334849, -1.199500263597268690 ) ) ;
#38170=CIRCLE ( 'NONE', #10840, 1.000000000000000000 ) ;
#38198=CARTESIAN_POINT ( 'NONE',  ( -0.3750911572844000119, -82.24349422833900292, -1.205494135727000149 ) ) ;
#38205=CARTESIAN_POINT ( 'NONE',  ( -1.310679582531389276, -78.85833333333332007, 0.7554284705563443225 ) ) ;
#38212=ORIENTED_EDGE ( 'NONE', *, *, #28146, .T. ) ;
#38234=CARTESIAN_POINT ( 'NONE',  ( 1.460959015002472494, -81.27083333333332860, 0.3926218265389233020 ) ) ;
#38245=( NAMED_UNIT ( * ) PLANE_ANGLE_UNIT ( ) SI_UNIT ( $, .RADIAN. ) );
#38269=CARTESIAN_POINT ( 'NONE',  ( 1.329937235669000017, -79.42218752083800837, -0.09921221311570001256 ) ) ;
#38282=CARTESIAN_POINT ( 'NONE',  ( -1.200131629027000102, -80.65689264423299676, -0.3495483843597000373 ) ) ;
#38301=CARTESIAN_POINT ( 'NONE',  ( 1.512024872110000029, -79.29138868576299615, -0.1127957995495999927 ) ) ;
#38309=CARTESIAN_POINT ( 'NONE',  ( 0.2086861075963999945, -78.54060936691300299, 1.317203954600000060 ) ) ;
#38359=CARTESIAN_POINT ( 'NONE',  ( -1.178447680628000205, -80.95308451575900222, -0.9280415206345000723 ) ) ;
#38364=DIRECTION ( 'NONE',  ( -1.000000000000000000, 0.000000000000000000, 0.000000000000000000 ) ) ;
#38375=CARTESIAN_POINT ( 'NONE',  ( 1.030280495153508280, -78.34966520152786984, -0.7508267048928350951 ) ) ;
#38407=CARTESIAN_POINT ( 'NONE',  ( 1.045500971020000058, -78.91169582999499710, 0.9575944129536000382 ) ) ;
#38413=EDGE_CURVE ( 'NONE', #41674, #46158, #35366, .T. ) ;
#38425=CARTESIAN_POINT ( 'NONE',  ( 1.272562703582658106, -78.00461759078670809, 0.06755297771290638686 ) ) ;
#38433=CARTESIAN_POINT ( 'NONE',  ( -1.266772977591273719, -81.64127194508073160, 0.1360379414319277391 ) ) ;
#38473=CARTESIAN_POINT ( 'NONE',  ( -1.500000000000000222, -78.01041666666668561, -0.1963495408493622085 ) ) ;
#38477=VERTEX_POINT ( 'NONE', #20943 ) ;
#38497=CARTESIAN_POINT ( 'NONE',  ( 1.324344358081999795, -79.02505838911800140, 0.1571239973995999795 ) ) ;
#38500=CARTESIAN_POINT ( 'NONE',  ( -0.5900578684300998855, -82.22042515683899921, -1.108170840844000082 ) ) ;
#38505=DIRECTION ( 'NONE',  ( 0.000000000000000000, -1.000000000000000000, 0.000000000000000000 ) ) ;
#38515=AXIS2_PLACEMENT_3D ( 'NONE', #25698, #43727, #57289 ) ;
#38556=EDGE_CURVE ( 'NONE', #34384, #49070, #44584, .T. ) ;
#38560=CARTESIAN_POINT ( 'NONE',  ( 0.2659376973789999710, -79.81908850788599352, -1.306848610430999980 ) ) ;
#38594=ORIENTED_EDGE ( 'NONE', *, *, #39787, .F. ) ;
#38616=CARTESIAN_POINT ( 'NONE',  ( 1.046213688572526390, -79.35145855826110051, -0.7275327676939092880 ) ) ;
#38620=CARTESIAN_POINT ( 'NONE',  ( -1.460959015002474493, -78.37916666666666288, 0.3926218265389144757 ) ) ;
#38636=EDGE_CURVE ( 'NONE', #50254, #900, #38031, .T. ) ;
#38641=CARTESIAN_POINT ( 'NONE',  ( -1.460959015002473382, -78.52083333333334281, -0.3926218265389205819 ) ) ;
#38644=CARTESIAN_POINT ( 'NONE',  ( 1.406250000003000045, -82.09374999999700151, -9.314605757769000352E-11 ) ) ;
#38666=CARTESIAN_POINT ( 'NONE',  ( -1.112997722094761111, -78.19065038299876846, -0.6198689731120797797 ) ) ;
#38694=CARTESIAN_POINT ( 'NONE',  ( -1.402375016663000018, -80.28557803647899505, 0.2083355298385999865 ) ) ;
#38697=CARTESIAN_POINT ( 'NONE',  ( -0.6817061190079000133, -78.45942315521890009, 1.354333385606999896 ) ) ;
#38706=EDGE_CURVE ( 'NONE', #50254, #900, #52121, .T. ) ;
#38722=CARTESIAN_POINT ( 'NONE',  ( 0.6025325372421354020, -80.81439488872916854, -1.122865852738351489 ) ) ;
#38737=CARTESIAN_POINT ( 'NONE',  ( -1.250000000000000000, -77.75000000000000000, 0.000000000000000000 ) ) ;
#38800=CARTESIAN_POINT ( 'NONE',  ( 1.310679582531387943, -80.20833333333332860, -0.7554284705563468760 ) ) ;
#38813=CARTESIAN_POINT ( 'NONE',  ( -0.1963495408493673433, -78.88541666666668561, 1.499999999999999334 ) ) ;
#38818=EDGE_CURVE ( 'NONE', #10750, #46629, #912, .T. ) ;
#38835=DIRECTION ( 'NONE',  ( -1.000000000000000000, 0.000000000000000000, 0.000000000000000000 ) ) ;
#38846=DIRECTION ( 'NONE',  ( 0.000000000000000000, 1.000000000000000000, 0.000000000000000000 ) ) ;
#38847=CARTESIAN_POINT ( 'NONE',  ( 1.170174673132000187, -79.96792637803000048, 0.6397400908730001001 ) ) ;
#38848=VECTOR ( 'NONE', #48236, 1000.000000000000000 ) ;
#38857=CARTESIAN_POINT ( 'NONE',  ( -0.5435958524137841641, -79.34034035607614044, -1.153047142414559856 ) ) ;
#38861=CARTESIAN_POINT ( 'NONE',  ( 1.310679582531388387, -80.60833333333333428, -0.7554284705563470981 ) ) ;
#38878=CARTESIAN_POINT ( 'NONE',  ( -0.5899402231854000700, -79.08717912789200000, -1.503093382721999882 ) ) ;
#38891=EDGE_CURVE ( 'NONE', #15713, #17863, #29724, .T. ) ;
#38929=CARTESIAN_POINT ( 'NONE',  ( -1.169594621339999918, -78.70366409087199600, 0.6104211924069999906 ) ) ;
#38945=VECTOR ( 'NONE', #12863, 1000.000000000000227 ) ;
#38955=CARTESIAN_POINT ( 'NONE',  ( -0.9818792729183725143, -78.09524149188138153, 0.8115973957462927491 ) ) ;
#38957=LINE ( 'NONE', #20383, #34588 ) ;
#38969=DIRECTION ( 'NONE',  ( 0.000000000000000000, -1.000000000000000000, 0.000000000000000000 ) ) ;
#38983=CARTESIAN_POINT ( 'NONE',  ( 1.275615568647000098, -80.58325377676599999, 0.6187600927687999519 ) ) ;
#38984=FACE_OUTER_BOUND ( 'NONE', #18358, .T. ) ;
#38986=CARTESIAN_POINT ( 'NONE',  ( -1.335620631414000004, -77.58869253983340286, 0.2413337786383999983 ) ) ;
#38987=CONICAL_SURFACE ( 'NONE', #47540, 1.249999999985999866, 0.7853981633972997312 ) ;
#38988=DIRECTION ( 'NONE',  ( 0.000000000000000000, 1.000000000000000000, 0.000000000000000000 ) ) ;
#39005=EDGE_CURVE ( 'NONE', #46158, #11615, #28365, .T. ) ;
#39012=CARTESIAN_POINT ( 'NONE',  ( -1.175893850647310446, -82.11831640066738203, 0.4910670358417331127 ) ) ;
#39015=CARTESIAN_POINT ( 'NONE',  ( -1.199500263597274241, -79.34791666666667709, 0.9218200799623669228 ) ) ;
#39066=APPLICATION_CONTEXT ( 'automotive_design' ) ;
#39078=CYLINDRICAL_SURFACE ( 'NONE', #31370, 1.500000000000000000 ) ;
#39084=DIRECTION ( 'NONE',  ( 0.000000000000000000, 1.000000000000000000, 0.000000000000000000 ) ) ;
#39103=CARTESIAN_POINT ( 'NONE',  ( -1.500000000000000000, -79.00000000000000000, 0.000000000000000000 ) ) ;
#39126=ORIENTED_EDGE ( 'NONE', *, *, #42688, .T. ) ;
#39138=CARTESIAN_POINT ( 'NONE',  ( 0.3292142484335000563, -79.36673629165399291, -1.292352404326999826 ) ) ;
#39152=CARTESIAN_POINT ( 'NONE',  ( -1.200131629027000102, -80.74444067939001002, -0.3495483843597000373 ) ) ;
#39167=CARTESIAN_POINT ( 'NONE',  ( -0.3603946542032999689, -79.38485486817801018, 1.573953487139999829 ) ) ;
#39190=CARTESIAN_POINT ( 'NONE',  ( -1.199500263597274241, -78.34791666666666288, 0.9218200799623669228 ) ) ;
#39201=CARTESIAN_POINT ( 'NONE',  ( -1.045756772073208829, -81.19753128763325378, 0.8139332635508695901 ) ) ;
#39209=DIRECTION ( 'NONE',  ( 0.000000000000000000, 1.000000000000000000, 0.000000000000000000 ) ) ;
#39237=CARTESIAN_POINT ( 'NONE',  ( -1.500000000000000222, -78.41041666666669130, -0.1963495408493622363 ) ) ;
#39246=ORIENTED_EDGE ( 'NONE', *, *, #25665, .F. ) ;
#39254=VECTOR ( 'NONE', #26227, 1000.000000000000000 ) ;
#39262=CARTESIAN_POINT ( 'NONE',  ( 1.460959015002472494, -79.77083333333334281, 0.3926218265389233020 ) ) ;
#39271=CARTESIAN_POINT ( 'NONE',  ( -1.200597545982000192, -80.77594520594300320, -0.5467811674232999630 ) ) ;
#39274=CARTESIAN_POINT ( 'NONE',  ( 1.505666248717000055, -78.80671151888600434, 0.1786365444185999962 ) ) ;
#39297=LINE ( 'NONE', #29847, #32816 ) ;
#39299=CARTESIAN_POINT ( 'NONE',  ( -1.213379087956198310, -81.62537046322781009, 0.3916290527410095090 ) ) ;
#39332=CYLINDRICAL_SURFACE ( 'NONE', #19226, 1.500000000000000000 ) ;
#39359=CARTESIAN_POINT ( 'NONE',  ( -0.7232461515322000656, -82.19001440484599641, -1.097480396689000104 ) ) ;
#39362=EDGE_CURVE ( 'NONE', #32341, #39914, #54316, .T. ) ;
#39414=CARTESIAN_POINT ( 'NONE',  ( -1.500000000000000888, -78.48958333333331439, 0.1963495408493559080 ) ) ;
#39422=CARTESIAN_POINT ( 'NONE',  ( 1.500000000000000000, -79.14999999999999147, 0.000000000000000000 ) ) ;
#39441=CARTESIAN_POINT ( 'NONE',  ( -0.1647852606798474728, -79.86509396069870093, -1.263697374764313874 ) ) ;
#39445=CARTESIAN_POINT ( 'NONE',  ( -0.9200108141794000050, -81.74253175281400274, -0.9654823929056000065 ) ) ;
#39461=CARTESIAN_POINT ( 'NONE',  ( -0.1806087918925000091, -80.48785071125600155, 1.406216040666999900 ) ) ;
#39465=EDGE_CURVE ( 'NONE', #46183, #43155, #35086, .T. ) ;
#39483=CARTESIAN_POINT ( 'NONE',  ( -0.9446365838440466955, -79.20834522158486379, -0.8548086173491427076 ) ) ;
#39498=LINE ( 'NONE', #25915, #54372 ) ;
#39504=CARTESIAN_POINT ( 'NONE',  ( 1.460959015002474048, -78.72916666666665719, -0.3926218265389178064 ) ) ;
#39508=AXIS2_PLACEMENT_3D ( 'NONE', #20224, #39084, #24929 ) ;
#39560=CARTESIAN_POINT ( 'NONE',  ( -1.227075629532000001, -79.83906442605000109, -0.7101723588523999320 ) ) ;
#39605=LINE ( 'NONE', #44917, #31673 ) ;
#39632=CARTESIAN_POINT ( 'NONE',  ( -0.9218200799623775810, -77.92708333333332860, 1.199500263597266247 ) ) ;
#39675=CARTESIAN_POINT ( 'NONE',  ( 1.310679582531385279, -78.79166666666667140, 0.7554284705563519831 ) ) ;
#39705=CARTESIAN_POINT ( 'NONE',  ( 0.5173218454072999739, -79.60896080275701081, 1.229208833401000067 ) ) ;
#39723=VERTEX_POINT ( 'NONE', #9321 ) ;
#39726=CARTESIAN_POINT ( 'NONE',  ( -1.297058042903999953, -81.24056691320100754, -0.3101879797029999941 ) ) ;
#39742=CARTESIAN_POINT ( 'NONE',  ( -1.191059436918999959, -79.14830987996700173, -0.7689280169367000983 ) ) ;
#39760=VERTEX_POINT ( 'NONE', #47106 ) ;
#39761=CARTESIAN_POINT ( 'NONE',  ( 0.7967880007212916338, -79.82850301384860359, -0.9953065419355184851 ) ) ;
#39772=CARTESIAN_POINT ( 'NONE',  ( -1.460959015002473826, -79.92083333333336270, -0.3926218265389207485 ) ) ;
#39784=CARTESIAN_POINT ( 'NONE',  ( -1.585290096527000259, -78.42326554362610125, -0.3067070840873000193 ) ) ;
#39787=EDGE_CURVE ( 'NONE', #39760, #45960, #21957, .T. ) ;
#39789=CARTESIAN_POINT ( 'NONE',  ( -1.500000000000000888, -80.98958333333332860, 0.1963495408493559080 ) ) ;
#39791=CARTESIAN_POINT ( 'NONE',  ( 0.6775591888709999733, -77.90986211677478934, -1.132025780260999870 ) ) ;
#39812=CONICAL_SURFACE ( 'NONE', #35078, 2.149999999947999729, 0.7853981633972997312 ) ;
#39821=SURFACE_SIDE_STYLE ('',( #44853 ) ) ;
#39843=CARTESIAN_POINT ( 'NONE',  ( 0.3499829075702999837, -79.44216343900099275, -1.373881155581999858 ) ) ;
#39848=CARTESIAN_POINT ( 'NONE',  ( -1.047405116191372443, -80.65287959514462557, -0.8248589924739977430 ) ) ;
#39865=CARTESIAN_POINT ( 'NONE',  ( 1.210004456578480880, -78.97461667811870711, -0.3996061539552085984 ) ) ;
#39875=CARTESIAN_POINT ( 'NONE',  ( -1.460959015002474493, -79.37916666666664867, 0.3926218265389144757 ) ) ;
#39914=VERTEX_POINT ( 'NONE', #37921 ) ;
#39953=CARTESIAN_POINT ( 'NONE',  ( 0.000000000000000000, -82.50000000000000000, -1.000000000000000000 ) ) ;
#39957=EDGE_CURVE ( 'NONE', #11684, #51104, #7159, .T. ) ;
#39994=CARTESIAN_POINT ( 'NONE',  ( 1.137658753740000028, -79.55934817937600201, 0.6959227610743999870 ) ) ;
#40009=CARTESIAN_POINT ( 'NONE',  ( -0.4078596229111138838, -80.15132319958321716, 1.208312492186587983 ) ) ;
#40012=EDGE_CURVE ( 'NONE', #11615, #15713, #25451, .T. ) ;
#40015=CARTESIAN_POINT ( 'NONE',  ( -1.208084210770999922, -81.68708052363099625, 0.5648970606752000689 ) ) ;
#40026=CARTESIAN_POINT ( 'NONE',  ( -1.189940096281000059, -80.83713527995598724, -0.6468527390756999562 ) ) ;
#40031=CARTESIAN_POINT ( 'NONE',  ( -0.9676267263329999535, -80.53746333463699614, 1.036212325607999807 ) ) ;
#40048=VECTOR ( 'NONE', #57531, 1000.000000000000000 ) ;
#40051=CARTESIAN_POINT ( 'NONE',  ( 1.268374697692444597, -79.90801042311336744, 0.1245783310639265173 ) ) ;
#40063=CARTESIAN_POINT ( 'NONE',  ( 0.9218200799623741393, -80.07708333333333428, -1.199500263597268690 ) ) ;
#40072=EDGE_CURVE ( 'NONE', #22104, #56774, #1260, .T. ) ;
#40076=CARTESIAN_POINT ( 'NONE',  ( -1.249999993052000047, -76.30000000069199473, -0.6999999993075000093 ) ) ;
#40081=CARTESIAN_POINT ( 'NONE',  ( -0.3926218265389255779, -80.89583333333337123, 1.460959015002472494 ) ) ;
#40082=CARTESIAN_POINT ( 'NONE',  ( 0.9218200799623692543, -79.72291666666667709, 1.199500263597272687 ) ) ;
#40083=CARTESIAN_POINT ( 'NONE',  ( 1.481171800329999844, -78.11983073899280328, 0.3241480609735999940 ) ) ;
#40140=CARTESIAN_POINT ( 'NONE',  ( -1.397510954313999854, -79.94980780150500266, -0.8088121278437000461 ) ) ;
#40141=CARTESIAN_POINT ( 'NONE',  ( 0.5643133282633999714, -78.81822964757999728, -1.192525073705999805 ) ) ;
#40150=DIRECTION ( 'NONE',  ( 0.000000000000000000, 0.000000000000000000, -1.000000000000000000 ) ) ;
#40182=LINE ( 'NONE', #26890, #41040 ) ;
#40215=CARTESIAN_POINT ( 'NONE',  ( -1.310679582531389498, -77.95833333333335702, 0.7554284705563444335 ) ) ;
#40276=CARTESIAN_POINT ( 'NONE',  ( -1.055696352445999908, -81.06023499620100381, -1.221768855801000253 ) ) ;
#40283=EDGE_CURVE ( 'NONE', #29318, #57022, #56403, .T. ) ;
#40315=CARTESIAN_POINT ( 'NONE',  ( 0.8766069548892785335, -79.43575010237100287, -0.9252077428013287808 ) ) ;
#40319=CARTESIAN_POINT ( 'NONE',  ( -0.2317941695893000198, -82.24449659242799271, -1.228320586388000013 ) ) ;
#40329=CARTESIAN_POINT ( 'NONE',  ( 0.7293115217919000637, -81.01790630965099638, -1.317947726832999988 ) ) ;
#40335=CARTESIAN_POINT ( 'NONE',  ( -0.7062052416310000691, -80.63092951705199596, -1.233256579520999763 ) ) ;
#40339=AXIS2_PLACEMENT_3D ( 'NONE', #42750, #11175, #43039 ) ;
#40356=CARTESIAN_POINT ( 'NONE',  ( -1.460777766812749734, -81.87926599238458891, 0.3927989208287778200 ) ) ;
#40358=CARTESIAN_POINT ( 'NONE',  ( -1.263722992889853014, -80.63947858834744409, 0.1647592273877500069 ) ) ;
#40376=DIRECTION ( 'NONE',  ( -0.7071067811865474617, 0.7071067811865474617, 9.196891653921612702E-11 ) ) ;
#40379=CARTESIAN_POINT ( 'NONE',  ( -1.369964363761594361, -82.06635564470731481, -0.4827857119653679030 ) ) ;
#40382=CARTESIAN_POINT ( 'NONE',  ( -0.6549273519428999712, -79.31629276448599342, 1.475891481164999908 ) ) ;
#40388=CARTESIAN_POINT ( 'NONE',  ( 1.500000000000000000, -79.65000000000000568, 0.000000000000000000 ) ) ;
#40389=CARTESIAN_POINT ( 'NONE',  ( 0.6485435286463999693, -79.01285795985199911, -1.370523042014000215 ) ) ;
#40391=EDGE_LOOP ( 'NONE', ( #45601, #3449, #43128, #15040 ) ) ;
#40405=DIRECTION ( 'NONE',  ( 0.000000000000000000, -1.000000000000000000, 0.000000000000000000 ) ) ;
#40409=CARTESIAN_POINT ( 'NONE',  ( -0.7554284705563483193, -81.48333333333334849, -1.310679582531387721 ) ) ;
#40411=EDGE_LOOP ( 'NONE', ( #8237, #22260, #56336, #31473 ) ) ;
#40432=CYLINDRICAL_SURFACE ( 'NONE', #50460, 4.000000000000000000 ) ;
#40442=CARTESIAN_POINT ( 'NONE',  ( -0.2833792192578999947, -80.29709616517300219, 1.589625787444000071 ) ) ;
#40444=CARTESIAN_POINT ( 'NONE',  ( 1.154392285689999742, -78.86784227096099187, -0.6387050628028000387 ) ) ;
#40462=AXIS2_PLACEMENT_3D ( 'NONE', #5442, #49756, #50043 ) ;
#40482=CARTESIAN_POINT ( 'NONE',  ( -0.05337949040085999963, -80.77983644895500959, -1.318251307669999983 ) ) ;
#40546=CARTESIAN_POINT ( 'NONE',  ( -0.4631590389519466555, -79.50102817191933013, -1.469247881823791957 ) ) ;
#40582=CARTESIAN_POINT ( 'NONE',  ( -1.460959015002474937, -78.47916666666664298, 0.3926218265389144757 ) ) ;
#40591=PLANE ( 'NONE',  #40462 ) ;
#40592=ADVANCED_FACE ( 'NONE', ( #23539 ), #6120, .T. ) ;
#40593=CARTESIAN_POINT ( 'NONE',  ( -0.6211595220380999871, -80.80550236970501032, -1.084739991049000096 ) ) ;
#40607=CARTESIAN_POINT ( 'NONE',  ( -0.1120320062231000002, -77.84019403377490676, -1.328911429676000067 ) ) ;
#40611=CARTESIAN_POINT ( 'NONE',  ( 0.2302091231002842686, -80.38984756532103404, -1.254262070711726906 ) ) ;
#40622=ORIENTED_EDGE ( 'NONE', *, *, #25087, .F. ) ;
#40626=CARTESIAN_POINT ( 'NONE',  ( 1.398926169692999766, -81.05658412839899540, 0.1637023605030999973 ) ) ;
#40633=CARTESIAN_POINT ( 'NONE',  ( -1.508831841893000236, -79.53945180266799753, 0.1495614418054999895 ) ) ;
#40656=CARTESIAN_POINT ( 'NONE',  ( 0.3448888686458475017, -80.00341931423071173, 1.227302044224852118 ) ) ;
#40688=CARTESIAN_POINT ( 'NONE',  ( -1.460959015002474493, -79.87916666666664867, 0.3926218265389144757 ) ) ;
#40689=CARTESIAN_POINT ( 'NONE',  ( -1.001490227998000027, -79.35438725917299507, -0.8734289068823000157 ) ) ;
#40719=FILL_AREA_STYLE_COLOUR ( '', #19042 ) ;
#40738=CARTESIAN_POINT ( 'NONE',  ( -1.137653363949000074, -79.79521086701498689, 1.002340751266999952 ) ) ;
#40858=CARTESIAN_POINT ( 'NONE',  ( 0.1449677685770666691, -78.01573408261680243, 1.266509336713319334 ) ) ;
#40860=CARTESIAN_POINT ( 'NONE',  ( -1.112877499973157436, -80.90331638296983385, -0.8763867746066754671 ) ) ;
#40864=ORIENTED_EDGE ( 'NONE', *, *, #28627, .F. ) ;
#40866=CARTESIAN_POINT ( 'NONE',  ( 1.579079316662999943, -81.25868548972499639, 0.3372275755211999737 ) ) ;
#40877=ORIENTED_EDGE ( 'NONE', *, *, #4833, .T. ) ;
#40881=CARTESIAN_POINT ( 'NONE',  ( -1.154258600661999923, -79.80741129628098918, -0.6680293646364998672 ) ) ;
#40898=CARTESIAN_POINT ( 'NONE',  ( 0.1443438050804999873, -78.08825715068029183, 1.325798245762999983 ) ) ;
#40908=CARTESIAN_POINT ( 'NONE',  ( 0.08638142328466999476, -81.13550306063599749, 1.330832257483999914 ) ) ;
#40916=CARTESIAN_POINT ( 'NONE',  ( 1.250000000000000000, -77.10000000000000853, -0.5000000000000000000 ) ) ;
#40919=CARTESIAN_POINT ( 'NONE',  ( 1.116962868089000027, -82.03575701190399627, 0.6857220190616999389 ) ) ;
#40927=CARTESIAN_POINT ( 'NONE',  ( -1.304983203281999904, -80.14632141193500559, 0.1938670925079999940 ) ) ;
#40933=ORIENTED_EDGE ( 'NONE', *, *, #38818, .T. ) ;
#40968=CARTESIAN_POINT ( 'NONE',  ( 0.07337134444413608014, -81.62075406677425349, 1.323144446007719965 ) ) ;
#40981=CARTESIAN_POINT ( 'NONE',  ( 0.9976655664682999580, -78.61019790845699617, 1.007334501387000092 ) ) ;
#40997=CARTESIAN_POINT ( 'NONE',  ( 0.1988171392200135945, -80.63513263419274324, -1.518600332402399777 ) ) ;
#41010=AXIS2_PLACEMENT_3D ( 'NONE', #28920, #56384, #19492 ) ;
#41014=DIRECTION ( 'NONE',  ( 0.000000000000000000, 1.000000000000000000, 0.000000000000000000 ) ) ;
#41028=CARTESIAN_POINT ( 'NONE',  ( -1.312293291923000149, -79.89443611377700449, -0.7594922433479999180 ) ) ;
#41040=VECTOR ( 'NONE', #52679, 1000.000000000000114 ) ;
#41048=VECTOR ( 'NONE', #26217, 1000.000000000000000 ) ;
#41092=ORIENTED_EDGE ( 'NONE', *, *, #58202, .F. ) ;
#41127=FACE_OUTER_BOUND ( 'NONE', #4576, .T. ) ;
#41151=ORIENTED_EDGE ( 'NONE', *, *, #22427, .F. ) ;
#41165=DIRECTION ( 'NONE',  ( 0.000000000000000000, 1.000000000000000000, 0.000000000000000000 ) ) ;
#41177=EDGE_CURVE ( 'NONE', #44267, #17252, #46378, .T. ) ;
#41186=CARTESIAN_POINT ( 'NONE',  ( -0.6568659331174000471, -78.13786977406140011, 1.160647793301999853 ) ) ;
#41194=CARTESIAN_POINT ( 'NONE',  ( -1.000000000000000000, -82.50000000000000000, 0.000000000000000000 ) ) ;
#41203=CARTESIAN_POINT ( 'NONE',  ( 1.070496197449000153, -81.10360888163698689, 0.9153310235335999634 ) ) ;
#41209=CARTESIAN_POINT ( 'NONE',  ( -1.200597545982000192, -80.69206026912699770, -0.5467811674232999630 ) ) ;
#41214=CARTESIAN_POINT ( 'NONE',  ( 0.3926218265389221362, -79.04583333333334849, -1.460959015002473160 ) ) ;
#41236=CARTESIAN_POINT ( 'NONE',  ( -1.249999996278000181, -76.50000000037098857, -0.4999999996289999915 ) ) ;
#41246=CARTESIAN_POINT ( 'NONE',  ( -1.248430190247999949, -79.13035038635399587, 0.06262635289305999720 ) ) ;
#41256=CARTESIAN_POINT ( 'NONE',  ( -0.9808057187987175851, -81.80885307972523890, -0.8911311466870025511 ) ) ;
#41269=ADVANCED_FACE ( 'NONE', ( #7293, #15866 ), #16447, .F. ) ;
#41271=CARTESIAN_POINT ( 'NONE',  ( 0.7144648680787000217, -78.51673172604100159, -1.337341431498000111 ) ) ;
#41273=ORIENTED_EDGE ( 'NONE', *, *, #26831, .T. ) ;
#41279=FACE_OUTER_BOUND ( 'NONE', #32335, .T. ) ;
#41289=CARTESIAN_POINT ( 'NONE',  ( 1.500000000000001110, -78.63958333333334849, -0.1963495408493590721 ) ) ;
#41308=STYLED_ITEM ( 'NONE', ( #34899 ), #16630 ) ;
#41319=CARTESIAN_POINT ( 'NONE',  ( -0.6603457068528999496, -80.88092951705199596, -1.153171400786999978 ) ) ;
#41330=B_SPLINE_SURFACE_WITH_KNOTS ( 'NONE', 3, 3, ( 
 ( #8162, #17304, #48331, #7870, #26163, #29428, #7006, #52179, #25583, #2590, #2871, #43605, #20869, #22615, #44461, #22312, #4012, #4908, #30867, #17901, #9626, #54506, #13745, #31149, #31450, #22907, #222, #35290, #40919, #53320, #22018, #508, #35889, #49189, #45654 ),
 ( #18484, #40026, #36477, #14043, #18200, #53616, #40626, #41203, #4616, #36192, #45064, #13454, #45358, #32037, #5196, #27614, #54210, #12865, #58338, #31745, #13154, #48903, #49790, #50081, #9336, #58039, #23198, #27325, #8443, #793, #53921, #9041, #8741, #26438, #17599 ),
 ( #35588, #26732, #44763, #4312, #40329, #49492, #27027, #29075, #24068, #1951, #47120, #14328, #51538, #5477, #37057, #28485, #50951, #10501, #19068, #42085, #55366, #14910, #51248, #9918, #5766, #27899, #45946, #32907, #37933, #50371, #6647, #46536, #32613, #37350, #55074 ),
 ( #23483, #19944, #10799, #6353, #6058, #1654, #19644, #37645, #15208, #55660, #41496, #33200, #33502, #32324, #1080, #28780, #18775, #46826, #23774, #24369, #14621, #55957, #50664, #41789, #42381, #15508, #10207, #11095, #24658, #42668, #36767, #54784, #28186, #46240, #1361 ) ),
 .UNSPECIFIED., .F., .F., .F.,
 ( 4, 4 ),
 ( 4, 1, 1, 1, 1, 1, 1, 1, 1, 1, 1, 1, 1, 1, 1, 1, 1, 1, 1, 1, 1, 1, 1, 1, 1, 1, 1, 1, 1, 1, 1, 1, 4 ),
 ( -0.05371687727927999811, 1.053716877278999986 ),
 ( -0.01895676948048000132, 0.01184798092530000083, 0.04265273133108000297, 0.07345748173685999471, 0.1042622321426000115, 0.1350669825483999942, 0.1658717329542000185, 0.1966764833600000151, 0.2274812337658000116, 0.2582859841715000049, 0.2890907345773000015, 0.3198954849830999980, 0.3507002353889000501, 0.3815049857946999912, 0.4123097362003999566, 0.4431144866061999532, 0.4739192370120000053, 0.5047239874178000019, 0.5355287378235999984, 0.5663334882294001060, 0.5971382386350999605, 0.6279429890408999571, 0.6587477394467000646, 0.6895524898524999502, 0.7203572402583000578, 0.7511619906639999122, 0.7819667410698000198, 0.8127714914756000164, 0.8435762418813999020, 0.8743809922872000095, 0.9051857426928999750, 0.9359904930987000826, 0.9667952435044999682 ),
 .UNSPECIFIED. ) ;
#41356=ORIENTED_EDGE ( 'NONE', *, *, #24622, .T. ) ;
#41391=CARTESIAN_POINT ( 'NONE',  ( 1.412851607863000014, -78.70172720777699737, -0.7817060856327000540 ) ) ;
#41394=DIRECTION ( 'NONE',  ( 0.000000000000000000, -1.000000000000000000, 0.000000000000000000 ) ) ;
#41399=B_SPLINE_CURVE_WITH_KNOTS ( 'NONE', 3,
 ( #11679, #2815, #29654, #47706 ),
 .UNSPECIFIED., .F., .F.,
 ( 4, 4 ),
 ( 0.000000000000000000, 1.000000000000000000 ),
 .UNSPECIFIED. ) ;
#41448=CARTESIAN_POINT ( 'NONE',  ( 0.9527810478389000526, -81.41904148856198731, 1.049889353731999986 ) ) ;
#41461=EDGE_CURVE ( 'NONE', #22736, #33739, #221, .T. ) ;
#41464=CARTESIAN_POINT ( 'NONE',  ( 2.299999999999999822, -76.00000000000000000, 0.000000000000000000 ) ) ;
#41477=CARTESIAN_POINT ( 'NONE',  ( 0.8912423865758999364, -78.03864452729919776, 0.9921004264782997684 ) ) ;
#41482=CARTESIAN_POINT ( 'NONE',  ( -2.799999999999999822, -76.00000000000000000, 0.000000000000000000 ) ) ;
#41496=CARTESIAN_POINT ( 'NONE',  ( -1.265869145960000219, -81.35542651680599135, 0.9852510953920999848 ) ) ;
#41503=CARTESIAN_POINT ( 'NONE',  ( 1.299878529918000014, -80.39438452883999275, -0.2255693107841999778 ) ) ;
#41507=VERTEX_POINT ( 'NONE', #44180 ) ;
#41545=CARTESIAN_POINT ( 'NONE',  ( 0.000000000000000000, -76.39999999999899671, 0.000000000000000000 ) ) ;
#41558=CARTESIAN_POINT ( 'NONE',  ( 1.199500263597271799, -80.19791666666667140, -0.9218200799623701425 ) ) ;
#41568=CARTESIAN_POINT ( 'NONE',  ( -1.199500263597270022, -81.55208333333334281, -0.9218200799623730290 ) ) ;
#41588=ORIENTED_EDGE ( 'NONE', *, *, #20120, .F. ) ;
#41644=AXIS2_PLACEMENT_3D ( 'NONE', #27408, #4985, #22992 ) ;
#41660=ORIENTED_EDGE ( 'NONE', *, *, #27537, .T. ) ;
#41667=CARTESIAN_POINT ( 'NONE',  ( 0.1963495408493571848, -80.26458333333334849, 1.500000000000000666 ) ) ;
#41673=DIRECTION ( 'NONE',  ( 0.000000000000000000, 1.000000000000000000, 0.000000000000000000 ) ) ;
#41674=VERTEX_POINT ( 'NONE', #36920 ) ;
#41676=CARTESIAN_POINT ( 'NONE',  ( -1.108343018679999847, -79.28756650451100541, -0.7155276831893999656 ) ) ;
#41713=DIRECTION ( 'NONE',  ( -1.000000000000000000, 0.000000000000000000, 0.000000000000000000 ) ) ;
#41714=DIRECTION ( 'NONE',  ( -1.000000000000000000, 0.000000000000000000, 0.000000000000000000 ) ) ;
#41717=CARTESIAN_POINT ( 'NONE',  ( 0.3926218265389159190, -80.35416666666668561, 1.460959015002474715 ) ) ;
#41733=CYLINDRICAL_SURFACE ( 'NONE', #13904, 1.500000000000000000 ) ;
#41736=CARTESIAN_POINT ( 'NONE',  ( 0.2289205461632000116, -81.96478034575399363, 1.399162150599000176 ) ) ;
#41738=ORIENTED_EDGE ( 'NONE', *, *, #49680, .T. ) ;
#41740=CARTESIAN_POINT ( 'NONE',  ( -1.460959015002474937, -81.97916666667948959, 0.3926218265389144757 ) ) ;
#41750=ORIENTED_EDGE ( 'NONE', *, *, #280, .T. ) ;
#41754=CARTESIAN_POINT ( 'NONE',  ( -1.199500263597274685, -79.44791666666668561, 0.9218200799623673669 ) ) ;
#41769=CARTESIAN_POINT ( 'NONE',  ( -1.327706488546999797, -79.18557347086598952, -0.1249263990498000187 ) ) ;
#41789=CARTESIAN_POINT ( 'NONE',  ( -1.187247102542000166, -81.96674830889799068, -1.078697698851999842 ) ) ;
#41796=CARTESIAN_POINT ( 'NONE',  ( -0.9462876233756999378, -80.09670878855399678, 0.9192961133846000443 ) ) ;
#41810=ORIENTED_EDGE ( 'NONE', *, *, #4758, .T. ) ;
#41834=CARTESIAN_POINT ( 'NONE',  ( 1.329937235669000017, -79.37841350325899725, -0.09921221311570001256 ) ) ;
#41844=ADVANCED_FACE ( 'NONE', ( #24703 ), #38987, .T. ) ;
#41872=CARTESIAN_POINT ( 'NONE',  ( 1.324344358081999795, -78.89373633638300021, 0.1571239973995999795 ) ) ;
#41903=CARTESIAN_POINT ( 'NONE',  ( -0.6744830649036911430, -82.24320892454605314, -1.051876958025935949 ) ) ;
#41931=CYLINDRICAL_SURFACE ( 'NONE', #41010, 1.500000000000000000 ) ;
#41941=CARTESIAN_POINT ( 'NONE',  ( -0.4635254915625000027, -82.00000000000000000, -1.426584774443000025 ) ) ;
#41943=CARTESIAN_POINT ( 'NONE',  ( -1.166489638287000030, -82.11937728024399519, 0.6163185517979000716 ) ) ;
#41958=FACE_OUTER_BOUND ( 'NONE', #42736, .T. ) ;
#41972=CARTESIAN_POINT ( 'NONE',  ( 1.449215700157000075, -78.20560097396669619, -0.7120307440141999678 ) ) ;
#41991=CARTESIAN_POINT ( 'NONE',  ( -1.250185882460489672, -77.76609322504926070, -0.2498302737146554653 ) ) ;
#42008=DIRECTION ( 'NONE',  ( -6.203993618971000339E-09, -1.000000000000000000, -6.182589629265999685E-10 ) ) ;
#42012=CARTESIAN_POINT ( 'NONE',  ( -1.199500263597270022, -79.55208333333332860, -0.9218200799623730290 ) ) ;
#42032=CARTESIAN_POINT ( 'NONE',  ( -1.393296160724000199, -81.61749198208599410, -0.2622693059933000059 ) ) ;
#42035=CARTESIAN_POINT ( 'NONE',  ( -1.199500263597274685, -81.94791666667777008, 0.9218200799623673669 ) ) ;
#42046=CARTESIAN_POINT ( 'NONE',  ( -0.7554284705563544255, -79.41666666666667140, 1.310679582531384169 ) ) ;
#42085=CARTESIAN_POINT ( 'NONE',  ( 0.08339889454722999862, -81.72327760821899290, 1.503976585945999922 ) ) ;
#42106=CONICAL_SURFACE ( 'NONE', #55293, 3.899999999992999733, 0.7853981633972997312 ) ;
#42142=CARTESIAN_POINT ( 'NONE',  ( -0.3926218265389190276, -77.60416666666667140, -1.460959015002473826 ) ) ;
#42171=CARTESIAN_POINT ( 'NONE',  ( 0.6284244718204999858, -78.34215887338820039, -1.176290284212999859 ) ) ;
#42187=ORIENTED_EDGE ( 'NONE', *, *, #25570, .T. ) ;
#42272=CARTESIAN_POINT ( 'NONE',  ( -0.7952960770845000082, -77.90792523368020284, 1.405246626978000180 ) ) ;
#42286=B_SPLINE_CURVE_WITH_KNOTS ( 'NONE', 3,
 ( #56413, #25392, #48425, #42838 ),
 .UNSPECIFIED., .F., .F.,
 ( 4, 4 ),
 ( 0.000000000000000000, 1.000000000000000000 ),
 .UNSPECIFIED. ) ;
#42290=CARTESIAN_POINT ( 'NONE',  ( -0.7111482236519753863, -78.67248581485152670, 1.058674648179741773 ) ) ;
#42300=CARTESIAN_POINT ( 'NONE',  ( -1.179157772963000061, -82.22698077501999592, 0.6230118014947999550 ) ) ;
#42311=CARTESIAN_POINT ( 'NONE',  ( -1.310679582531386611, -79.54166666666667140, -0.7554284705563495406 ) ) ;
#42331=CARTESIAN_POINT ( 'NONE',  ( -0.6748602203104000496, -81.95902128140700427, 1.357759211597000082 ) ) ;
#42334=VERTEX_POINT ( 'NONE', #28615 ) ;
#42339=CARTESIAN_POINT ( 'NONE',  ( 1.310679582531387943, -78.20833333333334281, -0.7554284705563468760 ) ) ;
#42347=CARTESIAN_POINT ( 'NONE',  ( -0.9218200799623775810, -79.42708333333334281, 1.199500263597266247 ) ) ;
#42361=CARTESIAN_POINT ( 'NONE',  ( 1.460959015002472494, -78.67083333333334849, 0.3926218265389232465 ) ) ;
#42381=CARTESIAN_POINT ( 'NONE',  ( -0.3849377561737999942, -82.01377306213599638, -1.557230663560999817 ) ) ;
#42387=CARTESIAN_POINT ( 'NONE',  ( -1.199500263597274241, -80.84791666666667709, 0.9218200799623669228 ) ) ;
#42401=EDGE_LOOP ( 'NONE', ( #25019, #8687, #6964, #13437 ) ) ;
#42409=VERTEX_POINT ( 'NONE', #32451 ) ;
#42411=ORIENTED_EDGE ( 'NONE', *, *, #57995, .T. ) ;
#42427=CARTESIAN_POINT ( 'NONE',  ( -1.000649921775999873, -79.66441203194099785, 0.8816325131470000853 ) ) ;
#42440=CARTESIAN_POINT ( 'NONE',  ( 1.221474390223999951, -81.35146937156800107, -0.5353283698298000326 ) ) ;
#42442=CARTESIAN_POINT ( 'NONE',  ( 1.371980222863132370, -79.21275704297983111, -0.7006253647128551920 ) ) ;
#42459=ORIENTED_EDGE ( 'NONE', *, *, #18529, .T. ) ;
#42464=CARTESIAN_POINT ( 'NONE',  ( -0.6568659331174000471, -78.05032173890430158, 1.160647793301999853 ) ) ;
#42531=CARTESIAN_POINT ( 'NONE',  ( 1.239259429943828650, -78.38146816523367022, -0.2975402487276854191 ) ) ;
#42551=CARTESIAN_POINT ( 'NONE',  ( 1.199500263597268246, -79.80208333333334281, 0.9218200799623752495 ) ) ;
#42561=CARTESIAN_POINT ( 'NONE',  ( 0.1747633057891999908, -77.85831261029910877, 1.605201443249000048 ) ) ;
#42569=DIRECTION ( 'NONE',  ( 0.000000000000000000, 1.000000000000000000, 0.000000000000000000 ) ) ;
#42580=CARTESIAN_POINT ( 'NONE',  ( 0.8554194063300312179, -78.43396144911410772, -0.9449817633163264397 ) ) ;
#42588=CARTESIAN_POINT ( 'NONE',  ( 0.03026270826137486547, -82.02290750955010878, 1.273738630170636599 ) ) ;
#42590=CARTESIAN_POINT ( 'NONE',  ( 1.221474390223999951, -81.48279142430399702, -0.5353283698298000326 ) ) ;
#42617=EDGE_LOOP ( 'NONE', ( #3902, #49880, #14929, #30180, #22405, #23850, #18141, #30816, #35989, #51052 ) ) ;
#42618=CARTESIAN_POINT ( 'NONE',  ( -0.7401269933634999632, -81.46289504759600675, 1.323311824859999986 ) ) ;
#42633=PLANE ( 'NONE',  #46135 ) ;
#42648=CARTESIAN_POINT ( 'NONE',  ( -0.1963495408493673156, -78.78541666666669130, 1.499999999999999556 ) ) ;
#42658=EDGE_CURVE ( 'NONE', #43048, #36029, #24613, .T. ) ;
#42668=CARTESIAN_POINT ( 'NONE',  ( 0.6676470363431000754, -82.24889682832498750, 1.458559589245999932 ) ) ;
#42688=EDGE_CURVE ( 'NONE', #11684, #18435, #45748, .T. ) ;
#42713=CARTESIAN_POINT ( 'NONE',  ( 1.323534079420999987, -79.91831375464900589, -0.1638099207045999872 ) ) ;
#42728=CARTESIAN_POINT ( 'NONE',  ( -1.417334032777999964, -79.02654225787900089, -0.4910847579886000736 ) ) ;
#42736=EDGE_LOOP ( 'NONE', ( #9059, #8407, #22903, #11321 ) ) ;
#42747=CARTESIAN_POINT ( 'NONE',  ( 0.3742884389835000047, -79.19216343900099275, -1.469294133937999902 ) ) ;
#42750=CARTESIAN_POINT ( 'NONE',  ( 0.000000000000000000, -75.67500000000001137, 0.000000000000000000 ) ) ;
#42752=CARTESIAN_POINT ( 'NONE',  ( -1.327706488546999797, -79.14179945328800159, -0.1249263990498000187 ) ) ;
#42775=CARTESIAN_POINT ( 'NONE',  ( -1.460959015002474493, -81.37916666666664867, 0.3926218265389144757 ) ) ;
#42781=CARTESIAN_POINT ( 'NONE',  ( -1.583750823903000038, -80.89244764574600310, 0.3147260902806000016 ) ) ;
#42807=FACE_OUTER_BOUND ( 'NONE', #31812, .T. ) ;
#42821=CARTESIAN_POINT ( 'NONE',  ( 1.224222772991306885, -78.92211854823271722, 0.3526872050934898861 ) ) ;
#42834=B_SPLINE_CURVE_WITH_KNOTS ( 'NONE', 3,
 ( #22054, #8482, #39772, #9078, #57786, #54252, #17341, #45104, #22949, #35331, #26476, #4052, #40063, #58080, #35627, #53656, #27065, #13196 ),
 .UNSPECIFIED., .F., .F.,
 ( 4, 2, 2, 2, 2, 2, 2, 2, 4 ),
 ( 0.000000000000000000, 0.1250000000000000000, 0.2500000000000000000, 0.3750000000000000000, 0.5000000000000000000, 0.6250000000000000000, 0.7500000000000000000, 0.8750000000000000000, 1.000000000000000000 ),
 .UNSPECIFIED. ) ;
#42835=ORIENTED_EDGE ( 'NONE', *, *, #42658, .F. ) ;
#42838=CARTESIAN_POINT ( 'NONE',  ( -0.6747260877994001316, -82.22962677363800310, -1.052256958371999840 ) ) ;
#42852=CARTESIAN_POINT ( 'NONE',  ( 0.6680689699263999692, -78.26673172604139950, -1.250497193771000104 ) ) ;
#42870=CARTESIAN_POINT ( 'NONE',  ( -1.172752930815400330, -77.78199484943172592, -0.4985573381714419883 ) ) ;
#42878=CARTESIAN_POINT ( 'NONE',  ( -0.07592439753940152802, -81.52996157210986894, 1.272577748247039953 ) ) ;
#42917=CARTESIAN_POINT ( 'NONE',  ( 1.460959015002474048, -78.22916666666667140, -0.3926218265389178064 ) ) ;
#42921=LINE ( 'NONE', #47365, #4934 ) ;
#42926=DIRECTION ( 'NONE',  ( 0.000000000000000000, 1.000000000000000000, 0.000000000000000000 ) ) ;
#42941=CARTESIAN_POINT ( 'NONE',  ( -1.500000000000000000, -78.89999999999999147, 0.000000000000000000 ) ) ;
#42988=EDGE_CURVE ( 'NONE', #46629, #4192, #43244, .T. ) ;
#42997=CARTESIAN_POINT ( 'NONE',  ( 1.250000000000000000, -76.29999999999999716, 0.000000000000000000 ) ) ;
#43004=CARTESIAN_POINT ( 'NONE',  ( -1.000649921775999873, -79.62063801436200094, 0.8816325131470000853 ) ) ;
#43006=DIRECTION ( 'NONE',  ( 0.000000000000000000, 0.000000000000000000, -1.000000000000000000 ) ) ;
#43018=CARTESIAN_POINT ( 'NONE',  ( -1.234140985588999984, -81.10340625466299969, 0.5054425604136000283 ) ) ;
#43019=CARTESIAN_POINT ( 'NONE',  ( 0.5951337072741889056, -79.15689260744959199, -1.420922764992056608 ) ) ;
#43039=DIRECTION ( 'NONE',  ( -1.000000000000000000, 0.000000000000000000, 0.000000000000000000 ) ) ;
#43045=ORIENTED_EDGE ( 'NONE', *, *, #9866, .F. ) ;
#43048=VERTEX_POINT ( 'NONE', #29355 ) ;
#43064=CARTESIAN_POINT ( 'NONE',  ( -1.310679582531389276, -78.35833333333332007, 0.7554284705563443225 ) ) ;
#43065=B_SPLINE_CURVE_WITH_KNOTS ( 'NONE', 3,
 ( #34497, #51962, #46965, #16227 ),
 .UNSPECIFIED., .F., .F.,
 ( 4, 4 ),
 ( 0.000000000000000000, 1.000000000000000000 ),
 .UNSPECIFIED. ) ;
#43093=CARTESIAN_POINT ( 'NONE',  ( -0.1746703279969999689, -78.35637572720449384, -1.307691051723000042 ) ) ;
#43113=CARTESIAN_POINT ( 'NONE',  ( -1.181111693982000110, -79.17654225787899236, -0.4092372983238000139 ) ) ;
#43128=ORIENTED_EDGE ( 'NONE', *, *, #18529, .F. ) ;
#43131=DIRECTION ( 'NONE',  ( 0.000000000000000000, -1.000000000000000000, 0.000000000000000000 ) ) ;
#43136=CARTESIAN_POINT ( 'NONE',  ( 0.9218200799623694763, -79.82291666666667140, 1.199500263597272465 ) ) ;
#43142=CARTESIAN_POINT ( 'NONE',  ( -1.141857967141000074, -79.78369273832200292, -0.6608524743567000259 ) ) ;
#43144=CARTESIAN_POINT ( 'NONE',  ( -1.509488703453999880, -79.05477463579200048, -0.1420306293263000064 ) ) ;
#43151=EDGE_CURVE ( 'NONE', #17252, #57807, #18196, .T. ) ;
#43155=VERTEX_POINT ( 'NONE', #39953 ) ;
#43162=CARTESIAN_POINT ( 'NONE',  ( 0.3994397004326888379, -78.10002733708165579, 1.210016675113110507 ) ) ;
#43170=CARTESIAN_POINT ( 'NONE',  ( 0.3166755616789259653, -81.00521267096443978, 1.233959662962462067 ) ) ;
#43191=CARTESIAN_POINT ( 'NONE',  ( -0.9820397338569999413, -80.80308451575899653, -0.7733679338621000099 ) ) ;
#43201=ORIENTED_EDGE ( 'NONE', *, *, #26460, .F. ) ;
#43210=CARTESIAN_POINT ( 'NONE',  ( 0.000000000000000000, -77.10000000000000853, 0.000000000000000000 ) ) ;
#43243=CARTESIAN_POINT ( 'NONE',  ( -0.1963495408493605987, -80.11458333333334281, -1.500000000000000444 ) ) ;
#43244=LINE ( 'NONE', #3377, #2153 ) ;
#43248=DIRECTION ( 'NONE',  ( 0.000000000000000000, 0.000000000000000000, -1.000000000000000000 ) ) ;
#43261=AXIS2_PLACEMENT_3D ( 'NONE', #57357, #4207, #30480 ) ;
#43283=FACE_OUTER_BOUND ( 'NONE', #14571, .T. ) ;
#43297=DIRECTION ( 'NONE',  ( -1.000000000000000000, 0.000000000000000000, 0.000000000000000000 ) ) ;
#43304=CARTESIAN_POINT ( 'NONE',  ( 1.460959015002474048, -77.72916666666668561, -0.3926218265389178064 ) ) ;
#43306=CARTESIAN_POINT ( 'NONE',  ( 0.3926218265389221362, -80.54583333333334849, -1.460959015002473160 ) ) ;
#43314=EDGE_CURVE ( 'NONE', #56774, #24789, #19869, .T. ) ;
#43315=FACE_OUTER_BOUND ( 'NONE', #25356, .T. ) ;
#43326=EDGE_LOOP ( 'NONE', ( #10685, #6276, #57191, #43895 ) ) ;
#43330=VERTEX_POINT ( 'NONE', #51466 ) ;
#43337=ORIENTED_EDGE ( 'NONE', *, *, #56544, .F. ) ;
#43405=AXIS2_PLACEMENT_3D ( 'NONE', #9892, #13425, #27874 ) ;
#43416=VERTEX_POINT ( 'NONE', #30150 ) ;
#43421=CARTESIAN_POINT ( 'NONE',  ( -1.312870888196999930, -79.73408011494099412, 0.1301370089704000088 ) ) ;
#43424=CARTESIAN_POINT ( 'NONE',  ( 1.066951212256000092, -78.36019790845671196, 1.077291633113999891 ) ) ;
#43443=CARTESIAN_POINT ( 'NONE',  ( 0.9950501885573103111, -79.05412480003177222, 0.7968050507756183620 ) ) ;
#43450=CARTESIAN_POINT ( 'NONE',  ( 1.078729748401755728, -81.35504527172810185, -0.6795942616195915775 ) ) ;
#43475=CARTESIAN_POINT ( 'NONE',  ( 0.000000000000000000, -75.67500000000001137, 0.000000000000000000 ) ) ;
#43526=AXIS2_PLACEMENT_3D ( 'NONE', #45889, #10156, #14564 ) ;
#43532=CARTESIAN_POINT ( 'NONE',  ( -2.299999999999999822, -76.00000000000000000, 0.000000000000000000 ) ) ;
#43544=CONICAL_SURFACE ( 'NONE', #28438, 3.399999999997999733, 0.9827937232471395390 ) ;
#43557=EDGE_CURVE ( 'NONE', #34809, #13233, #22847, .T. ) ;
#43568=B_SPLINE_CURVE_WITH_KNOTS ( 'NONE', 3,
 ( #17734, #31279, #27151, #4740 ),
 .UNSPECIFIED., .F., .F.,
 ( 4, 4 ),
 ( 0.000000000000000000, 1.000000000000000000 ),
 .UNSPECIFIED. ) ;
#43592=CARTESIAN_POINT ( 'NONE',  ( -0.4870599102559999838, -82.22795905130099925, -1.180149847382000017 ) ) ;
#43601=AXIS2_PLACEMENT_3D ( 'NONE', #9553, #27245, #49116 ) ;
#43605=CARTESIAN_POINT ( 'NONE',  ( -1.307405465782000009, -81.23633620685998835, 0.09225987258616000219 ) ) ;
#43611=CARTESIAN_POINT ( 'NONE',  ( -1.419358333703000019, -79.04332556885799477, 0.07120080608633000407 ) ) ;
#43664=CARTESIAN_POINT ( 'NONE',  ( 0.9283799206808001081, -78.55482622072899801, 0.9373773696604000838 ) ) ;
#43690=VERTEX_POINT ( 'NONE', #22758 ) ;
#43715=B_SPLINE_CURVE_WITH_KNOTS ( 'NONE', 3,
 ( #28412, #37867, #32836, #10730, #55888, #23125, #1879, #46459, #36698, #28709, #41717, #19288, #27829, #50883, #1293, #37278, #19572, #54715 ),
 .UNSPECIFIED., .F., .F.,
 ( 4, 2, 2, 2, 2, 2, 2, 2, 4 ),
 ( 0.000000000000000000, 0.1250000000000000833, 0.2500000000000001665, 0.3750000000000001665, 0.5000000000000002220, 0.6250000000000002220, 0.7500000000000001110, 0.8750000000000001110, 1.000000000000000000 ),
 .UNSPECIFIED. ) ;
#43716=CARTESIAN_POINT ( 'NONE',  ( -1.250000000000000000, -82.25000000000000000, 8.279869130157999738E-11 ) ) ;
#43720=CARTESIAN_POINT ( 'NONE',  ( 0.2147767365671000017, -80.43441590662199303, -1.401402989476999927 ) ) ;
#43722=CARTESIAN_POINT ( 'NONE',  ( -1.265160441076000009, -79.08784971804600161, -0.7115061034973000353 ) ) ;
#43724=DIRECTION ( 'NONE',  ( 0.000000000000000000, 0.000000000000000000, -1.000000000000000000 ) ) ;
#43727=DIRECTION ( 'NONE',  ( 0.000000000000000000, 1.000000000000000000, 0.000000000000000000 ) ) ;
#43747=CARTESIAN_POINT ( 'NONE',  ( -1.222766595631025854, -81.67307490878640408, -0.3613108255141002645 ) ) ;
#43774=EDGE_LOOP ( 'NONE', ( #24253, #31768, #30535, #4040 ) ) ;
#43781=CARTESIAN_POINT ( 'NONE',  ( 1.500000000000000000, -81.76041666666726826, 0.1963495408493652339 ) ) ;
#43851=ORIENTED_EDGE ( 'NONE', *, *, #35602, .T. ) ;
#43881=EDGE_CURVE ( 'NONE', #22868, #17863, #19303, .T. ) ;
#43885=CARTESIAN_POINT ( 'NONE',  ( -0.5176806821990824758, -80.34214269217306992, -1.165494644203259655 ) ) ;
#43889=CARTESIAN_POINT ( 'NONE',  ( -0.9657971644277000278, -82.19488396904600336, -0.9195906491977999808 ) ) ;
#43895=ORIENTED_EDGE ( 'NONE', *, *, #36248, .T. ) ;
#43904=CARTESIAN_POINT ( 'NONE',  ( -1.260178996155999931, -80.14056234758800201, -0.6496216418182000352 ) ) ;
#43923=CARTESIAN_POINT ( 'NONE',  ( 1.179993905018462241, -79.43096596752555172, 0.4803374300081332260 ) ) ;
#43926=CARTESIAN_POINT ( 'NONE',  ( 0.9218200799623692543, -78.22291666666664867, 1.199500263597272687 ) ) ;
#43940=B_SPLINE_CURVE_WITH_KNOTS ( 'NONE', 3,
 ( #44205, #54236, #40356, #27053, #53346, #26187, #17927, #53947, #57773, #30607, #13772, #26464, #13482, #22043, #45090, #4642 ),
 .UNSPECIFIED., .F., .F.,
 ( 4, 2, 2, 2, 2, 2, 2, 4 ),
 ( 0.2857224320369311510, 0.3750071280323146738, 0.4642918240276981967, 0.5535765200230817751, 0.6428612160184652424, 0.8214306080092326212, 0.9107153040046163106, 1.000000000000000000 ),
 .UNSPECIFIED. ) ;
#43943=CARTESIAN_POINT ( 'NONE',  ( 0.3098463080081999554, -79.21130845337700066, 1.484230999220000013 ) ) ;
#43944=CARTESIAN_POINT ( 'NONE',  ( -0.3926218265389190276, -78.60416666666667140, -1.460959015002473826 ) ) ;
#43950=CARTESIAN_POINT ( 'NONE',  ( 0.6216730717741000278, -78.40598835058560212, -1.163652956044999964 ) ) ;
#43966=ORIENTED_EDGE ( 'NONE', *, *, #17405, .T. ) ;
#44002=CARTESIAN_POINT ( 'NONE',  ( 1.187026915874999755, -80.52788208903798761, 0.5757885860275999690 ) ) ;
#44009=CARTESIAN_POINT ( 'NONE',  ( -1.181111693982000110, -79.17654225787899236, -0.4092372983238000139 ) ) ;
#44072=CARTESIAN_POINT ( 'NONE',  ( -1.500000000000000000, -78.00000000000000000, 0.000000000000000000 ) ) ;
#44094=CARTESIAN_POINT ( 'NONE',  ( -0.5900578684300998855, -82.25488867623700173, -1.108170840844000082 ) ) ;
#44107=DIRECTION ( 'NONE',  ( -1.224058225713999994E-08, -0.9999999999999998890, 4.602708956829999399E-10 ) ) ;
#44120=CARTESIAN_POINT ( 'NONE',  ( -0.3926218265389255779, -78.89583333333335702, 1.460959015002472494 ) ) ;
#44144=ORIENTED_EDGE ( 'NONE', *, *, #50116, .T. ) ;
#44147=B_SPLINE_CURVE_WITH_KNOTS ( 'NONE', 3,
 ( #27696, #8825, #5558, #44841, #31529, #9417, #40409, #17981, #4983, #53997, #54585, #13538, #13832, #49576, #9123, #45147, #27406, #4698 ),
 .UNSPECIFIED., .F., .F.,
 ( 4, 2, 2, 2, 2, 2, 2, 2, 4 ),
 ( 0.000000000000000000, 0.1250000000000000000, 0.2500000000000000000, 0.3750000000000000000, 0.5000000000000000000, 0.6250000000000000000, 0.7500000000000000000, 0.8750000000000000000, 1.000000000000000000 ),
 .UNSPECIFIED. ) ;
#44155=ADVANCED_FACE ( 'NONE', ( #21324 ), #39332, .T. ) ;
#44171=CARTESIAN_POINT ( 'NONE',  ( 0.8471236057751000414, -81.04211641967700075, 1.030027924806000028 ) ) ;
#44180=CARTESIAN_POINT ( 'NONE',  ( -1.500000000000000000, -80.40000000000000568, 0.000000000000000000 ) ) ;
#44188=CARTESIAN_POINT ( 'NONE',  ( -1.063776463958000074, -79.54521086701498689, 0.9372507776557998938 ) ) ;
#44205=CARTESIAN_POINT ( 'NONE',  ( -1.499934128473817241, -81.90004407876089942, 2.109063419893342596E-06 ) ) ;
#44223=CARTESIAN_POINT ( 'NONE',  ( -0.9234216768726070113, -80.80927045197968539, -0.8478083823816136011 ) ) ;
#44227=CARTESIAN_POINT ( 'NONE',  ( 1.118108678836999825, -79.16169582999499710, 1.024097206608999944 ) ) ;
#44252=CARTESIAN_POINT ( 'NONE',  ( 0.7554284705563509839, -78.56666666666666288, -1.310679582531386167 ) ) ;
#44267=VERTEX_POINT ( 'NONE', #44637 ) ;
#44269=CYLINDRICAL_SURFACE ( 'NONE', #6522, 1.500000000000000000 ) ;
#44281=CARTESIAN_POINT ( 'NONE',  ( -0.5412065714428999641, -79.83330536170299752, -1.203187872875000064 ) ) ;
#44284=CARTESIAN_POINT ( 'NONE',  ( -1.197912192620000038, -78.12365292024510666, 0.5527856627588000338 ) ) ;
#44302=CARTESIAN_POINT ( 'NONE',  ( 0.06739636946983651455, -78.87920693182361731, -1.272432065101433807 ) ) ;
#44331=LINE ( 'NONE', #44630, #17955 ) ;
#44343=CARTESIAN_POINT ( 'NONE',  ( 1.500000000000000000, -79.65000000000000568, 0.000000000000000000 ) ) ;
#44352=B_SPLINE_CURVE_WITH_KNOTS ( 'NONE', 3,
 ( #2622, #56636, #11764, #29741, #47793, #7325, #1367, #32912, #1660, #2242, #1958, #19074, #19951, #42387, #55666, #19363, #15215, #37939 ),
 .UNSPECIFIED., .F., .F.,
 ( 4, 2, 2, 2, 2, 2, 2, 2, 4 ),
 ( 0.000000000000000000, 0.1249999999999999722, 0.2499999999999999445, 0.3749999999999998890, 0.4999999999999998890, 0.6249999999999998890, 0.7499999999999997780, 0.8749999999999998890, 1.000000000000000000 ),
 .UNSPECIFIED. ) ;
#44411=CARTESIAN_POINT ( 'NONE',  ( -0.9950304368180999948, -80.56410876238999208, -1.271568498479000109 ) ) ;
#44426=ORIENTED_EDGE ( 'NONE', *, *, #55841, .F. ) ;
#44430=CARTESIAN_POINT ( 'NONE',  ( 0.3292142484335000563, -79.41051030923300402, -1.292352404326999826 ) ) ;
#44439=B_SPLINE_CURVE_WITH_KNOTS ( 'NONE', 3,
 ( #48573, #39414, #40582, #12823, #12541, #45314, #8997, #26981, #179, #31104, #35845, #18152, #53874, #26396, #53276, #54162, #8115, #4271 ),
 .UNSPECIFIED., .F., .F.,
 ( 4, 2, 2, 2, 2, 2, 2, 2, 4 ),
 ( 0.000000000000000000, 0.1250000000000000833, 0.2500000000000001665, 0.3750000000000001665, 0.5000000000000002220, 0.6250000000000002220, 0.7500000000000001110, 0.8750000000000001110, 1.000000000000000000 ),
 .UNSPECIFIED. ) ;
#44447=CARTESIAN_POINT ( 'NONE',  ( 1.180314793947099261, -79.53115984866582266, 0.4804541877614367240 ) ) ;
#44451=CARTESIAN_POINT ( 'NONE',  ( 1.304222966381000104, -81.44485601252800677, 0.2785293583740000023 ) ) ;
#44452=AXIS2_PLACEMENT_3D ( 'NONE', #20842, #38846, #52436 ) ;
#44461=CARTESIAN_POINT ( 'NONE',  ( 0.1719131973598000129, -81.37741046657400545, -1.299333209432999903 ) ) ;
#44466=CARTESIAN_POINT ( 'NONE',  ( -0.5179932711920000044, -79.19792250334801054, -1.319781611125000031 ) ) ;
#44484=LINE ( 'NONE', #53945, #11033 ) ;
#44486=CARTESIAN_POINT ( 'NONE',  ( 1.406250000003000045, -82.09374999999700151, -9.314605757769000352E-11 ) ) ;
#44489=CARTESIAN_POINT ( 'NONE',  ( 1.219314106501412365, -79.87620745940748179, -0.3721447959605043154 ) ) ;
#44514=CARTESIAN_POINT ( 'NONE',  ( 1.190716386653000169, -79.21706751772300947, 1.090600000265000036 ) ) ;
#44521=CARTESIAN_POINT ( 'NONE',  ( -0.7468003766476000171, -78.26866860913609969, 1.319557257415000073 ) ) ;
#44539=DIRECTION ( 'NONE',  ( -1.000000000000000000, 0.000000000000000000, 0.000000000000000000 ) ) ;
#44541=CARTESIAN_POINT ( 'NONE',  ( -1.460959015002473826, -78.42083333333336270, -0.3926218265389207485 ) ) ;
#44570=CARTESIAN_POINT ( 'NONE',  ( -0.9967936402423711595, -82.25000000000000000, -0.7825337139414764165 ) ) ;
#44574=CARTESIAN_POINT ( 'NONE',  ( -1.356492273396000092, -79.45368156769499990, -0.8757286844311999996 ) ) ;
#44577=CARTESIAN_POINT ( 'NONE',  ( -1.169594621339999918, -78.61977915405600470, 0.6104211924069999906 ) ) ;
#44584=B_SPLINE_CURVE_WITH_KNOTS ( 'NONE', 3,
 ( #49573, #22692, #14122, #36560, #22394, #40997, #45437, #54292, #589, #36847 ),
 .UNSPECIFIED., .F., .F.,
 ( 4, 2, 2, 2, 4 ),
 ( 0.000000000000000000, 0.2499999999999998890, 0.4999999999999998890, 0.7499999999999998890, 1.000000000000000000 ),
 .UNSPECIFIED. ) ;
#44597=CARTESIAN_POINT ( 'NONE',  ( 0.8120539164135156529, -79.07002642441428009, 0.9822165099403028510 ) ) ;
#44602=EDGE_CURVE ( 'NONE', #57807, #43416, #29618, .T. ) ;
#44630=CARTESIAN_POINT ( 'NONE',  ( -1.500000000000000000, -75.67500000000001137, 0.000000000000000000 ) ) ;
#44637=CARTESIAN_POINT ( 'NONE',  ( 4.000000000000000000, -77.29999999999999716, 0.000000000000000000 ) ) ;
#44640=ORIENTED_EDGE ( 'NONE', *, *, #16504, .F. ) ;
#44652=FACE_OUTER_BOUND ( 'NONE', #57929, .T. ) ;
#44712=CARTESIAN_POINT ( 'NONE',  ( 1.025649293883999835, -80.81217187929600243, 1.247099486493999931 ) ) ;
#44731=CARTESIAN_POINT ( 'NONE',  ( 0.5765222740522000233, -80.06131301898899721, 1.202579817323000233 ) ) ;
#44747=CARTESIAN_POINT ( 'NONE',  ( -0.7342790699846932778, -79.67427446810803815, 1.041378959097729817 ) ) ;
#44752=CARTESIAN_POINT ( 'NONE',  ( 0.7341740840635999632, -80.84950453195499165, -1.113348630318000021 ) ) ;
#44763=CARTESIAN_POINT ( 'NONE',  ( -0.9429895430810999457, -80.92385680317599395, -1.174528710654999974 ) ) ;
#44769=CARTESIAN_POINT ( 'NONE',  ( -0.6885369103866999518, -80.13480328324099844, -1.350873448928000098 ) ) ;
#44790=CARTESIAN_POINT ( 'NONE',  ( 0.4801485855953882553, -80.30554746943639088, -1.179926170174790512 ) ) ;
#44815=CARTESIAN_POINT ( 'NONE',  ( -0.2137776359178999996, -78.52249079038800517, -1.600472757759999753 ) ) ;
#44822=CARTESIAN_POINT ( 'NONE',  ( -1.472799192485999997, -77.87176762208750347, -0.3599880333205999761 ) ) ;
#44841=CARTESIAN_POINT ( 'NONE',  ( -1.310679582531386389, -81.44166666666667709, -0.7554284705563492075 ) ) ;
#44853=SURFACE_STYLE_FILL_AREA ( #13248 ) ;
#44856=ORIENTED_EDGE ( 'NONE', *, *, #19298, .F. ) ;
#44876=CARTESIAN_POINT ( 'NONE',  ( 0.3219823053856999961, -80.04903304826798660, -1.582258297802999980 ) ) ;
#44878=CARTESIAN_POINT ( 'NONE',  ( -0.1746703279969999689, -78.27249079038830359, -1.307691051723000042 ) ) ;
#44883=CARTESIAN_POINT ( 'NONE',  ( 0.000000000000000000, -76.29999999999999716, 0.000000000000000000 ) ) ;
#44917=CARTESIAN_POINT ( 'NONE',  ( 1.500000000000000000, -78.25000000000000000, 0.000000000000000000 ) ) ;
#44948=( LENGTH_UNIT ( ) NAMED_UNIT ( * ) SI_UNIT ( .MILLI., .METRE. ) );
#44998=CARTESIAN_POINT ( 'NONE',  ( -1.250000000000000000, -77.64999999999999147, 0.000000000000000000 ) ) ;
#45019=CARTESIAN_POINT ( 'NONE',  ( 0.9218200799623692543, -80.22291666666664867, 1.199500263597272687 ) ) ;
#45028=CARTESIAN_POINT ( 'NONE',  ( -0.1698911186725000078, -80.60705187618100354, 1.322768475116000042 ) ) ;
#45045=CARTESIAN_POINT ( 'NONE',  ( -0.9420598709024999851, -79.27896011182599523, -0.8215979549846998964 ) ) ;
#45050=CARTESIAN_POINT ( 'NONE',  ( 1.274147325018575971, -80.50115893599860328, 0.01855956267719174532 ) ) ;
#45055=CARTESIAN_POINT ( 'NONE',  ( 1.316231252753000014, -82.02853028149598913, 0.2147359707272000207 ) ) ;
#45064=CARTESIAN_POINT ( 'NONE',  ( -1.111488374662999989, -81.24468314134999503, 0.8650934752202000810 ) ) ;
#45070=CARTESIAN_POINT ( 'NONE',  ( -1.312293291923000149, -79.58906442605000109, -0.7594922433479999180 ) ) ;
#45090=CARTESIAN_POINT ( 'NONE',  ( 1.499741147044569178, -81.66063338586604914, 0.1964284907518392131 ) ) ;
#45094=CARTESIAN_POINT ( 'NONE',  ( 1.500000000000000000, -81.75000000000000000, 0.000000000000000000 ) ) ;
#45104=CARTESIAN_POINT ( 'NONE',  ( -0.3926218265389189721, -80.00416666666666288, -1.460959015002473604 ) ) ;
#45113=CARTESIAN_POINT ( 'NONE',  ( 0.3565886142880393406, -81.10348178115825135, 1.276299026773298317 ) ) ;
#45116=CARTESIAN_POINT ( 'NONE',  ( -1.499999999985999866, -82.00000000001401190, -1.019196462549000076E-10 ) ) ;
#45119=APPLICATION_CONTEXT ( 'automotive_design' ) ;
#45122=CARTESIAN_POINT ( 'NONE',  ( 0.7608607662309999631, -78.57210341376899976, -1.424185669224000028 ) ) ;
#45127=CARTESIAN_POINT ( 'NONE',  ( 0.7554284705563452107, -79.73333333333330586, 1.310679582531388609 ) ) ;
#45128=CARTESIAN_POINT ( 'NONE',  ( 0.1534498121882000021, -78.16368429802710693, 1.409436946036999760 ) ) ;
#45146=CARTESIAN_POINT ( 'NONE',  ( 0.000000000000000000, -76.15000000005198899, -2.149999999947999729 ) ) ;
#45147=CARTESIAN_POINT ( 'NONE',  ( 1.460959015002474493, -81.62916666666667709, -0.3926218265389176953 ) ) ;
#45156=AXIS2_PLACEMENT_3D ( 'NONE', #6749, #18161, #41165 ) ;
#45177=CARTESIAN_POINT ( 'NONE',  ( -1.597158643424000157, -80.39632141193499137, 0.2372724044997999993 ) ) ;
#45178=CARTESIAN_POINT ( 'NONE',  ( -1.138524516885000004, -79.11590538786700222, 0.6666316858816999646 ) ) ;
#45200=CARTESIAN_POINT ( 'NONE',  ( -0.8849062459890528753, -82.21372529178493949, -0.9173043153348533485 ) ) ;
#45223=EDGE_CURVE ( 'NONE', #5279, #29318, #41399, .T. ) ;
#45274=ORIENTED_EDGE ( 'NONE', *, *, #15972, .F. ) ;
#45298=CARTESIAN_POINT ( 'NONE',  ( 1.232424253006426884, -77.92032519149937286, 0.3249715972912227135 ) ) ;
#45308=CARTESIAN_POINT ( 'NONE',  ( 1.085118080231999960, -81.30829811310599098, 1.195714296125000020 ) ) ;
#45314=CARTESIAN_POINT ( 'NONE',  ( -0.9218200799623775810, -78.42708333333332860, 1.199500263597266247 ) ) ;
#45323=CARTESIAN_POINT ( 'NONE',  ( 0.2659376973789999710, -79.86286252546500464, -1.306848610430999980 ) ) ;
#45338=CARTESIAN_POINT ( 'NONE',  ( -1.150888948972000003, -79.17973486506399183, 0.6738713386821000295 ) ) ;
#45347=CARTESIAN_POINT ( 'NONE',  ( -1.321095329625999959, -82.27659339840100472, -0.1826337427822999904 ) ) ;
#45358=CARTESIAN_POINT ( 'NONE',  ( -1.221962791321999919, -81.33873264782599222, -0.7004284825205000509 ) ) ;
#45365=CARTESIAN_POINT ( 'NONE',  ( 0.6275421466605000109, -80.49360977560299091, 1.160498354042999836 ) ) ;
#45371=ORIENTED_EDGE ( 'NONE', *, *, #4364, .T. ) ;
#45386=DIRECTION ( 'NONE',  ( 0.000000000000000000, 1.000000000000000000, 0.000000000000000000 ) ) ;
#45388=ORIENTED_EDGE ( 'NONE', *, *, #54890, .F. ) ;
#45392=CARTESIAN_POINT ( 'NONE',  ( -0.9503192246700015167, -80.59177414278872220, 0.8489797128931024783 ) ) ;
#45421=CARTESIAN_POINT ( 'NONE',  ( -0.9218200799623778030, -79.82708333333334849, 1.199500263597266914 ) ) ;
#45422=CARTESIAN_POINT ( 'NONE',  ( -0.5750548074078000171, -79.20554938902999709, 1.295897153995000162 ) ) ;
#45437=CARTESIAN_POINT ( 'NONE',  ( -0.1250341999720060160, -80.61872301050603085, -1.526447402715753965 ) ) ;
#45439=LINE ( 'NONE', #45146, #37505 ) ;
#45470=CARTESIAN_POINT ( 'NONE',  ( -1.511528582562000178, -79.40406894431399110, 0.07582444189424000780 ) ) ;
#45484=VECTOR ( 'NONE', #28158, 1000.000000000000000 ) ;
#45516=LINE ( 'NONE', #1232, #36498 ) ;
#45537=ORIENTED_EDGE ( 'NONE', *, *, #11017, .F. ) ;
#45539=ORIENTED_EDGE ( 'NONE', *, *, #30024, .T. ) ;
#45546=FACE_OUTER_BOUND ( 'NONE', #50379, .T. ) ;
#45596=AXIS2_PLACEMENT_3D ( 'NONE', #4394, #40405, #13533 ) ;
#45601=ORIENTED_EDGE ( 'NONE', *, *, #30799, .T. ) ;
#45603=EDGE_LOOP ( 'NONE', ( #21815, #7178, #52415, #50244 ) ) ;
#45635=CARTESIAN_POINT ( 'NONE',  ( -0.1765672563250000049, -78.33632026758570532, -1.321892640673999919 ) ) ;
#45645=CARTESIAN_POINT ( 'NONE',  ( -0.2317941695893000198, -82.37581864516299390, -1.228320586388000013 ) ) ;
#45654=CARTESIAN_POINT ( 'NONE',  ( -1.155705185623000064, -82.27088077809300160, -0.4398327176956999818 ) ) ;
#45660=CARTESIAN_POINT ( 'NONE',  ( -1.500000000000000888, -81.48958333333335702, 0.1963495408493559080 ) ) ;
#45720=CARTESIAN_POINT ( 'NONE',  ( -1.488622005431999851, -78.36789385589818835, -0.2880046469693999800 ) ) ;
#45728=CARTESIAN_POINT ( 'NONE',  ( 1.310679582531387943, -81.70833333333332860, -0.7554284705563468760 ) ) ;
#45743=VECTOR ( 'NONE', #56984, 1000.000000000000000 ) ;
#45748=B_SPLINE_CURVE_WITH_KNOTS ( 'NONE', 3,
 ( #2727, #2436, #47323, #25435, #20723, #38722, #15712, #20153, #25145, #56450, #20437, #52031, #3011, #43170, #56163, #7719, #16302, #24571, #52315, #21292, #51745, #33706, #16874, #11295, #29275, #28992, #25722, #6852, #43450, #33993, #7433, #48187, #24862, #30137, #42878, #56743, #2151, #47033, #39299, #38433, #43747, #3299, #12152, #51455, #29849, #16005, #38140, #11585, #57310, #29563, #47618, #7142, #11008, #6563, #34568, #42588, #21006, #34280, #11871, #39012, #57021, #16582, #52600, #45200, #13000 ),
 .UNSPECIFIED., .F., .F.,
 ( 4, 2, 2, 2, 2, 2, 2, 2, 2, 2, 2, 2, 2, 2, 2, 2, 1, 2, 2, 2, 2, 2, 2, 2, 2, 2, 2, 2, 2, 2, 2, 2, 4 ),
 ( 0.000000000000000000, 0.03125000000000006245, 0.06250000000000012490, 0.09375000000000019429, 0.1250000000000002220, 0.1562500000000002776, 0.1875000000000003331, 0.2187500000000004163, 0.2500000000000004441, 0.2812500000000004996, 0.3125000000000005551, 0.3437500000000005551, 0.3750000000000005551, 0.4062500000000006106, 0.4375000000000006106, 0.4687500000000006106, 0.5000000000000005551, 0.5312500000000006661, 0.5625000000000006661, 0.5937500000000007772, 0.6250000000000006661, 0.6562500000000006661, 0.6875000000000005551, 0.7187500000000005551, 0.7500000000000004441, 0.7812500000000004441, 0.8125000000000004441, 0.8437500000000003331, 0.8750000000000003331, 0.9062500000000002220, 0.9375000000000002220, 0.9687500000000001110, 1.000000000000000000 ),
 .UNSPECIFIED. ) ;
#45767=CARTESIAN_POINT ( 'NONE',  ( 0.6263439973055000554, -79.75135730798099587, 1.488256452092999949 ) ) ;
#45773=CARTESIAN_POINT ( 'NONE',  ( -1.250000000000000000, -77.10000000000000853, -0.5000000000000000000 ) ) ;
#45807=CARTESIAN_POINT ( 'NONE',  ( 0.7262865762285000137, -80.82944907233598997, -1.101387507969000090 ) ) ;
#45824=AXIS2_PLACEMENT_3D ( 'NONE', #50421, #46000, #4953 ) ;
#45838=CARTESIAN_POINT ( 'NONE',  ( 1.592284932317999946, -78.25521359734770499, 0.2680347371437999948 ) ) ;
#45840=DIRECTION ( 'NONE',  ( -1.000000000000000000, 0.000000000000000000, 0.000000000000000000 ) ) ;
#45874=CIRCLE ( 'NONE', #55290, 4.000000000000000000 ) ;
#45889=CARTESIAN_POINT ( 'NONE',  ( 0.000000000000000000, 0.000000000000000000, 0.000000000000000000 ) ) ;
#45894=CARTESIAN_POINT ( 'NONE',  ( 1.324686507300999905, -80.82369000798900061, -0.5052412751467000307 ) ) ;
#45923=VECTOR ( 'NONE', #21187, 1000.000000000000000 ) ;
#45928=CARTESIAN_POINT ( 'NONE',  ( 1.196963559360000096, -78.47931953192639298, -0.5880938590690999446 ) ) ;
#45946=CARTESIAN_POINT ( 'NONE',  ( 1.215992416571999968, -82.05245088088400962, -0.8889676458159999628 ) ) ;
#45953=CARTESIAN_POINT ( 'NONE',  ( 0.1998609718125000101, -80.29515928207800357, -1.304078681214000168 ) ) ;
#45960=VERTEX_POINT ( 'NONE', #13399 ) ;
#45964=CONICAL_SURFACE ( 'NONE', #21407, 3.399999999997999733, 0.9827937232471395390 ) ;
#45990=CARTESIAN_POINT ( 'NONE',  ( 0.9336649615752000697, -80.32105334749999770, -0.9522845488932000224 ) ) ;
#46000=DIRECTION ( 'NONE',  ( 0.000000000000000000, 1.000000000000000000, 0.000000000000000000 ) ) ;
#46031=ADVANCED_FACE ( 'NONE', ( #53565 ), #2956, .F. ) ;
#46034=CARTESIAN_POINT ( 'NONE',  ( 1.310679582531388387, -78.60833333333333428, -0.7554284705563470981 ) ) ;
#46102=CARTESIAN_POINT ( 'NONE',  ( 1.208351632240000084, -81.37518792952799629, -0.5295771361605000616 ) ) ;
#46133=FACE_OUTER_BOUND ( 'NONE', #22098, .T. ) ;
#46135=AXIS2_PLACEMENT_3D ( 'NONE', #43210, #42926, #1615 ) ;
#46158=VERTEX_POINT ( 'NONE', #46514 ) ;
#46182=CARTESIAN_POINT ( 'NONE',  ( -0.9218200799623714747, -77.97291666666667709, -1.199500263597270466 ) ) ;
#46183=VERTEX_POINT ( 'NONE', #15190 ) ;
#46192=CARTESIAN_POINT ( 'NONE',  ( 1.399266414090999833, -81.86555509899200445, 0.2282827057232000301 ) ) ;
#46195=CARTESIAN_POINT ( 'NONE',  ( -1.500000000000000888, -81.98958333334674364, 0.1963495408493559080 ) ) ;
#46224=CARTESIAN_POINT ( 'NONE',  ( -1.112801787005999854, -79.26242257069900177, -0.6258220204580999813 ) ) ;
#46240=CARTESIAN_POINT ( 'NONE',  ( -1.520492615867999886, -82.42132092353099893, -0.2596922552208000279 ) ) ;
#46246=CARTESIAN_POINT ( 'NONE',  ( -0.1680659145979999936, -80.54322239898399971, 1.308557476745999981 ) ) ;
#46256=DIRECTION ( 'NONE',  ( 0.000000000000000000, 0.000000000000000000, -1.000000000000000000 ) ) ;
#46257=ORIENTED_EDGE ( 'NONE', *, *, #44602, .T. ) ;
#46258=EDGE_CURVE ( 'NONE', #19498, #46158, #49022, .T. ) ;
#46284=FACE_OUTER_BOUND ( 'NONE', #29346, .T. ) ;
#46292=CARTESIAN_POINT ( 'NONE',  ( 1.324099017018209867, -81.99695209267724749, -0.05344395349994826572 ) ) ;
#46305=CARTESIAN_POINT ( 'NONE',  ( -1.199500263597270022, -80.05208333333334281, -0.9218200799623730290 ) ) ;
#46320=DIRECTION ( 'NONE',  ( 1.000000000000000000, 0.000000000000000000, 0.000000000000000000 ) ) ;
#46324=CARTESIAN_POINT ( 'NONE',  ( 1.324344358081999795, -78.93751035396100235, 0.1571239973995999795 ) ) ;
#46328=EDGE_CURVE ( 'NONE', #10831, #22736, #53265, .T. ) ;
#46378=LINE ( 'NONE', #23911, #50310 ) ;
#46393=CARTESIAN_POINT ( 'NONE',  ( -0.5872121148612000630, -82.06976465686300060, 1.181418957762000010 ) ) ;
#46421=CARTESIAN_POINT ( 'NONE',  ( -1.393431170853000056, -78.94979032468299351, 0.8158852592188999830 ) ) ;
#46428=ADVANCED_FACE ( 'NONE', ( #8948 ), #2383, .F. ) ;
#46440=CARTESIAN_POINT ( 'NONE',  ( 1.088860609755996744, -77.95691271763917030, -0.6622528567310277392 ) ) ;
#46459=CARTESIAN_POINT ( 'NONE',  ( -0.3926218265389255779, -80.39583333333335702, 1.460959015002472494 ) ) ;
#46482=CARTESIAN_POINT ( 'NONE',  ( 0.6617453507451001027, -81.76632985222998684, -1.253855045949999969 ) ) ;
#46499=CARTESIAN_POINT ( 'NONE',  ( -1.460959015002474937, -79.47916666666667140, 0.3926218265389144757 ) ) ;
#46514=CARTESIAN_POINT ( 'NONE',  ( -1.500000000000000000, -78.89999999999999147, 0.000000000000000000 ) ) ;
#46515=CARTESIAN_POINT ( 'NONE',  ( -1.182296476285000120, -78.72738264883200543, 0.6170503964917000150 ) ) ;
#46531=B_SPLINE_CURVE_WITH_KNOTS ( 'NONE', 3,
 ( #49248, #39789, #3221, #8499, #48668, #57802, #3498, #40081, #58097, #48105, #21501, #53673, #52802, #13213, #31208, #8798, #57512, #21208 ),
 .UNSPECIFIED., .F., .F.,
 ( 4, 2, 2, 2, 2, 2, 2, 2, 4 ),
 ( 0.000000000000000000, 0.1250000000000000833, 0.2500000000000001665, 0.3750000000000001665, 0.5000000000000002220, 0.6250000000000002220, 0.7500000000000001110, 0.8750000000000001110, 1.000000000000000000 ),
 .UNSPECIFIED. ) ;
#46536=CARTESIAN_POINT ( 'NONE',  ( -1.029597909886999840, -82.28757464707300073, 1.099498802994000046 ) ) ;
#46578=CARTESIAN_POINT ( 'NONE',  ( 0.9788970803261000109, -79.82492711368898597, -0.9057243817226000582 ) ) ;
#46605=CARTESIAN_POINT ( 'NONE',  ( -1.460959015002473382, -81.52083333333332860, -0.3926218265389205819 ) ) ;
#46617=CARTESIAN_POINT ( 'NONE',  ( -0.5996107393304999089, -78.59022199029399758, 1.191235959310000148 ) ) ;
#46629=VERTEX_POINT ( 'NONE', #10648 ) ;
#46635=ADVANCED_FACE ( 'NONE', ( #42807 ), #41931, .T. ) ;
#46640=AXIS2_PLACEMENT_3D ( 'NONE', #23003, #41014, #606 ) ;
#46699=CARTESIAN_POINT ( 'NONE',  ( 0.000000000000000000, -76.15000000005198899, 0.000000000000000000 ) ) ;
#46716=CARTESIAN_POINT ( 'NONE',  ( 1.250000000000000000, -77.10000000000000853, 0.000000000000000000 ) ) ;
#46747=CARTESIAN_POINT ( 'NONE',  ( 0.9432352957733999288, -82.07814290487699793, 0.9428059748164999698 ) ) ;
#46772=CARTESIAN_POINT ( 'NONE',  ( 0.7554284705563509839, -78.06666666666669130, -1.310679582531386167 ) ) ;
#46779=CARTESIAN_POINT ( 'NONE',  ( -1.474644042471999983, -81.06599406054799317, -0.3526571989726999812 ) ) ;
#46785=CARTESIAN_POINT ( 'NONE',  ( 1.199500263597271799, -78.19791666666667140, -0.9218200799623701425 ) ) ;
#46790=ORIENTED_EDGE ( 'NONE', *, *, #56491, .F. ) ;
#46807=CARTESIAN_POINT ( 'NONE',  ( 1.310679582531385501, -78.69166666666669130, 0.7554284705563518720 ) ) ;
#46826=CARTESIAN_POINT ( 'NONE',  ( 1.515699252679999942, -81.68459978947099387, 0.5251668156352999883 ) ) ;
#46828=CARTESIAN_POINT ( 'NONE',  ( 1.500000000000000000, -81.15000000000000568, 0.000000000000000000 ) ) ;
#46852=ORIENTED_EDGE ( 'NONE', *, *, #14913, .T. ) ;
#46869=CARTESIAN_POINT ( 'NONE',  ( 0.5173218454072999739, -79.56518678517799970, 1.229208833401000067 ) ) ;
#46880=CARTESIAN_POINT ( 'NONE',  ( -1.500000000000000000, -77.50000000000000000, 0.000000000000000000 ) ) ;
#46903=CARTESIAN_POINT ( 'NONE',  ( 1.185193155257999953, -79.68253060846500091, -1.096599795159000079 ) ) ;
#46909=CARTESIAN_POINT ( 'NONE',  ( -1.150888948972000003, -79.09218682990699278, 0.6738713386821000295 ) ) ;
#46939=VECTOR ( 'NONE', #42569, 1000.000000000000000 ) ;
#46962=CARTESIAN_POINT ( 'NONE',  ( -0.1250341999720059050, -81.01872301050605074, -1.526447402715753965 ) ) ;
#46965=CARTESIAN_POINT ( 'NONE',  ( -0.4877242113430015902, -82.25000000000000000, -1.155856577702833343 ) ) ;
#46966=CARTESIAN_POINT ( 'NONE',  ( 0.000000000000000000, -75.67500000000001137, 0.000000000000000000 ) ) ;
#46980=CARTESIAN_POINT ( 'NONE',  ( -1.271001786909834452, -79.14473929417310671, 0.08712350718595020249 ) ) ;
#47024=CARTESIAN_POINT ( 'NONE',  ( -0.5694255183457415104, -78.33855170281904634, -1.140105177683416127 ) ) ;
#47033=CARTESIAN_POINT ( 'NONE',  ( -0.9692428243007442656, -81.59356749952172549, 0.8270901151029305121 ) ) ;
#47035=CARTESIAN_POINT ( 'NONE',  ( 1.289124607492999841, -81.03627781387399409, 0.3416633729347999804 ) ) ;
#47064=ORIENTED_EDGE ( 'NONE', *, *, #17899, .T. ) ;
#47066=CARTESIAN_POINT ( 'NONE',  ( 1.370449731437000107, -80.87330263137000941, 0.3632173918321999762 ) ) ;
#47073=CARTESIAN_POINT ( 'NONE',  ( -0.9218200799623716968, -78.07291666666667140, -1.199500263597270910 ) ) ;
#47077=ADVANCED_FACE ( 'NONE', ( #287 ), #1725, .T. ) ;
#47100=B_SPLINE_CURVE_WITH_KNOTS ( 'NONE', 3,
 ( #56883, #20578, #29704, #15565, #7575, #25573, #47751, #7284, #37704, #11154, #43306, #20007, #52171, #2862, #38861, #33559, #33264, #34422 ),
 .UNSPECIFIED., .F., .F.,
 ( 4, 2, 2, 2, 2, 2, 2, 2, 4 ),
 ( 0.000000000000000000, 0.1250000000000000000, 0.2500000000000000000, 0.3750000000000000000, 0.5000000000000000000, 0.6250000000000000000, 0.7500000000000000000, 0.8750000000000000000, 1.000000000000000000 ),
 .UNSPECIFIED. ) ;
#47106=CARTESIAN_POINT ( 'NONE',  ( -0.4635254915625000027, -82.00000000000000000, -1.426584774443000025 ) ) ;
#47120=CARTESIAN_POINT ( 'NONE',  ( -1.188678760311000060, -81.30005482907799319, 0.9251722853060999618 ) ) ;
#47142=EDGE_LOOP ( 'NONE', ( #29152, #52256, #3339, #26721 ) ) ;
#47174=CARTESIAN_POINT ( 'NONE',  ( -0.9200108141794000050, -81.69875773523600060, -0.9654823929056000065 ) ) ;
#47193=CARTESIAN_POINT ( 'NONE',  ( -1.273775855157000203, -79.09293819223900357, -0.8223283506838999779 ) ) ;
#47201=CARTESIAN_POINT ( 'NONE',  ( -1.295435361468000091, -77.69719476943419068, -0.3166359884281000348 ) ) ;
#47202=EDGE_CURVE ( 'NONE', #42409, #35842, #32065, .T. ) ;
#47221=CARTESIAN_POINT ( 'NONE',  ( 1.499999999999999778, -81.16041666666666288, 0.1963495408493654004 ) ) ;
#47237=FACE_OUTER_BOUND ( 'NONE', #43326, .T. ) ;
#47241=CARTESIAN_POINT ( 'NONE',  ( 1.500000000000000888, -78.73958333333332860, -0.1963495408493590444 ) ) ;
#47264=CARTESIAN_POINT ( 'NONE',  ( 1.250000000000000000, -77.10000000000000853, -0.5000000000000000000 ) ) ;
#47266=CARTESIAN_POINT ( 'NONE',  ( -1.306902306487000009, -82.16898990362500399, -0.1806716399126999939 ) ) ;
#47269=CARTESIAN_POINT ( 'NONE',  ( 0.9947802209974141441, -78.95392151193854602, 0.7966053719781494014 ) ) ;
#47289=CARTESIAN_POINT ( 'NONE',  ( 0.7554284705563453217, -79.83333333333335702, 1.310679582531389276 ) ) ;
#47297=DIRECTION ( 'NONE',  ( -1.000000000000000000, 0.000000000000000000, 0.000000000000000000 ) ) ;
#47300=CARTESIAN_POINT ( 'NONE',  ( 1.240545393080999981, -78.81247058323299370, -0.6863720704128000172 ) ) ;
#47315=CARTESIAN_POINT ( 'NONE',  ( -0.8707220695187634085, -78.81560043429374218, -0.9317800878112861840 ) ) ;
#47323=CARTESIAN_POINT ( 'NONE',  ( -0.6127213972747047599, -80.73488747946474575, -1.116963982030347635 ) ) ;
#47337=ORIENTED_EDGE ( 'NONE', *, *, #9866, .T. ) ;
#47365=CARTESIAN_POINT ( 'NONE',  ( 1.999999999936000084, -76.30000000006400285, -2.601307164620000538E-10 ) ) ;
#47379=DIRECTION ( 'NONE',  ( 0.000000000000000000, -1.000000000000000000, 0.000000000000000000 ) ) ;
#47420=CARTESIAN_POINT ( 'NONE',  ( 0.000000000000000000, -76.39999999999899671, 0.000000000000000000 ) ) ;
#47428=( NAMED_UNIT ( * ) SI_UNIT ( $, .STERADIAN. ) SOLID_ANGLE_UNIT ( ) );
#47454=CARTESIAN_POINT ( 'NONE',  ( 0.2020314717676000016, -80.31521474169700525, -1.318241039644999946 ) ) ;
#47466=CARTESIAN_POINT ( 'NONE',  ( -1.181111693982000110, -79.27654225787900089, -0.4092372983238000139 ) ) ;
#47470=CARTESIAN_POINT ( 'NONE',  ( 1.246077061130999919, -80.85534313775698934, -0.4752592857455000264 ) ) ;
#47487=FACE_OUTER_BOUND ( 'NONE', #19307, .T. ) ;
#47515=CARTESIAN_POINT ( 'NONE',  ( 0.7554284705563452107, -78.23333333333330586, 1.310679582531388609 ) ) ;
#47538=CARTESIAN_POINT ( 'NONE',  ( -0.1963495408493605987, -78.61458333333332860, -1.500000000000000444 ) ) ;
#47540=AXIS2_PLACEMENT_3D ( 'NONE', #6398, #56578, #43006 ) ;
#47542=LINE ( 'NONE', #38644, #30679 ) ;
#47563=CARTESIAN_POINT ( 'NONE',  ( 0.4270232520405565224, -78.30196075596913374, -1.201314851622765634 ) ) ;
#47577=VERTEX_POINT ( 'NONE', #30113 ) ;
#47594=CARTESIAN_POINT ( 'NONE',  ( 1.013266355313000133, -77.86407167464599866, 1.127933319133000101 ) ) ;
#47598=ADVANCED_FACE ( 'NONE', ( #47877 ), #39812, .F. ) ;
#47617=DIRECTION ( 'NONE',  ( 0.000000000000000000, 1.000000000000000000, 0.000000000000000000 ) ) ;
#47618=CARTESIAN_POINT ( 'NONE',  ( 1.261602909406688955, -81.91159713657988561, 0.1820348148243792208 ) ) ;
#47660=ORIENTED_EDGE ( 'NONE', *, *, #5812, .T. ) ;
#47679=CARTESIAN_POINT ( 'NONE',  ( -1.460959015002474493, -78.87916666666666288, 0.3926218265389144757 ) ) ;
#47680=CARTESIAN_POINT ( 'NONE',  ( -0.4929706056563897265, -82.23302231136467810, -1.172003319111136754 ) ) ;
#47706=CARTESIAN_POINT ( 'NONE',  ( -1.178447680628000205, -80.95308451575900222, -0.9280415206345000723 ) ) ;
#47729=CARTESIAN_POINT ( 'NONE',  ( 4.000000000000000000, -76.79999999999999716, 0.000000000000000000 ) ) ;
#47738=CARTESIAN_POINT ( 'NONE',  ( -0.9102058945833000347, -80.61289048198399598, 0.9747214924314999696 ) ) ;
#47747=CARTESIAN_POINT ( 'NONE',  ( -0.9448991540836102487, -79.30853710731122419, -0.8550289145944398594 ) ) ;
#47750=CARTESIAN_POINT ( 'NONE',  ( 1.500000000000000888, -77.73958333333332860, -0.1963495408493590444 ) ) ;
#47751=CARTESIAN_POINT ( 'NONE',  ( -0.7554284705563483193, -80.48333333333333428, -1.310679582531387721 ) ) ;
#47766=CARTESIAN_POINT ( 'NONE',  ( -1.434155062425999994, -79.05986310998500244, -0.2237658014421000097 ) ) ;
#47793=CARTESIAN_POINT ( 'NONE',  ( 1.199500263597268246, -80.70208333333333428, 0.9218200799623752495 ) ) ;
#47794=CARTESIAN_POINT ( 'NONE',  ( -1.500000000000000000, -81.40000000000000568, 0.000000000000000000 ) ) ;
#47823=CARTESIAN_POINT ( 'NONE',  ( -1.138524516885000004, -79.19979032468299351, 0.6666316858816999646 ) ) ;
#47844=CARTESIAN_POINT ( 'NONE',  ( 0.1162510832417349149, -79.01752743935004730, 1.268882844012923838 ) ) ;
#47872=CARTESIAN_POINT ( 'NONE',  ( 0.9236342483431000394, -80.42865684227599843, -0.9420537984437000745 ) ) ;
#47876=CARTESIAN_POINT ( 'NONE',  ( -1.488622005431999851, -78.06252216817030387, -0.2880046469693999800 ) ) ;
#47877=FACE_OUTER_BOUND ( 'NONE', #28282, .T. ) ;
#47893=CARTESIAN_POINT ( 'NONE',  ( 1.271232804528975580, -79.00641992688407811, 0.09643353776494044405 ) ) ;
#47934=EDGE_LOOP ( 'NONE', ( #8158, #25422, #53628 ) ) ;
#47974=CARTESIAN_POINT ( 'NONE',  ( 0.3926218265389220807, -80.14583333333337123, -1.460959015002473382 ) ) ;
#47980=B_SPLINE_CURVE_WITH_KNOTS ( 'NONE', 3,
 ( #39103, #2812, #25236, #2524, #52686, #56539, #8099, #44120, #38813, #26095, #16100, #56830, #52116, #29936, #39675, #11676, #16386, #34371 ),
 .UNSPECIFIED., .F., .F.,
 ( 4, 2, 2, 2, 2, 2, 2, 2, 4 ),
 ( 0.000000000000000000, 0.1250000000000000833, 0.2500000000000001665, 0.3750000000000001665, 0.5000000000000002220, 0.6250000000000002220, 0.7500000000000001110, 0.8750000000000001110, 1.000000000000000000 ),
 .UNSPECIFIED. ) ;
#48008=ORIENTED_EDGE ( 'NONE', *, *, #43881, .T. ) ;
#48027=CARTESIAN_POINT ( 'NONE',  ( 1.329937235669000017, -79.46596153841599630, -0.09921221311570001256 ) ) ;
#48032=ADVANCED_FACE ( 'NONE', ( #26183 ), #35024, .F. ) ;
#48041=CARTESIAN_POINT ( 'NONE',  ( -0.05395919428434999693, -80.75611789099500015, -1.332567581519000122 ) ) ;
#48059=CARTESIAN_POINT ( 'NONE',  ( -1.469401861277999988, -80.52594520594300320, -0.6692011555514000287 ) ) ;
#48084=CARTESIAN_POINT ( 'NONE',  ( 0.1963495408493571848, -78.26458333333334849, 1.500000000000000666 ) ) ;
#48105=CARTESIAN_POINT ( 'NONE',  ( 0.1963495408493571015, -80.86458333333332860, 1.500000000000000444 ) ) ;
#48107=FACE_OUTER_BOUND ( 'NONE', #20473, .T. ) ;
#48151=CARTESIAN_POINT ( 'NONE',  ( -0.1963495408493673433, -79.88541666666667140, 1.499999999999999334 ) ) ;
#48159=CARTESIAN_POINT ( 'NONE',  ( 0.5499573741622000300, -79.64061393252499954, 1.306754138290999956 ) ) ;
#48161=CARTESIAN_POINT ( 'NONE',  ( -0.2007418666109000160, -78.16174741493239253, -1.502878855747000086 ) ) ;
#48187=CARTESIAN_POINT ( 'NONE',  ( 1.157688070529184321, -81.43455268099248201, 0.5329657265460440163 ) ) ;
#48190=CARTESIAN_POINT ( 'NONE',  ( 1.199500263597268246, -79.20208333333333428, 0.9218200799623752495 ) ) ;
#48228=DIRECTION ( 'NONE',  ( 0.7071067811865474617, 0.7071067811865474617, -9.196969555969614050E-11 ) ) ;
#48236=DIRECTION ( 'NONE',  ( 0.000000000000000000, 1.000000000000000000, 0.000000000000000000 ) ) ;
#48316=CARTESIAN_POINT ( 'NONE',  ( 1.251999141562743167, -80.48525731161612384, -0.2411094176575541426 ) ) ;
#48321=CARTESIAN_POINT ( 'NONE',  ( -1.321095329625999959, -82.14527134566500877, -0.1826337427822999904 ) ) ;
#48331=CARTESIAN_POINT ( 'NONE',  ( -0.8205178898083000938, -80.81311342771999762, -1.021985690358000243 ) ) ;
#48336=CARTESIAN_POINT ( 'NONE',  ( -0.1931516691869999969, -80.43247902352800338, 1.503874604587000174 ) ) ;
#48340=CARTESIAN_POINT ( 'NONE',  ( -1.256510416662318663, -82.24348958333220594, 0.1636246174179673829 ) ) ;
#48361=CARTESIAN_POINT ( 'NONE',  ( 0.3926218265389159745, -78.25416666666667709, 1.460959015002474493 ) ) ;
#48368=ADVANCED_FACE ( 'NONE', ( #56220 ), #51800, .T. ) ;
#48381=CARTESIAN_POINT ( 'NONE',  ( 1.592284932317999946, -78.67132866053199791, 0.2680347371437999948 ) ) ;
#48388=CARTESIAN_POINT ( 'NONE',  ( 0.1427930653877000078, -78.10831261029910877, 1.311554697429999861 ) ) ;
#48408=CARTESIAN_POINT ( 'NONE',  ( -0.3926218265389189721, -78.50416666666667709, -1.460959015002473604 ) ) ;
#48414=ADVANCED_FACE ( 'NONE', ( #22141 ), #10644, .F. ) ;
#48425=CARTESIAN_POINT ( 'NONE',  ( -0.6838172738181883537, -82.21924584448981932, -1.066457163286079979 ) ) ;
#48427=CARTESIAN_POINT ( 'NONE',  ( 0.000000000000000000, -75.67500000000001137, 0.000000000000000000 ) ) ;
#48436=CARTESIAN_POINT ( 'NONE',  ( -0.5179932711920000044, -79.39255081561999816, -1.319781611125000031 ) ) ;
#48439=CARTESIAN_POINT ( 'NONE',  ( -1.040416939902000237, -78.11213479155139794, -1.102939138596999991 ) ) ;
#48444=CARTESIAN_POINT ( 'NONE',  ( -1.259732397319124342, -79.12633733726526941, -0.4364906895173376600 ) ) ;
#48481=B_SPLINE_CURVE_WITH_KNOTS ( 'NONE', 3,
 ( #14573, #46195, #41740, #19312, #42035, #50904, #1604, #37302, #14862, #32858, #52352, #6889, #57060, #7471, #12467, #3611, #43781, #3333 ),
 .UNSPECIFIED., .F., .F.,
 ( 4, 2, 2, 2, 2, 2, 2, 2, 4 ),
 ( 0.000000000000000000, 0.1250000000000000833, 0.2500000000000001665, 0.3750000000000001665, 0.5000000000000002220, 0.6250000000000002220, 0.7500000000000001110, 0.8750000000000001110, 1.000000000000000000 ),
 .UNSPECIFIED. ) ;
#48546=VECTOR ( 'NONE', #21363, 1000.000000000000000 ) ;
#48573=CARTESIAN_POINT ( 'NONE',  ( -1.500000000000000000, -78.50000000000000000, 0.000000000000000000 ) ) ;
#48597=CYLINDRICAL_SURFACE ( 'NONE', #51530, 1.500000000000000000 ) ;
#48601=CARTESIAN_POINT ( 'NONE',  ( 0.5769587189189382403, -79.91279883384609661, -1.136438736130747529 ) ) ;
#48602=EDGE_LOOP ( 'NONE', ( #1963, #33979, #39126, #55611, #27274 ) ) ;
#48605=CARTESIAN_POINT ( 'NONE',  ( -0.8719406389885000497, -81.24640551900300522, -1.009106372638000071 ) ) ;
#48620=CARTESIAN_POINT ( 'NONE',  ( -1.227075629532000001, -79.64443611377700449, -0.7101723588523999320 ) ) ;
#48640=ADVANCED_FACE ( 'NONE', ( #47237 ), #51235, .T. ) ;
#48668=CARTESIAN_POINT ( 'NONE',  ( -1.199500263597274685, -80.94791666666668561, 0.9218200799623673669 ) ) ;
#48671=CARTESIAN_POINT ( 'NONE',  ( -1.250000000000000000, -77.10000000000000853, 0.5000000000000000000 ) ) ;
#48699=DIRECTION ( 'NONE',  ( -1.000000000000000000, 0.000000000000000000, 0.000000000000000000 ) ) ;
#48710=CARTESIAN_POINT ( 'NONE',  ( 0.000000000000000000, -75.67500000000001137, 0.000000000000000000 ) ) ;
#48723=CARTESIAN_POINT ( 'NONE',  ( 1.299878529918000014, -80.47826946565700723, -0.2255693107841999778 ) ) ;
#48726=CARTESIAN_POINT ( 'NONE',  ( -0.1108284043172000077, -77.77636455657749082, -1.314634435239000032 ) ) ;
#48751=CARTESIAN_POINT ( 'NONE',  ( -1.250000000000000000, -76.50000000000000000, 0.000000000000000000 ) ) ;
#48788=ORIENTED_EDGE ( 'NONE', *, *, #39465, .F. ) ;
#48804=CONICAL_SURFACE ( 'NONE', #26166, 3.899999999992999733, 0.7853981633972997312 ) ;
#48848=EDGE_CURVE ( 'NONE', #16033, #45960, #23498, .T. ) ;
#48850=CARTESIAN_POINT ( 'NONE',  ( -1.169332518864999892, -82.05248746382200409, -1.113388286646999958 ) ) ;
#48869=CARTESIAN_POINT ( 'NONE',  ( -0.6056189234361001317, -80.35315015347299550, -1.188192690176999911 ) ) ;
#48888=CARTESIAN_POINT ( 'NONE',  ( -0.01872084306268049364, -79.62656959496065667, 1.274104374990254973 ) ) ;
#48889=ADVANCED_FACE ( 'NONE', ( #38984 ), #11558, .T. ) ;
#48894=CARTESIAN_POINT ( 'NONE',  ( 0.2153359604882000011, -81.99643347552201078, 1.316133176457000120 ) ) ;
#48903=CARTESIAN_POINT ( 'NONE',  ( -1.271707153813000035, -81.76195542696700613, 0.6054370633115999656 ) ) ;
#48908=CARTESIAN_POINT ( 'NONE',  ( 1.040651332726000078, -79.79327398392099724, -0.9628624948066000222 ) ) ;
#48911=CARTESIAN_POINT ( 'NONE',  ( -1.115313966523381550, -82.22395833333196435, 0.6418514623139731645 ) ) ;
#48926=CARTESIAN_POINT ( 'NONE',  ( 1.412760417132294943, -82.08723958285546018, -0.1840777080652946651 ) ) ;
#48928=CARTESIAN_POINT ( 'NONE',  ( -0.7578051741271042419, -80.57587266093590017, 1.024356917418570267 ) ) ;
#48944=CARTESIAN_POINT ( 'NONE',  ( 0.8762648495846868668, -81.43265505382323965, -0.9941098996437038871 ) ) ;
#48951=CARTESIAN_POINT ( 'NONE',  ( 1.412851607863000014, -79.11784227096099187, -0.7817060856327000540 ) ) ;
#48959=CARTESIAN_POINT ( 'NONE',  ( -1.146672249030999957, -77.71141162325049834, 0.4628715253012000153 ) ) ;
#49003=DIRECTION ( 'NONE',  ( 0.000000000000000000, 0.000000000000000000, -1.000000000000000000 ) ) ;
#49008=CARTESIAN_POINT ( 'NONE',  ( 1.330388504836999886, -80.14249923068300063, 0.7273297589862000034 ) ) ;
#49010=CARTESIAN_POINT ( 'NONE',  ( 0.2064441143900000164, -78.52055390729400131, 1.303052737963999785 ) ) ;
#49022=B_SPLINE_CURVE_WITH_KNOTS ( 'NONE', 3,
 ( #6038, #51516, #42361, #46807, #19923, #6916, #11075, #10779, #34051, #42648, #50933, #11648, #20216, #28465, #38205, #47679, #28757, #42941 ),
 .UNSPECIFIED., .F., .F.,
 ( 4, 2, 2, 2, 2, 2, 2, 2, 4 ),
 ( 0.000000000000000000, 0.1249999999999999722, 0.2499999999999999445, 0.3749999999999998890, 0.4999999999999998890, 0.6249999999999998890, 0.7499999999999997780, 0.8749999999999998890, 1.000000000000000000 ),
 .UNSPECIFIED. ) ;
#49030=CARTESIAN_POINT ( 'NONE',  ( -1.181111693982000110, -79.27654225787900089, -0.4092372983238000139 ) ) ;
#49039=CARTESIAN_POINT ( 'NONE',  ( -0.7554284705563540925, -79.31666666666669130, 1.310679582531384391 ) ) ;
#49068=VERTEX_POINT ( 'NONE', #2409 ) ;
#49070=VERTEX_POINT ( 'NONE', #22354 ) ;
#49076=ORIENTED_EDGE ( 'NONE', *, *, #2042, .F. ) ;
#49103=CARTESIAN_POINT ( 'NONE',  ( -0.3713770062794000126, -82.26979749068699732, -1.193557338046999927 ) ) ;
#49116=DIRECTION ( 'NONE',  ( 1.000000000000000000, 0.000000000000000000, 0.000000000000000000 ) ) ;
#49137=CARTESIAN_POINT ( 'NONE',  ( 1.508679547070999938, -80.71294663253300428, -0.5754170318403001305 ) ) ;
#49157=CARTESIAN_POINT ( 'NONE',  ( -1.213636094208999872, -80.79966376390299843, -0.5527192377158001158 ) ) ;
#49173=CARTESIAN_POINT ( 'NONE',  ( 1.219634552038143083, -79.97640533137604280, -0.3722560451975370222 ) ) ;
#49178=CARTESIAN_POINT ( 'NONE',  ( 0.08638142328466999476, -81.04795502547899844, 1.330832257483999914 ) ) ;
#49189=CARTESIAN_POINT ( 'NONE',  ( -1.242342038214000022, -82.25520586034700443, -0.2121855787343999988 ) ) ;
#49195=CARTESIAN_POINT ( 'NONE',  ( -0.8999941789210000875, -80.66976366365300066, -1.015940422307999969 ) ) ;
#49212=ADVANCED_FACE ( 'NONE', ( #46284 ), #1009, .F. ) ;
#49219=CARTESIAN_POINT ( 'NONE',  ( -1.260218936850459936, -79.63768523161391499, 0.1932868554924389581 ) ) ;
#49243=CARTESIAN_POINT ( 'NONE',  ( 0.8292593438864999111, -78.07597717995859909, -1.385477418387000004 ) ) ;
#49248=CARTESIAN_POINT ( 'NONE',  ( -1.500000000000000000, -81.00000000000000000, 0.000000000000000000 ) ) ;
#49250=CARTESIAN_POINT ( 'NONE',  ( -1.092853437769999880, -78.91363271308999572, -1.051005954092999906 ) ) ;
#49271=CARTESIAN_POINT ( 'NONE',  ( -1.249999993052000047, -76.30000000069199473, -0.6999999993075000093 ) ) ;
#49305=CARTESIAN_POINT ( 'NONE',  ( 1.161710437675000041, -79.54714775010999972, -0.9743588931339001169 ) ) ;
#49338=CARTESIAN_POINT ( 'NONE',  ( -0.1963495408493673156, -79.28541666666667709, 1.499999999999999556 ) ) ;
#49345=ORIENTED_EDGE ( 'NONE', *, *, #36983, .T. ) ;
#49355=CARTESIAN_POINT ( 'NONE',  ( 0.9218200799623742503, -81.17708333333334281, -1.199500263597268912 ) ) ;
#49361=VERTEX_POINT ( 'NONE', #54749 ) ;
#49398=DIRECTION ( 'NONE',  ( 9.558576152644999723E-12, 1.000000000000000000, 3.007563087384999928E-10 ) ) ;
#49462=CARTESIAN_POINT ( 'NONE',  ( -1.185397549814999785, -80.25976351251399876, -0.6110718436566999756 ) ) ;
#49477=CARTESIAN_POINT ( 'NONE',  ( 1.164955675041443817, -80.04001182890594635, 0.6368716809728905970 ) ) ;
#49482=CARTESIAN_POINT ( 'NONE',  ( 0.6224761083686999319, -81.92930503473399995, -1.179448874982999884 ) ) ;
#49486=EDGE_CURVE ( 'NONE', #57807, #28437, #56787, .T. ) ;
#49492=CARTESIAN_POINT ( 'NONE',  ( 1.339915889275999916, -81.06493106288900208, -0.6881352248621999124 ) ) ;
#49498=CARTESIAN_POINT ( 'NONE',  ( 0.9925657212695000453, -80.28940021773100000, -1.012359935335999994 ) ) ;
#49516=ORIENTED_EDGE ( 'NONE', *, *, #13867, .F. ) ;
#49520=CARTESIAN_POINT ( 'NONE',  ( -1.257915819032439098, -80.16243413275964258, -0.2016166298787092637 ) ) ;
#49527=AXIS2_PLACEMENT_3D ( 'NONE', #11361, #15775, #33767 ) ;
#49537=PRODUCT_DEFINITION ( 'UNKNOWN', '', #6519, #53417 ) ;
#49544=CARTESIAN_POINT ( 'NONE',  ( -0.7022187824378000043, -82.19906693409399168, -1.095132696781000003 ) ) ;
#49555=CARTESIAN_POINT ( 'NONE',  ( -1.428376501803000131, -77.83869253983340286, 0.2580938706625000023 ) ) ;
#49573=CARTESIAN_POINT ( 'NONE',  ( 1.500000000000000000, -80.75000000000000000, 0.000000000000000000 ) ) ;
#49576=CARTESIAN_POINT ( 'NONE',  ( 1.199500263597271577, -81.59791666666669130, -0.9218200799623702535 ) ) ;
#49607=CARTESIAN_POINT ( 'NONE',  ( 1.590911073979999868, -80.64438452883999275, -0.2760724992506000119 ) ) ;
#49680=EDGE_CURVE ( 'NONE', #22393, #900, #8640, .T. ) ;
#49703=VECTOR ( 'NONE', #20066, 1000.000000000000000 ) ;
#49704=ORIENTED_EDGE ( 'NONE', *, *, #51363, .T. ) ;
#49705=ADVANCED_FACE ( 'NONE', ( #34126 ), #35309, .F. ) ;
#49730=CARTESIAN_POINT ( 'NONE',  ( 1.200757745776334318, -77.87262074594069361, -0.4270230002123092117 ) ) ;
#49756=DIRECTION ( 'NONE',  ( 0.000000000000000000, -1.000000000000000000, 0.000000000000000000 ) ) ;
#49758=CARTESIAN_POINT ( 'NONE',  ( -0.5470841013496000604, -79.81324990208399583, -1.216254552179000026 ) ) ;
#49771=CARTESIAN_POINT ( 'NONE',  ( -1.309352690804000074, -78.28086903840210198, -0.2533212985548999874 ) ) ;
#49779=CARTESIAN_POINT ( 'NONE',  ( 0.6791306551168999617, -81.43317880092300243, -1.147762040996999966 ) ) ;
#49790=CARTESIAN_POINT ( 'NONE',  ( -1.393363954175000030, -81.80898018020499762, -0.2057425908966999950 ) ) ;
#49796=CARTESIAN_POINT ( 'NONE',  ( 0.5117640625906000329, -79.50135730798099587, 1.216002981391000048 ) ) ;
#49797=EDGE_LOOP ( 'NONE', ( #22914, #46257, #29917, #29452 ) ) ;
#49799=CARTESIAN_POINT ( 'NONE',  ( -1.471932811527529195, -79.41769483858601575, -0.3335056313496183034 ) ) ;
#49817=CARTESIAN_POINT ( 'NONE',  ( 1.041288859402153877, -80.44866080611242865, 0.7340484819354226032 ) ) ;
#49851=CARTESIAN_POINT ( 'NONE',  ( 0.3926218265389159745, -79.75416666666667709, 1.460959015002474493 ) ) ;
#49852=CARTESIAN_POINT ( 'NONE',  ( -1.391953914337000109, -78.31252216817028966, -0.2693022098514999962 ) ) ;
#49860=CARTESIAN_POINT ( 'NONE',  ( 1.500000000000000000, -81.75000000000000000, 0.000000000000000000 ) ) ;
#49863=FACE_BOUND ( 'NONE', #31260, .T. ) ;
#49880=ORIENTED_EDGE ( 'NONE', *, *, #981, .F. ) ;
#49900=CARTESIAN_POINT ( 'NONE',  ( -1.347695613438000040, -80.39056234758800201, -0.6947364142266000409 ) ) ;
#49901=CARTESIAN_POINT ( 'NONE',  ( 0.2696047275149000555, -79.01668014110398985, 1.291465103089999955 ) ) ;
#49903=AXIS2_PLACEMENT_3D ( 'NONE', #21251, #43131, #21541 ) ;
#50038=CARTESIAN_POINT ( 'NONE',  ( 0.000000000000000000, -76.29999999999999716, -2.000000000000000000 ) ) ;
#50043=DIRECTION ( 'NONE',  ( 1.000000000000000000, 0.000000000000000000, 0.000000000000000000 ) ) ;
#50045=CARTESIAN_POINT ( 'NONE',  ( 1.323534079420999987, -80.00586178980599072, -0.1638099207045999872 ) ) ;
#50061=CARTESIAN_POINT ( 'NONE',  ( -0.9612450871864000046, -78.78283387801499771, -0.9244371432244999909 ) ) ;
#50062=CARTESIAN_POINT ( 'NONE',  ( 1.249999996278000181, -76.50000000037098857, 0.4999999996289999915 ) ) ;
#50081=CARTESIAN_POINT ( 'NONE',  ( -1.042454788111000008, -81.85600493344199435, -0.9471436726904000070 ) ) ;
#50091=CARTESIAN_POINT ( 'NONE',  ( -0.3926218265389189721, -79.00416666666667709, -1.460959015002473604 ) ) ;
#50110=CARTESIAN_POINT ( 'NONE',  ( -0.4077636671461413176, -80.05112375978934836, 1.207988005846317270 ) ) ;
#50116=EDGE_CURVE ( 'NONE', #56774, #27498, #36221, .T. ) ;
#50144=CARTESIAN_POINT ( 'NONE',  ( -0.1273708076881999995, -77.97099286884960634, -1.510858618444999912 ) ) ;
#50161=FACE_OUTER_BOUND ( 'NONE', #8766, .T. ) ;
#50162=DIRECTION ( 'NONE',  ( 0.000000000000000000, -1.000000000000000000, 0.000000000000000000 ) ) ;
#50163=DIRECTION ( 'NONE',  ( 0.000000000000000000, 1.000000000000000000, 0.000000000000000000 ) ) ;
#50167=ORIENTED_EDGE ( 'NONE', *, *, #53837, .F. ) ;
#50189=CARTESIAN_POINT ( 'NONE',  ( 1.610212697858000030, -79.65213206121900669, -0.1201205297940999978 ) ) ;
#50234=CARTESIAN_POINT ( 'NONE',  ( -0.3926218265389190276, -81.10416666666667140, -1.460959015002473826 ) ) ;
#50242=EDGE_CURVE ( 'NONE', #32054, #5068, #4044, .T. ) ;
#50244=ORIENTED_EDGE ( 'NONE', *, *, #50242, .T. ) ;
#50250=AXIS2_PLACEMENT_3D ( 'NONE', #4736, #54334, #40150 ) ;
#50254=VERTEX_POINT ( 'NONE', #4648 ) ;
#50310=VECTOR ( 'NONE', #55508, 1000.000000000000114 ) ;
#50319=CARTESIAN_POINT ( 'NONE',  ( -0.05736323927548000329, -80.72446476122699721, -1.416633329004000075 ) ) ;
#50350=CARTESIAN_POINT ( 'NONE',  ( -0.6568659331174000471, -78.18164379163989963, 1.160647793301999853 ) ) ;
#50371=CARTESIAN_POINT ( 'NONE',  ( 0.6269351409810999254, -82.19352514059698933, 1.369619292736000027 ) ) ;
#50378=CARTESIAN_POINT ( 'NONE',  ( -0.2944660333051000167, -79.55096993136200467, 1.286023070983999927 ) ) ;
#50379=EDGE_LOOP ( 'NONE', ( #38212, #12689, #31351, #56119 ) ) ;
#50381=CARTESIAN_POINT ( 'NONE',  ( 1.500000000000001110, -79.13958333333334849, -0.1963495408493590721 ) ) ;
#50394=VERTEX_POINT ( 'NONE', #24101 ) ;
#50420=CARTESIAN_POINT ( 'NONE',  ( 0.4526505179569237369, -81.90290258620123609, -1.245472627785131126 ) ) ;
#50421=CARTESIAN_POINT ( 'NONE',  ( 0.000000000000000000, -76.00000000000000000, 0.000000000000000000 ) ) ;
#50432=CARTESIAN_POINT ( 'NONE',  ( 1.460959015002472494, -79.67083333333336270, 0.3926218265389232465 ) ) ;
#50433=CARTESIAN_POINT ( 'NONE',  ( -1.500872881732000064, -78.86402008970900113, -0.2152271930174000092 ) ) ;
#50454=CARTESIAN_POINT ( 'NONE',  ( -1.750000000000000000, -67.52659999995799467, 0.000000000000000000 ) ) ;
#50460=AXIS2_PLACEMENT_3D ( 'NONE', #48427, #30391, #35388 ) ;
#50462=ORIENTED_EDGE ( 'NONE', *, *, #4364, .F. ) ;
#50481=CARTESIAN_POINT ( 'NONE',  ( -0.6747260877994001316, -82.22962677363800310, -1.052256958371999840 ) ) ;
#50520=CARTESIAN_POINT ( 'NONE',  ( -0.1174688447357000037, -81.27596268276600711, -1.314064945473999879 ) ) ;
#50544=ORIENTED_EDGE ( 'NONE', *, *, #40012, .T. ) ;
#50549=CARTESIAN_POINT ( 'NONE',  ( 1.500000000000000000, -77.76041666666668561, 0.1963495408493652339 ) ) ;
#50553=CARTESIAN_POINT ( 'NONE',  ( 0.000000000000000000, -75.67500000000001137, 0.000000000000000000 ) ) ;
#50577=CARTESIAN_POINT ( 'NONE',  ( 0.000000000000000000, -76.00000000000000000, -2.299999999999952749 ) ) ;
#50585=CARTESIAN_POINT ( 'NONE',  ( 0.000000000000000000, -76.39999999999999147, -0.5999999999999999778 ) ) ;
#50604=CARTESIAN_POINT ( 'NONE',  ( 1.310679582531388387, -78.10833333333333428, -0.7554284705563470981 ) ) ;
#50612=CARTESIAN_POINT ( 'NONE',  ( 1.496442341964999923, -81.81018341126400628, 0.2441364298766999785 ) ) ;
#50626=CARTESIAN_POINT ( 'NONE',  ( -1.500000000000000888, -79.48958333333334281, 0.1963495408493559080 ) ) ;
#50645=CARTESIAN_POINT ( 'NONE',  ( 1.315129997485000146, -78.48515813772890226, 0.2213803045116000123 ) ) ;
#50664=CARTESIAN_POINT ( 'NONE',  ( -1.586895984600000142, -81.91972355565999919, -0.2343193179190000142 ) ) ;
#50672=CARTESIAN_POINT ( 'NONE',  ( -1.310679582531389498, -81.45833333333332860, 0.7554284705563444335 ) ) ;
#50677=ORIENTED_EDGE ( 'NONE', *, *, #24776, .F. ) ;
#50729=CIRCLE ( 'NONE', #36543, 0.5000000000000000000 ) ;
#50749=CARTESIAN_POINT ( 'NONE',  ( -0.9612450871864000046, -78.73905986043699556, -0.9244371432244999909 ) ) ;
#50815=CARTESIAN_POINT ( 'NONE',  ( -1.296534853615000094, -81.67286366981399226, -0.2440552883437999976 ) ) ;
#50835=EDGE_CURVE ( 'NONE', #41674, #43048, #47980, .T. ) ;
#50883=CARTESIAN_POINT ( 'NONE',  ( 1.199500263597268246, -80.30208333333334281, 0.9218200799623752495 ) ) ;
#50892=EDGE_LOOP ( 'NONE', ( #48788, #43045, #94 ) ) ;
#50901=CARTESIAN_POINT ( 'NONE',  ( -0.5177863484446000308, -82.19630592153200155, -1.254600239572999820 ) ) ;
#50904=CARTESIAN_POINT ( 'NONE',  ( -0.9218200799623775810, -81.92708333334323356, 1.199500263597266247 ) ) ;
#50933=CARTESIAN_POINT ( 'NONE',  ( -0.3926218265389256890, -78.79583333333334849, 1.460959015002472050 ) ) ;
#50934=CARTESIAN_POINT ( 'NONE',  ( -0.9151233253627000241, -78.28670764420459705, -0.9701162038759999495 ) ) ;
#50951=CARTESIAN_POINT ( 'NONE',  ( 1.456666284817000001, -81.58220334850499000, -0.3834374542928999929 ) ) ;
#50961=EDGE_LOOP ( 'NONE', ( #43337, #23560, #51842, #31621, #27015, #24618, #32635, #7248, #32171, #41151 ) ) ;
#50962=ORIENTED_EDGE ( 'NONE', *, *, #38706, .T. ) ;
#50980=EDGE_LOOP ( 'NONE', ( #42459, #51713, #56176, #25074, #40877, #41273 ) ) ;
#50981=ADVANCED_FACE ( 'NONE', ( #10739 ), #1589, .T. ) ;
#50997=CARTESIAN_POINT ( 'NONE',  ( 0.3292142484335000563, -79.27918825649700807, -1.292352404326999826 ) ) ;
#51003=CARTESIAN_POINT ( 'NONE',  ( 0.000000000000000000, -76.00000000000000000, 0.000000000000000000 ) ) ;
#51039=CARTESIAN_POINT ( 'NONE',  ( -1.159125165887999964, -77.64758214605309661, 0.4678983327651999868 ) ) ;
#51052=ORIENTED_EDGE ( 'NONE', *, *, #36384, .F. ) ;
#51069=CARTESIAN_POINT ( 'NONE',  ( -0.2056945464814999847, -80.79322239898399971, 1.601533168507999871 ) ) ;
#51104=VERTEX_POINT ( 'NONE', #43191 ) ;
#51117=EDGE_CURVE ( 'NONE', #7313, #47577, #16322, .T. ) ;
#51118=DIRECTION ( 'NONE',  ( 0.000000000000000000, 1.000000000000000000, 0.000000000000000000 ) ) ;
#51139=CARTESIAN_POINT ( 'NONE',  ( -1.140592747978000032, -79.04901557144499691, -0.9947442812858000583 ) ) ;
#51154=CARTESIAN_POINT ( 'NONE',  ( -1.127782339217550778, -78.21133870775913977, 0.5953878299651829131 ) ) ;
#51165=CARTESIAN_POINT ( 'NONE',  ( 0.1510373474112000070, -81.63162929444700922, 1.325052402434999888 ) ) ;
#51175=CARTESIAN_POINT ( 'NONE',  ( 0.3926218265389220807, -79.64583333333334281, -1.460959015002473382 ) ) ;
#51176=ADVANCED_FACE ( 'NONE', ( #31832 ), #12385, .F. ) ;
#51183=CIRCLE ( 'NONE', #53051, 2.000000000000000000 ) ;
#51196=CARTESIAN_POINT ( 'NONE',  ( 0.7721134610030000456, -81.21483193069099116, -1.304907259309999956 ) ) ;
#51235=CONICAL_SURFACE ( 'NONE', #5988, 1.249999999985999866, 0.7853981633972997312 ) ;
#51241=AXIS2_PLACEMENT_3D ( 'NONE', #55724, #37404, #55425 ) ;
#51248=CARTESIAN_POINT ( 'NONE',  ( -1.490129969386999820, -81.86435186793200103, -0.2200309544077999890 ) ) ;
#51290=CARTESIAN_POINT ( 'NONE',  ( 0.5173218454072999739, -79.47763875002098644, 1.229208833401000067 ) ) ;
#51298=DIRECTION ( 'NONE',  ( 0.000000000000000000, -1.000000000000000000, 0.000000000000000000 ) ) ;
#51300=CARTESIAN_POINT ( 'NONE',  ( -0.3125244749084483131, -82.00520833143282573, -1.470171615151792288 ) ) ;
#51303=CARTESIAN_POINT ( 'NONE',  ( 0.8962411872155999770, -81.45069461833000446, 0.9875868993909000526 ) ) ;
#51306=PLANE ( 'NONE',  #27289 ) ;
#51323=CARTESIAN_POINT ( 'NONE',  ( 0.3219823053856999961, -79.63291798508399211, -1.582258297802999980 ) ) ;
#51328=CARTESIAN_POINT ( 'NONE',  ( -0.5996107393304999089, -78.54644797271500067, 1.191235959310000148 ) ) ;
#51363=EDGE_CURVE ( 'NONE', #12731, #43330, #18086, .T. ) ;
#51397=CARTESIAN_POINT ( 'NONE',  ( 1.290211209374999779, -81.42480055290900509, 0.2755370129015000114 ) ) ;
#51401=CARTESIAN_POINT ( 'NONE',  ( 0.5516207887802486720, -78.81080817526184035, -1.149250216138818725 ) ) ;
#51430=CARTESIAN_POINT ( 'NONE',  ( -1.585290096527000259, -78.00715048044240518, -0.3067070840873000193 ) ) ;
#51447=CARTESIAN_POINT ( 'NONE',  ( -1.254928322143489483, -78.73609231238140183, 0.2213947216297834919 ) ) ;
#51455=CARTESIAN_POINT ( 'NONE',  ( -0.5870063249280824680, -81.73668083619796221, -1.130609457767802972 ) ) ;
#51457=CARTESIAN_POINT ( 'NONE',  ( 0.7341740840635999632, -80.93705256711200491, -1.113348630318000021 ) ) ;
#51466=CARTESIAN_POINT ( 'NONE',  ( -1.250000000000000000, -77.10000000000000853, 0.5000000000000000000 ) ) ;
#51469=CARTESIAN_POINT ( 'NONE',  ( -0.9218200799623716968, -79.57291666666667140, -1.199500263597270910 ) ) ;
#51480=VERTEX_POINT ( 'NONE', #29439 ) ;
#51487=CARTESIAN_POINT ( 'NONE',  ( 0.09183084214940000212, -80.97252787813199859, 1.414788531112000092 ) ) ;
#51516=CARTESIAN_POINT ( 'NONE',  ( 1.499999999999999778, -78.66041666666669130, 0.1963495408493654004 ) ) ;
#51517=CARTESIAN_POINT ( 'NONE',  ( -1.112801787005999854, -79.30619658827799867, -0.6258220204580999813 ) ) ;
#51530=AXIS2_PLACEMENT_3D ( 'NONE', #52442, #17283, #43297 ) ;
#51538=CARTESIAN_POINT ( 'NONE',  ( -1.306825378516000002, -81.39410433555399038, -0.7490716765632000618 ) ) ;
#51551=CARTESIAN_POINT ( 'NONE',  ( 0.000000000000000000, -77.50000000000000000, -3.799999999999999822 ) ) ;
#51595=CARTESIAN_POINT ( 'NONE',  ( 0.9218200799623742503, -77.67708333333335702, -1.199500263597268912 ) ) ;
#51597=FACE_BOUND ( 'NONE', #29094, .T. ) ;
#51616=CARTESIAN_POINT ( 'NONE',  ( -1.583750823903000038, -80.47633258256199440, 0.3147260902806000016 ) ) ;
#51622=CARTESIAN_POINT ( 'NONE',  ( -0.6568659331174000471, -78.09409575648280111, 1.160647793301999853 ) ) ;
#51678=CARTESIAN_POINT ( 'NONE',  ( -0.9870767835202882701, -80.96949413944575724, -1.171048524979026118 ) ) ;
#51692=CARTESIAN_POINT ( 'NONE',  ( -0.6199991881899920010, -79.06523188490864129, 1.113316751120226211 ) ) ;
#51696=AXIS2_PLACEMENT_3D ( 'NONE', #10004, #54584, #18573 ) ;
#51707=CARTESIAN_POINT ( 'NONE',  ( 1.460959015002472494, -80.17083333333334849, 0.3926218265389232465 ) ) ;
#51711=CARTESIAN_POINT ( 'NONE',  ( 0.1963495408493571015, -79.86458333333331439, 1.500000000000000444 ) ) ;
#51713=ORIENTED_EDGE ( 'NONE', *, *, #34135, .F. ) ;
#51720=CARTESIAN_POINT ( 'NONE',  ( -1.256882289721999779, -78.56440746632799232, 0.6559773548962000156 ) ) ;
#51731=ORIENTED_EDGE ( 'NONE', *, *, #18366, .T. ) ;
#51738=CARTESIAN_POINT ( 'NONE',  ( 0.7278917586638090631, -78.57707606855669269, 1.047022026650526794 ) ) ;
#51745=CARTESIAN_POINT ( 'NONE',  ( -1.254047611068101142, -81.16422748949325694, -0.2299481821587232855 ) ) ;
#51798=FACE_OUTER_BOUND ( 'NONE', #54311, .T. ) ;
#51800=CYLINDRICAL_SURFACE ( 'NONE', #36071, 1.500000000000000000 ) ;
#51842=ORIENTED_EDGE ( 'NONE', *, *, #9953, .F. ) ;
#51844=ORIENTED_EDGE ( 'NONE', *, *, #36092, .F. ) ;
#51868=CARTESIAN_POINT ( 'NONE',  ( -1.154258600661999923, -79.71986326112400434, -0.6680293646364998672 ) ) ;
#51880=CARTESIAN_POINT ( 'NONE',  ( -0.7068627984950999199, -81.05379363128199088, 1.130893941374999878 ) ) ;
#51905=CARTESIAN_POINT ( 'NONE',  ( -0.9420598709024999851, -79.19141207666899618, -0.8215979549846998964 ) ) ;
#51928=CARTESIAN_POINT ( 'NONE',  ( 0.9218200799623692543, -81.22291666666669130, 1.199500263597272687 ) ) ;
#51949=CARTESIAN_POINT ( 'NONE',  ( -1.199500263597270022, -78.55208333333332860, -0.9218200799623730290 ) ) ;
#51958=CARTESIAN_POINT ( 'NONE',  ( 1.500000000000000222, -81.13359037631325066, -0.3093141193355204432 ) ) ;
#51962=CARTESIAN_POINT ( 'NONE',  ( -0.5849273512657638951, -82.25000000000000000, -1.109837523374604729 ) ) ;
#51972=ADVANCED_FACE ( 'NONE', ( #11395 ), #43544, .T. ) ;
#52007=CARTESIAN_POINT ( 'NONE',  ( -1.183003490338000008, -79.14322140577399978, -0.6653023415106000815 ) ) ;
#52031=CARTESIAN_POINT ( 'NONE',  ( 0.9577060863230739685, -80.95750822540561842, 0.8401837386943417085 ) ) ;
#52032=ORIENTED_EDGE ( 'NONE', *, *, #15765, .F. ) ;
#52055=ORIENTED_EDGE ( 'NONE', *, *, #38636, .F. ) ;
#52068=CARTESIAN_POINT ( 'NONE',  ( -0.7554284705563480973, -78.08333333333334281, -1.310679582531387277 ) ) ;
#52080=CARTESIAN_POINT ( 'NONE',  ( 1.500000000000000000, -79.25000000000000000, 0.000000000000000000 ) ) ;
#52116=CARTESIAN_POINT ( 'NONE',  ( 0.9218200799623694763, -78.82291666666668561, 1.199500263597272465 ) ) ;
#52118=CARTESIAN_POINT ( 'NONE',  ( 0.3926218265389159190, -81.35416666666667140, 1.460959015002474715 ) ) ;
#52121=CIRCLE ( 'NONE', #37011, 1.500000000000000000 ) ;
#52155=CARTESIAN_POINT ( 'NONE',  ( -1.327128730425999992, -79.67025063774299554, 0.1315503032697999675 ) ) ;
#52171=CARTESIAN_POINT ( 'NONE',  ( 0.9218200799623741393, -80.57708333333334849, -1.199500263597268690 ) ) ;
#52179=CARTESIAN_POINT ( 'NONE',  ( 0.9961526269716999282, -81.04823719390898873, 0.8517633278984999556 ) ) ;
#52185=CARTESIAN_POINT ( 'NONE',  ( 1.130428667122000075, -80.17865684227599843, -1.152972209120999958 ) ) ;
#52210=CARTESIAN_POINT ( 'NONE',  ( -0.1963495408493673156, -78.28541666666667709, 1.499999999999999556 ) ) ;
#52225=CARTESIAN_POINT ( 'NONE',  ( 0.000000000000000000, -82.25000000001401190, 0.000000000000000000 ) ) ;
#52235=CARTESIAN_POINT ( 'NONE',  ( 1.310116429410000061, -79.00133983115898673, 0.1554359553024000085 ) ) ;
#52256=ORIENTED_EDGE ( 'NONE', *, *, #5956, .T. ) ;
#52257=CARTESIAN_POINT ( 'NONE',  ( -0.9110512128634435935, -78.58818742932150769, 0.8906210113203995027 ) ) ;
#52275=CARTESIAN_POINT ( 'NONE',  ( -1.500000000000000000, -78.00000000000000000, 0.000000000000000000 ) ) ;
#52287=CARTESIAN_POINT ( 'NONE',  ( 1.384987510431000102, -77.86983073899280328, 0.3030985439221999811 ) ) ;
#52315=CARTESIAN_POINT ( 'NONE',  ( -1.165026237870049997, -81.11652304393463453, 0.5177110879644187813 ) ) ;
#52352=CARTESIAN_POINT ( 'NONE',  ( 0.3926218265389159190, -81.85416666667249785, 1.460959015002474715 ) ) ;
#52412=VERTEX_POINT ( 'NONE', #56752 ) ;
#52415=ORIENTED_EDGE ( 'NONE', *, *, #14756, .T. ) ;
#52436=DIRECTION ( 'NONE',  ( 0.000000000000000000, 0.000000000000000000, -1.000000000000000000 ) ) ;
#52442=CARTESIAN_POINT ( 'NONE',  ( 0.000000000000000000, -75.67500000000001137, 0.000000000000000000 ) ) ;
#52450=CARTESIAN_POINT ( 'NONE',  ( -1.500000000000000222, -77.51041666666668561, -0.1963495408493622085 ) ) ;
#52466=FACE_OUTER_BOUND ( 'NONE', #28205, .T. ) ;
#52513=CARTESIAN_POINT ( 'NONE',  ( 1.310679582531387943, -78.70833333333332860, -0.7554284705563468760 ) ) ;
#52518=CARTESIAN_POINT ( 'NONE',  ( -0.5351185351402000245, -79.15017770130199892, 1.205899990410000067 ) ) ;
#52536=CARTESIAN_POINT ( 'NONE',  ( -1.500000000000000000, -78.39999999999999147, 0.000000000000000000 ) ) ;
#52547=ORIENTED_EDGE ( 'NONE', *, *, #35582, .T. ) ;
#52569=ORIENTED_EDGE ( 'NONE', *, *, #37977, .T. ) ;
#52572=CARTESIAN_POINT ( 'NONE',  ( -0.9004272109156999937, -80.67671995918098560, 0.9642496934733999492 ) ) ;
#52575=CARTESIAN_POINT ( 'NONE',  ( -1.377158602743000060, -77.62176762208750347, -0.3366111412210999743 ) ) ;
#52577=CARTESIAN_POINT ( 'NONE',  ( 0.000000000000000000, -76.29999999999999716, 0.000000000000000000 ) ) ;
#52600=CARTESIAN_POINT ( 'NONE',  ( -1.052442226633345967, -82.19782380993190429, -0.7179146240541253166 ) ) ;
#52679=DIRECTION ( 'NONE',  ( 0.7071067811865474617, -0.7071067811865474617, 8.138997328409543352E-11 ) ) ;
#52686=CARTESIAN_POINT ( 'NONE',  ( -1.199500263597274685, -78.94791666666668561, 0.9218200799623673669 ) ) ;
#52717=DIRECTION ( 'NONE',  ( 0.000000000000000000, 0.000000000000000000, -1.000000000000000000 ) ) ;
#52725=CARTESIAN_POINT ( 'NONE',  ( -0.8465867926663999121, -80.74519081100000051, -0.9556525628790000226 ) ) ;
#52738=CARTESIAN_POINT ( 'NONE',  ( 0.7341740840635999632, -80.89327854953300800, -1.113348630318000021 ) ) ;
#52753=CARTESIAN_POINT ( 'NONE',  ( -1.341023944040999893, -79.11523479771300060, -0.2092349045463000046 ) ) ;
#52756=CARTESIAN_POINT ( 'NONE',  ( 0.6811966951781786017, -82.14583333333094117, 1.183578528101640437 ) ) ;
#52779=CARTESIAN_POINT ( 'NONE',  ( -0.9218200799623778030, -81.32708333333334849, 1.199500263597266914 ) ) ;
#52796=CARTESIAN_POINT ( 'NONE',  ( -0.2914033309752999679, -79.01861702419900269, -1.588174433604999880 ) ) ;
#52797=CARTESIAN_POINT ( 'NONE',  ( 0.7554284705563509839, -78.66666666666667140, -1.310679582531385945 ) ) ;
#52802=CARTESIAN_POINT ( 'NONE',  ( 0.9218200799623694763, -80.82291666666668561, 1.199500263597272465 ) ) ;
#52804=CARTESIAN_POINT ( 'NONE',  ( -0.8575312565364999751, -77.81063687001270068, -1.002634541711000082 ) ) ;
#52822=CARTESIAN_POINT ( 'NONE',  ( -1.199500263597270244, -78.45208333333333428, -0.9218200799623728070 ) ) ;
#52856=CARTESIAN_POINT ( 'NONE',  ( -1.290198984414000050, -80.83131689367100137, -0.5875878301326999953 ) ) ;
#52859=CARTESIAN_POINT ( 'NONE',  ( 0.3098463080081999554, -78.90593676564900250, 1.484230999220000013 ) ) ;
#52886=ORIENTED_EDGE ( 'NONE', *, *, #3001, .T. ) ;
#52916=DIRECTION ( 'NONE',  ( 0.000000000000000000, -1.000000000000000000, 0.000000000000000000 ) ) ;
#52929=SURFACE_STYLE_FILL_AREA ( #6611 ) ;
#52958=LINE ( 'NONE', #17515, #48546 ) ;
#53003=DIRECTION ( 'NONE',  ( 0.000000000000000000, 0.000000000000000000, -1.000000000000000000 ) ) ;
#53018=CARTESIAN_POINT ( 'NONE',  ( -0.9820397338569999413, -80.80308451575899653, -0.7733679338621000099 ) ) ;
#53024=CARTESIAN_POINT ( 'NONE',  ( -0.2317941695893000198, -82.28827061000599485, -1.228320586388000013 ) ) ;
#53043=CARTESIAN_POINT ( 'NONE',  ( 1.330388504836999886, -79.83712754295498826, 0.7273297589862000034 ) ) ;
#53051=AXIS2_PLACEMENT_3D ( 'NONE', #52577, #2986, #15402 ) ;
#53085=CARTESIAN_POINT ( 'NONE',  ( -1.403403115923000044, -77.87752668643429388, 0.5665048067823000855 ) ) ;
#53109=AXIS2_PLACEMENT_3D ( 'NONE', #20868, #29997, #25294 ) ;
#53146=CARTESIAN_POINT ( 'NONE',  ( 1.310116429410000061, -78.91745489434200067, 0.1554359553024000085 ) ) ;
#53206=ADVANCED_FACE ( 'NONE', ( #41958 ), #14788, .T. ) ;
#53265=CIRCLE ( 'NONE', #49527, 2.799999999999999822 ) ;
#53271=CARTESIAN_POINT ( 'NONE',  ( -0.06533073702471998978, -80.61372138577100088, -1.613397371670999947 ) ) ;
#53276=CARTESIAN_POINT ( 'NONE',  ( 1.310679582531385279, -78.29166666666667140, 0.7554284705563519831 ) ) ;
#53289=CARTESIAN_POINT ( 'NONE',  ( -1.000649921775999873, -79.70818604951899999, 0.8816325131470000853 ) ) ;
#53308=CARTESIAN_POINT ( 'NONE',  ( -1.085072108435533256, -80.29443781902547528, -0.6701691410297031526 ) ) ;
#53311=FACE_OUTER_BOUND ( 'NONE', #55385, .T. ) ;
#53312=CARTESIAN_POINT ( 'NONE',  ( 1.221474390223999951, -81.43901740672500011, -0.5353283698298000326 ) ) ;
#53320=CARTESIAN_POINT ( 'NONE',  ( 0.5455113502570001494, -82.08278176514200197, 1.191738699715000127 ) ) ;
#53325=CARTESIAN_POINT ( 'NONE',  ( -0.3164422402712000482, -79.49559824363400651, 1.381999876370000102 ) ) ;
#53328=CARTESIAN_POINT ( 'NONE',  ( 0.1738511560287839264, -82.16536458333123960, 1.334635416660091556 ) ) ;
#53346=CARTESIAN_POINT ( 'NONE',  ( -1.199173895638943721, -81.84803276288215557, 0.9215510758497256205 ) ) ;
#53348=CARTESIAN_POINT ( 'NONE',  ( -0.3055749384948234781, -80.54406969723000032, 1.237013315672344627 ) ) ;
#53401=CARTESIAN_POINT ( 'NONE',  ( 0.000000000000000000, -76.29999999999999716, 0.000000000000000000 ) ) ;
#53417=PRODUCT_DEFINITION_CONTEXT ( 'detailed design', #45119, 'design' ) ;
#53430=CARTESIAN_POINT ( 'NONE',  ( -1.341023944040999893, -79.30986310998500244, -0.2092349045463000046 ) ) ;
#53432=CARTESIAN_POINT ( 'NONE',  ( -1.281518013001000211, -77.67713930981540216, -0.3132342491214999969 ) ) ;
#53450=CARTESIAN_POINT ( 'NONE',  ( 0.7735502751808678301, -78.92691180497098458, -1.012571407719350614 ) ) ;
#53459=CARTESIAN_POINT ( 'NONE',  ( 1.460959015002472494, -79.17083333333334849, 0.3926218265389232465 ) ) ;
#53486=ORIENTED_EDGE ( 'NONE', *, *, #28500, .F. ) ;
#53557=CARTESIAN_POINT ( 'NONE',  ( -0.8908853506697682612, -77.71360592741159223, -0.9112983582399447613 ) ) ;
#53565=FACE_OUTER_BOUND ( 'NONE', #42617, .T. ) ;
#53584=CARTESIAN_POINT ( 'NONE',  ( 0.6343572851480000496, -80.60121327037900585, 1.173101423079000005 ) ) ;
#53601=CARTESIAN_POINT ( 'NONE',  ( -1.149866947101319203, -79.78558583878638899, -0.5516533143361346259 ) ) ;
#53607=CARTESIAN_POINT ( 'NONE',  ( 0.8471236057751000414, -80.99834240209798963, 1.030027924806000028 ) ) ;
#53616=CARTESIAN_POINT ( 'NONE',  ( 1.252904471488000215, -81.00955937516098970, -0.6434491202905999740 ) ) ;
#53622=CARTESIAN_POINT ( 'NONE',  ( 0.5499573741622000300, -79.44598562025299771, 1.306754138290999956 ) ) ;
#53625=CARTESIAN_POINT ( 'NONE',  ( -1.230473908959625495, -82.23697916666547769, 0.3298056902639138754 ) ) ;
#53628=ORIENTED_EDGE ( 'NONE', *, *, #43151, .F. ) ;
#53647=DIRECTION ( 'NONE',  ( 1.000000000000000000, 3.791713626542000006E-11, -3.791713626542000006E-11 ) ) ;
#53656=CARTESIAN_POINT ( 'NONE',  ( 1.460959015002474493, -80.12916666666669130, -0.3926218265389176953 ) ) ;
#53669=CARTESIAN_POINT ( 'NONE',  ( -1.607511835558000035, -79.41551801124799681, -0.1512538100690999920 ) ) ;
#53673=CARTESIAN_POINT ( 'NONE',  ( 0.7554284705563453217, -80.83333333333335702, 1.310679582531389276 ) ) ;
#53677=CARTESIAN_POINT ( 'NONE',  ( -1.040416939902000237, -78.41750647927929663, -1.102939138596999991 ) ) ;
#53686=FACE_OUTER_BOUND ( 'NONE', #14071, .T. ) ;
#53733=CARTESIAN_POINT ( 'NONE',  ( 1.061497194196000082, -80.53940021773100000, -1.082666072229000020 ) ) ;
#53740=DIRECTION ( 'NONE',  ( 0.000000000000000000, 1.000000000000000000, 0.000000000000000000 ) ) ;
#53763=CARTESIAN_POINT ( 'NONE',  ( -1.500000000000000444, -79.38958333333333428, 0.1963495408493560745 ) ) ;
#53783=AXIS2_PLACEMENT_3D ( 'NONE', #33859, #24444, #56034 ) ;
#53837=EDGE_CURVE ( 'NONE', #15471, #35000, #26477, .T. ) ;
#53858=CARTESIAN_POINT ( 'NONE',  ( -1.249847342545643336, -77.66590148185295561, -0.2497756822732188076 ) ) ;
#53866=CARTESIAN_POINT ( 'NONE',  ( -1.599507418690000016, -82.00287484044099529, -0.2211225942084000251 ) ) ;
#53874=CARTESIAN_POINT ( 'NONE',  ( 0.9218200799623694763, -78.32291666666667140, 1.199500263597272465 ) ) ;
#53887=CARTESIAN_POINT ( 'NONE',  ( 0.6343572851480000496, -80.55743925279999473, 1.173101423079000005 ) ) ;
#53905=CARTESIAN_POINT ( 'NONE',  ( -0.9250595310797312676, -80.31033944340789787, -0.8763432897296752344 ) ) ;
#53909=CARTESIAN_POINT ( 'NONE',  ( -1.208084210770999922, -81.64330650605199935, 0.5648970606752000689 ) ) ;
#53921=CARTESIAN_POINT ( 'NONE',  ( -0.2266931603661999917, -82.18517820610701108, 1.390102994847999929 ) ) ;
#53928=CARTESIAN_POINT ( 'NONE',  ( -1.087531843820000121, -79.98596541309798624, 1.056511543117000018 ) ) ;
#53945=CARTESIAN_POINT ( 'NONE',  ( -1.500000000000000000, -80.00000000000000000, 0.000000000000000000 ) ) ;
#53947=CARTESIAN_POINT ( 'NONE',  ( -0.3925236660400593380, -81.79597738037770682, 1.460591605855642072 ) ) ;
#53948=ORIENTED_EDGE ( 'NONE', *, *, #45223, .T. ) ;
#53949=CARTESIAN_POINT ( 'NONE',  ( 1.169289758545334790, -80.43275932425954977, 0.5071859018191248181 ) ) ;
#53971=CARTESIAN_POINT ( 'NONE',  ( -1.163821121499999833, -78.96900440081799388, -1.119256147183999905 ) ) ;
#53976=CARTESIAN_POINT ( 'NONE',  ( 0.1963495408493571848, -79.76458333333334849, 1.500000000000000666 ) ) ;
#53977=CARTESIAN_POINT ( 'NONE',  ( 1.066951212256000092, -78.66556959618499434, 1.077291633113999891 ) ) ;
#53997=CARTESIAN_POINT ( 'NONE',  ( 0.1963495408493637351, -81.53541666666667709, -1.499999999999999778 ) ) ;
#54027=CARTESIAN_POINT ( 'NONE',  ( 0.6554565090088000368, -80.19211185406399522, 1.367230381797000183 ) ) ;
#54029=CARTESIAN_POINT ( 'NONE',  ( -0.9319389680074999793, -79.21513063462899140, -0.8127712196805999545 ) ) ;
#54041=CARTESIAN_POINT ( 'NONE',  ( -1.500000000000000000, -77.50000000000000000, 0.000000000000000000 ) ) ;
#54075=CARTESIAN_POINT ( 'NONE',  ( -1.310679582531386611, -81.04166666666668561, -0.7554284705563495406 ) ) ;
#54147=CARTESIAN_POINT ( 'NONE',  ( 0.5252637606625818467, -77.80901481852902180, -1.160894468899167364 ) ) ;
#54156=CARTESIAN_POINT ( 'NONE',  ( -0.2218574163239999952, -81.60597385339299592, -1.599372756014999952 ) ) ;
#54162=CARTESIAN_POINT ( 'NONE',  ( 1.460959015002472494, -78.27083333333335702, 0.3926218265389233020 ) ) ;
#54177=CARTESIAN_POINT ( 'NONE',  ( 0.9336649615752000697, -80.40860138265699675, -0.9522845488933000535 ) ) ;
#54191=CARTESIAN_POINT ( 'NONE',  ( -1.159125165887999964, -77.69135616363169561, 0.4678983327651999868 ) ) ;
#54197=DIRECTION ( 'NONE',  ( 0.000000000000000000, 1.000000000000000000, 0.000000000000000000 ) ) ;
#54199=CARTESIAN_POINT ( 'NONE',  ( -1.321095329625999959, -82.23281938082300258, -0.1826337427822999904 ) ) ;
#54210=CARTESIAN_POINT ( 'NONE',  ( 1.362073333348000181, -81.52683166077699184, -0.3585378043983000196 ) ) ;
#54216=CARTESIAN_POINT ( 'NONE',  ( 1.125436458607999901, -79.45174468460000128, 0.6884462015638999066 ) ) ;
#54221=VERTEX_POINT ( 'NONE', #12405 ) ;
#54236=CARTESIAN_POINT ( 'NONE',  ( -1.499529583595990090, -81.88967706888531950, 0.1963376940543553328 ) ) ;
#54239=CARTESIAN_POINT ( 'NONE',  ( -1.273668632959473745, -80.14653265090674950, 0.05892260551989451922 ) ) ;
#54252=CARTESIAN_POINT ( 'NONE',  ( -0.9218200799623714747, -79.97291666666667709, -1.199500263597270466 ) ) ;
#54253=EDGE_CURVE ( 'NONE', #46629, #19319, #25317, .T. ) ;
#54260=CARTESIAN_POINT ( 'NONE',  ( -1.250000000000000000, -82.25000000000000000, 8.279869130157999738E-11 ) ) ;
#54274=CARTESIAN_POINT ( 'NONE',  ( -0.6817061190079000133, -78.76479484294699773, 1.354333385606999896 ) ) ;
#54281=B_SPLINE_CURVE_WITH_KNOTS ( 'NONE', 3,
 ( #27620, #45660, #5203, #50672, #799, #18781, #36773, #32331, #19075, #24376, #52118, #11678, #29367, #33794, #24949, #38234, #33207, #29653 ),
 .UNSPECIFIED., .F., .F.,
 ( 4, 2, 2, 2, 2, 2, 2, 2, 4 ),
 ( 0.000000000000000000, 0.1250000000000000833, 0.2500000000000001665, 0.3750000000000001665, 0.5000000000000002220, 0.6250000000000002220, 0.7500000000000001110, 0.8750000000000001110, 1.000000000000000000 ),
 .UNSPECIFIED. ) ;
#54292=CARTESIAN_POINT ( 'NONE',  ( -0.7186926218484306350, -80.58590376313252079, -1.352462990148321831 ) ) ;
#54311=EDGE_LOOP ( 'NONE', ( #28281, #22822, #39246 ) ) ;
#54316=B_SPLINE_CURVE_WITH_KNOTS ( 'NONE', 3,
 ( #44998, #53858, #35528, #53557, #8982, #13391, #13096, #54147, #8682, #31684, #49730, #27259, #45298, #4849, #18429, #22845, #40858, #449, #36418, #38955, #33364, #15373, #11814, #38666, #2100, #7375, #24808, #19805, #47563, #6799, #38375, #42531, #56685, #16243, #6211, #38089, #34223, #10954, #20667, #52257, #29789, #7091, #16530, #11531, #15657, #56111, #55820, #25089, #51401, #24518, #15947, #56396, #24226, #42821, #47269, #33652, #2385, #47844, #28935, #51692, #11242, #34509, #46980, #56969, #43113 ),
 .UNSPECIFIED., .F., .F.,
 ( 4, 2, 2, 2, 2, 2, 2, 2, 2, 2, 2, 2, 2, 2, 2, 2, 1, 2, 2, 2, 2, 2, 2, 2, 2, 2, 2, 2, 2, 2, 2, 2, 4 ),
 ( 0.000000000000000000, 0.03125000000000000694, 0.06250000000000001388, 0.09375000000000002776, 0.1250000000000000278, 0.1562500000000000000, 0.1874999999999999722, 0.2187500000000000000, 0.2500000000000000000, 0.2812500000000000000, 0.3125000000000000000, 0.3437500000000000000, 0.3750000000000000000, 0.4062500000000000555, 0.4375000000000000555, 0.4687500000000000555, 0.5000000000000000000, 0.5312500000000000000, 0.5625000000000000000, 0.5937500000000000000, 0.6250000000000000000, 0.6562500000000000000, 0.6875000000000000000, 0.7187500000000000000, 0.7500000000000000000, 0.7812500000000001110, 0.8125000000000001110, 0.8437500000000001110, 0.8750000000000001110, 0.9062500000000001110, 0.9375000000000001110, 0.9687500000000001110, 1.000000000000000000 ),
 .UNSPECIFIED. ) ;
#54323=CARTESIAN_POINT ( 'NONE',  ( 1.504745031191999871, -80.09288660730200604, -0.1862378672923999945 ) ) ;
#54325=CARTESIAN_POINT ( 'NONE',  ( -0.9052918118899000444, -78.22287816700719532, -0.9596938812619000281 ) ) ;
#54334=DIRECTION ( 'NONE',  ( 0.000000000000000000, 1.000000000000000000, 0.000000000000000000 ) ) ;
#54341=CARTESIAN_POINT ( 'NONE',  ( -0.4877208950597860526, -82.24320891948377721, -1.155849057614090514 ) ) ;
#54372=VECTOR ( 'NONE', #40376, 1000.000000000000114 ) ;
#54373=CARTESIAN_POINT ( 'NONE',  ( 1.250000000000000000, -76.29999999999999716, -0.6999999999999999556 ) ) ;
#54454=CARTESIAN_POINT ( 'NONE',  ( -0.7881893378370999903, -81.40752335986800858, 1.409245008412000066 ) ) ;
#54459=CARTESIAN_POINT ( 'NONE',  ( -1.500000000000000000, -77.89999999999999147, 0.000000000000000000 ) ) ;
#54471=CARTESIAN_POINT ( 'NONE',  ( -0.2976639488673999967, -79.65857342613799119, 1.299989344602000108 ) ) ;
#54485=CARTESIAN_POINT ( 'NONE',  ( -1.309352690804000074, -78.23709502082350298, -0.2533212985548999874 ) ) ;
#54494=CARTESIAN_POINT ( 'NONE',  ( 0.8962411872155999770, -81.58201667106600041, 0.9875868993909000526 ) ) ;
#54506=CARTESIAN_POINT ( 'NONE',  ( -1.183389931723999977, -81.70658373923900797, 0.5633908112155999737 ) ) ;
#54517=EDGE_LOOP ( 'NONE', ( #33945, #55828, #21612, #3330, #45537 ) ) ;
#54520=LINE ( 'NONE', #36492, #34937 ) ;
#54526=EDGE_LOOP ( 'NONE', ( #8397, #35379, #36074, #33218 ) ) ;
#54552=CARTESIAN_POINT ( 'NONE',  ( -1.310962691340256780, -81.76182832648821375, -0.1935753109423370699 ) ) ;
#54555=CARTESIAN_POINT ( 'NONE',  ( -1.087669557110363838, -82.13271128940070298, -0.8608145078121063332 ) ) ;
#54567=CARTESIAN_POINT ( 'NONE',  ( -0.9855275769405000830, -77.92138024546849806, -1.152289182367999931 ) ) ;
#54584=DIRECTION ( 'NONE',  ( 0.000000000000000000, -1.000000000000000000, 0.000000000000000000 ) ) ;
#54585=CARTESIAN_POINT ( 'NONE',  ( 0.3926218265389221362, -81.54583333333334849, -1.460959015002473160 ) ) ;
#54589=ORIENTED_EDGE ( 'NONE', *, *, #22079, .T. ) ;
#54591=ADVANCED_FACE ( 'NONE', ( #2845 ), #36906, .T. ) ;
#54597=VERTEX_POINT ( 'NONE', #11997 ) ;
#54612=CARTESIAN_POINT ( 'NONE',  ( -0.7062052416310000691, -80.93630120477999412, -1.233256579520999763 ) ) ;
#54630=CARTESIAN_POINT ( 'NONE',  ( -0.5849236359613864122, -82.23641784656102516, -1.109830192218287825 ) ) ;
#54660=ORIENTED_EDGE ( 'NONE', *, *, #38891, .T. ) ;
#54678=CARTESIAN_POINT ( 'NONE',  ( 1.199500263597268246, -77.80208333333335702, 0.9218200799623752495 ) ) ;
#54679=CARTESIAN_POINT ( 'NONE',  ( -1.107979503908000041, -78.05676310382339977, -1.174561767264999945 ) ) ;
#54715=CARTESIAN_POINT ( 'NONE',  ( 1.500000000000000000, -80.25000000000000000, 0.000000000000000000 ) ) ;
#54725=EDGE_LOOP ( 'NONE', ( #34441, #56991, #14797, #56769 ) ) ;
#54733=CARTESIAN_POINT ( 'NONE',  ( 0.9005648571752999931, -80.92291525475098979, 1.095007794218000097 ) ) ;
#54748=FACE_OUTER_BOUND ( 'NONE', #43774, .T. ) ;
#54749=CARTESIAN_POINT ( 'NONE',  ( -1.500000000000000000, -78.39999999999999147, 0.000000000000000000 ) ) ;
#54765=CARTESIAN_POINT ( 'NONE',  ( -1.150888948972000003, -79.13596084748500914, 0.6738713386821000295 ) ) ;
#54768=EDGE_CURVE ( 'NONE', #33739, #43690, #28302, .T. ) ;
#54784=CARTESIAN_POINT ( 'NONE',  ( -1.096457908046999830, -82.34294633480099890, 1.170898023252000097 ) ) ;
#54791=CARTESIAN_POINT ( 'NONE',  ( 1.187026915874999755, -80.44399715222199632, 0.5757885860275999690 ) ) ;
#54795=CARTESIAN_POINT ( 'NONE',  ( 0.9218200799623741393, -79.07708333333334849, -1.199500263597268690 ) ) ;
#54828=CARTESIAN_POINT ( 'NONE',  ( -1.185397549814999785, -80.17221547735599074, -0.6110718436566999756 ) ) ;
#54844=CARTESIAN_POINT ( 'NONE',  ( 1.499999999999999778, -79.66041666666667709, 0.1963495408493654004 ) ) ;
#54845=CARTESIAN_POINT ( 'NONE',  ( -0.9215294167384999735, -77.86600855774059937, -1.077461862040000051 ) ) ;
#54854=DIRECTION ( 'NONE',  ( 0.000000000000000000, -1.000000000000000000, 0.000000000000000000 ) ) ;
#54863=LINE ( 'NONE', #50454, #34587 ) ;
#54885=CARTESIAN_POINT ( 'NONE',  ( 1.500000000000000000, -78.64999999999999147, 0.000000000000000000 ) ) ;
#54890=EDGE_CURVE ( 'NONE', #38477, #45960, #44331, .T. ) ;
#54892=CARTESIAN_POINT ( 'NONE',  ( -0.5899402231854000700, -79.50329419107600870, -1.503093382721999882 ) ) ;
#54947=ORIENTED_EDGE ( 'NONE', *, *, #43314, .F. ) ;
#54958=B_SPLINE_CURVE_WITH_KNOTS ( 'NONE', 3,
 ( #50481, #6464, #41903, #55480 ),
 .UNSPECIFIED., .F., .F.,
 ( 4, 4 ),
 ( 0.000000000000000000, 1.000000000000000000 ),
 .UNSPECIFIED. ) ;
#54998=FACE_OUTER_BOUND ( 'NONE', #17561, .T. ) ;
#55024=CARTESIAN_POINT ( 'NONE',  ( -0.1948004972424999814, -81.71671722884900646, -1.404319104179999833 ) ) ;
#55055=CARTESIAN_POINT ( 'NONE',  ( -1.182296476285000120, -78.68360863125299431, 0.6170503964917000150 ) ) ;
#55056=CARTESIAN_POINT ( 'NONE',  ( -3.999999999993000266, -77.30000000000720206, 8.632643823722999667E-11 ) ) ;
#55074=CARTESIAN_POINT ( 'NONE',  ( -1.328207365693999886, -82.38162415354899792, -0.5054827672177999442 ) ) ;
#55081=CARTESIAN_POINT ( 'NONE',  ( 1.010832202629999843, -79.35251943783799788, -0.8478131160371998876 ) ) ;
#55100=EDGE_LOOP ( 'NONE', ( #41810, #31645, #52547, #25887, #49704 ) ) ;
#55115=CARTESIAN_POINT ( 'NONE',  ( -0.9102058945833000347, -80.56911646440499908, 0.9747214924314999696 ) ) ;
#55154=CARTESIAN_POINT ( 'NONE',  ( 0.9218200799623741393, -78.57708333333334849, -1.199500263597268690 ) ) ;
#55236=ORIENTED_EDGE ( 'NONE', *, *, #34450, .T. ) ;
#55243=CARTESIAN_POINT ( 'NONE',  ( -1.199500263597274241, -80.34791666666667709, 0.9218200799623669228 ) ) ;
#55254=CARTESIAN_POINT ( 'NONE',  ( 1.136236858042999787, -78.30482622072879906, 1.147248764840999913 ) ) ;
#55272=CARTESIAN_POINT ( 'NONE',  ( 1.201075292024272434, -77.97281434202166395, -0.4271495449073431372 ) ) ;
#55290=AXIS2_PLACEMENT_3D ( 'NONE', #55573, #47617, #33992 ) ;
#55292=CARTESIAN_POINT ( 'NONE',  ( 1.460959015002474048, -79.72916666666668561, -0.3926218265389178064 ) ) ;
#55293=AXIS2_PLACEMENT_3D ( 'NONE', #12854, #54197, #36181 ) ;
#55306=CARTESIAN_POINT ( 'NONE',  ( 1.500000000000000000, -78.14999999999999147, 0.000000000000000000 ) ) ;
#55314=CARTESIAN_POINT ( 'NONE',  ( -0.8736801639325000313, -80.67485213784600262, -1.116492654993999967 ) ) ;
#55349=CARTESIAN_POINT ( 'NONE',  ( -0.5409299486741000473, -79.08634822410400034, 1.218996123443000013 ) ) ;
#55350=LINE ( 'NONE', #55056, #27003 ) ;
#55366=CARTESIAN_POINT ( 'NONE',  ( -0.7686600910219999472, -81.77030236145701281, 1.295400560101000131 ) ) ;
#55379=DIRECTION ( 'NONE',  ( 0.000000000000000000, -1.000000000000000000, 0.000000000000000000 ) ) ;
#55385=EDGE_LOOP ( 'NONE', ( #27043, #56974, #24863, #4577 ) ) ;
#55409=CARTESIAN_POINT ( 'NONE',  ( 1.021809889922000059, -79.32880087987798845, -0.8570204080543000202 ) ) ;
#55417=CARTESIAN_POINT ( 'NONE',  ( -0.9058031679606026731, -82.18505110562824711, 0.9672994567659488618 ) ) ;
#55422=AXIS2_PLACEMENT_3D ( 'NONE', #46699, #6513, #15075 ) ;
#55425=DIRECTION ( 'NONE',  ( 0.000000000000000000, -0.7071067811865475727, -0.7071067811865475727 ) ) ;
#55438=B_SPLINE_CURVE_WITH_KNOTS ( 'NONE', 3,
 ( #21079, #16658, #15788, #34351 ),
 .UNSPECIFIED., .F., .F.,
 ( 4, 4 ),
 ( 0.000000000000000000, 1.000000000000000000 ),
 .UNSPECIFIED. ) ;
#55440=CARTESIAN_POINT ( 'NONE',  ( 0.1963495408493638184, -81.63541666666668561, -1.499999999999999778 ) ) ;
#55452=CARTESIAN_POINT ( 'NONE',  ( -0.1120320062231000002, -77.79642001619639302, -1.328911429676000067 ) ) ;
#55480=CARTESIAN_POINT ( 'NONE',  ( -0.6747260877994001316, -82.25000000000000000, -1.052256958371999840 ) ) ;
#55499=AXIS2_PLACEMENT_3D ( 'NONE', #57215, #12345, #35044 ) ;
#55508=DIRECTION ( 'NONE',  ( -0.7071067811865474617, -0.7071067811865474617, -8.139044558222544110E-11 ) ) ;
#55536=CARTESIAN_POINT ( 'NONE',  ( 0.7554284705563452107, -80.23333333333330586, 1.310679582531388609 ) ) ;
#55545=CARTESIAN_POINT ( 'NONE',  ( 1.010832202629999843, -79.43640437465400339, -0.8478131160371998876 ) ) ;
#55573=CARTESIAN_POINT ( 'NONE',  ( 0.000000000000000000, -77.29999999999999716, 0.000000000000000000 ) ) ;
#55575=CARTESIAN_POINT ( 'NONE',  ( 0.2153359604882000011, -82.08398151067899562, 1.316133176457000120 ) ) ;
#55609=CARTESIAN_POINT ( 'NONE',  ( -0.7514556209146998622, -81.02214050151400215, 1.202236998062000239 ) ) ;
#55611=ORIENTED_EDGE ( 'NONE', *, *, #12268, .T. ) ;
#55622=CARTESIAN_POINT ( 'NONE',  ( -1.417334032777999964, -79.02654225787900089, -0.4910847579886000736 ) ) ;
#55646=ORIENTED_EDGE ( 'NONE', *, *, #6448, .T. ) ;
#55660=CARTESIAN_POINT ( 'NONE',  ( -0.5022895558335001009, -81.30840176356799986, 1.523433483890000106 ) ) ;
#55666=CARTESIAN_POINT ( 'NONE',  ( -1.310679582531389276, -80.85833333333332007, 0.7554284705563443225 ) ) ;
#55716=CYLINDRICAL_SURFACE ( 'NONE', #8524, 1.500000000000000000 ) ;
#55722=CARTESIAN_POINT ( 'NONE',  ( 0.6791306551168999617, -81.30185674818700647, -1.147762040996999966 ) ) ;
#55724=CARTESIAN_POINT ( 'NONE',  ( 0.000000000000000000, -76.39999999999999147, 0.5999999999999999778 ) ) ;
#55727=FACE_OUTER_BOUND ( 'NONE', #47934, .T. ) ;
#55736=DIRECTION ( 'NONE',  ( 0.000000000000000000, -1.000000000000000000, 0.000000000000000000 ) ) ;
#55750=CARTESIAN_POINT ( 'NONE',  ( -0.2406813341972999787, -78.78867248381800437, -1.311734976874999958 ) ) ;
#55820=CARTESIAN_POINT ( 'NONE',  ( -0.1930468007397637131, -78.76310372970323215, -1.260176113982175217 ) ) ;
#55828=ORIENTED_EDGE ( 'NONE', *, *, #15972, .T. ) ;
#55841=EDGE_CURVE ( 'NONE', #9701, #37791, #34183, .T. ) ;
#55848=CARTESIAN_POINT ( 'NONE',  ( -0.6549273519428999712, -78.90017770130199892, 1.475891481164999908 ) ) ;
#55866=CARTESIAN_POINT ( 'NONE',  ( 0.03840548688684078393, -77.87740459572674467, -1.273959412799388291 ) ) ;
#55876=CARTESIAN_POINT ( 'NONE',  ( -0.9657971644277000278, -82.28243200420399717, -0.9195906491977999808 ) ) ;
#55888=CARTESIAN_POINT ( 'NONE',  ( -1.199500263597274685, -80.44791666666668561, 0.9218200799623673669 ) ) ;
#55906=CARTESIAN_POINT ( 'NONE',  ( 1.018949564034999922, -81.36366980083398914, 1.122801824928000070 ) ) ;
#55957=CARTESIAN_POINT ( 'NONE',  ( -1.448341597990999929, -81.87269880242300246, 0.6895295675035000293 ) ) ;
#56001=CARTESIAN_POINT ( 'NONE',  ( -0.8465867926663999121, -80.70141679342098939, -0.9556525628790000226 ) ) ;
#56014=CARTESIAN_POINT ( 'NONE',  ( 1.199500263597271799, -77.69791666666667140, -0.9218200799623701425 ) ) ;
#56034=DIRECTION ( 'NONE',  ( -1.000000000000000000, 0.000000000000000000, 0.000000000000000000 ) ) ;
#56039=CARTESIAN_POINT ( 'NONE',  ( 0.1443438050804999873, -78.04448313310169283, 1.325798245762999983 ) ) ;
#56064=CARTESIAN_POINT ( 'NONE',  ( 1.500000000000000000, -80.25000000000000000, 0.000000000000000000 ) ) ;
#56111=CARTESIAN_POINT ( 'NONE',  ( -0.6620585326085253186, -78.73130076599741756, -1.088327036680617255 ) ) ;
#56119=ORIENTED_EDGE ( 'NONE', *, *, #47202, .T. ) ;
#56130=AXIS2_PLACEMENT_3D ( 'NONE', #2516, #34651, #43248 ) ;
#56139=CARTESIAN_POINT ( 'NONE',  ( 1.301389418711000223, -77.82021811561179447, -0.5625343731648000389 ) ) ;
#56155=CARTESIAN_POINT ( 'NONE',  ( -1.244679651825236766, -78.76789556114634649, -0.2779941050184971396 ) ) ;
#56163=CARTESIAN_POINT ( 'NONE',  ( 0.05911904726909338048, -81.02111415281734708, 1.273296317862433025 ) ) ;
#56165=ADVANCED_FACE ( 'NONE', ( #27371 ), #16972, .T. ) ;
#56166=CARTESIAN_POINT ( 'NONE',  ( -0.6509962010243000030, -81.68124191782798960, 1.163950211895000031 ) ) ;
#56176=ORIENTED_EDGE ( 'NONE', *, *, #54768, .F. ) ;
#56203=CARTESIAN_POINT ( 'NONE',  ( 1.500000000000000888, -78.23958333333330017, -0.1963495408493590444 ) ) ;
#56213=LINE ( 'NONE', #52080, #38848 ) ;
#56220=FACE_OUTER_BOUND ( 'NONE', #5636, .T. ) ;
#56280=CIRCLE ( 'NONE', #29871, 0.5000000000000000000 ) ;
#56302=CARTESIAN_POINT ( 'NONE',  ( 1.193978368322000216, -81.84759560537901280, -0.5941311122250999555 ) ) ;
#56317=CARTESIAN_POINT ( 'NONE',  ( -1.310679582531386611, -81.54166666666668561, -0.7554284705563495406 ) ) ;
#56329=CARTESIAN_POINT ( 'NONE',  ( -1.210921577777000158, -78.09993436228529617, 0.5587889421650999999 ) ) ;
#56336=ORIENTED_EDGE ( 'NONE', *, *, #41177, .F. ) ;
#56348=ADVANCED_FACE ( 'NONE', ( #37984 ), #55716, .T. ) ;
#56371=CARTESIAN_POINT ( 'NONE',  ( -0.7554284705563480973, -78.58333333333332860, -1.310679582531387277 ) ) ;
#56384=DIRECTION ( 'NONE',  ( 0.000000000000000000, -1.000000000000000000, 0.000000000000000000 ) ) ;
#56396=CARTESIAN_POINT ( 'NONE',  ( 1.209689523629019714, -78.87441410267364006, -0.3994885700558234998 ) ) ;
#56403=B_SPLINE_CURVE_WITH_KNOTS ( 'NONE', 3,
 ( #38359, #51678, #56667, #46962, #16223, #15054, #37484, #28324, #51958, #10643 ),
 .UNSPECIFIED., .F., .F.,
 ( 4, 2, 2, 2, 4 ),
 ( 0.000000000000000000, 0.2500000000000000555, 0.5000000000000001110, 0.7500000000000002220, 1.000000000000000000 ),
 .UNSPECIFIED. ) ;
#56413=CARTESIAN_POINT ( 'NONE',  ( -0.7022187824378000043, -82.19906693409399168, -1.095132696781000003 ) ) ;
#56427=CARTESIAN_POINT ( 'NONE',  ( 0.2897255177615999933, -78.96130845337700066, 1.387848051154999762 ) ) ;
#56443=CARTESIAN_POINT ( 'NONE',  ( 1.239585895167351959, -78.48166632226170236, -0.2976318702780533787 ) ) ;
#56450=CARTESIAN_POINT ( 'NONE',  ( 1.264835035987859069, -80.90980377984654126, 0.1533566471899267813 ) ) ;
#56464=CARTESIAN_POINT ( 'NONE',  ( -1.416666666666666741, -77.85000000000000853, 0.000000000000000000 ) ) ;
#56490=CARTESIAN_POINT ( 'NONE',  ( 0.1963495408493638184, -78.13541666666668561, -1.499999999999999778 ) ) ;
#56491=EDGE_CURVE ( 'NONE', #49068, #1594, #36502, .T. ) ;
#56514=CARTESIAN_POINT ( 'NONE',  ( -0.9420598709024999851, -79.32273412940499213, -0.8215979549846998964 ) ) ;
#56528=CARTESIAN_POINT ( 'NONE',  ( 0.9218200799623742503, -80.17708333333334281, -1.199500263597268912 ) ) ;
#56539=CARTESIAN_POINT ( 'NONE',  ( -0.9218200799623775810, -78.92708333333332860, 1.199500263597266247 ) ) ;
#56544=EDGE_CURVE ( 'NONE', #41507, #38110, #47100, .T. ) ;
#56567=DIRECTION ( 'NONE',  ( 0.000000000000000000, 1.000000000000000000, 0.000000000000000000 ) ) ;
#56576=CARTESIAN_POINT ( 'NONE',  ( 1.137658753740000028, -79.47180014421898875, 0.6959227610743999870 ) ) ;
#56578=DIRECTION ( 'NONE',  ( 0.000000000000000000, 1.000000000000000000, 0.000000000000000000 ) ) ;
#56598=VERTEX_POINT ( 'NONE', #2576 ) ;
#56607=CARTESIAN_POINT ( 'NONE',  ( -1.397510954313999854, -79.53369273832200292, -0.8088121278437000461 ) ) ;
#56609=CARTESIAN_POINT ( 'NONE',  ( 0.000000000000000000, -77.50000000000000000, 0.000000000000000000 ) ) ;
#56633=CARTESIAN_POINT ( 'NONE',  ( 1.245336569551569461, -79.38326152196685825, -0.2691890748858687399 ) ) ;
#56636=CARTESIAN_POINT ( 'NONE',  ( 1.499999999999999778, -80.66041666666667709, 0.1963495408493654004 ) ) ;
#56667=CARTESIAN_POINT ( 'NONE',  ( -0.7186926218484306350, -80.98590376313251227, -1.352462990148321831 ) ) ;
#56684=ORIENTED_EDGE ( 'NONE', *, *, #6168, .F. ) ;
#56685=CARTESIAN_POINT ( 'NONE',  ( 1.308909830689670484, -78.41327112893952744, 0.2203332426835378777 ) ) ;
#56714=CARTESIAN_POINT ( 'NONE',  ( -0.5991125319583999742, -80.32943159551300027, -1.175427489992000085 ) ) ;
#56718=CARTESIAN_POINT ( 'NONE',  ( 0.9474668951539000350, -77.91944336237389734, 1.054687619119999864 ) ) ;
#56736=CARTESIAN_POINT ( 'NONE',  ( 1.104063888217883260, -78.95871505373607135, -0.6377135191370438827 ) ) ;
#56743=CARTESIAN_POINT ( 'NONE',  ( -0.3336506835427100470, -81.54586305396269097, 1.229856053167274421 ) ) ;
#56752=CARTESIAN_POINT ( 'NONE',  ( 1.250000000000000000, -76.29999999999999716, 0.6999999999999999556 ) ) ;
#56769=ORIENTED_EDGE ( 'NONE', *, *, #14422, .F. ) ;
#56774=VERTEX_POINT ( 'NONE', #37280 ) ;
#56787=LINE ( 'NONE', #31338, #38018 ) ;
#56812=DIRECTION ( 'NONE',  ( 0.000000000000000000, 1.000000000000000000, 0.000000000000000000 ) ) ;
#56823=ADVANCED_FACE ( 'NONE', ( #49863, #41279 ), #18849, .F. ) ;
#56830=CARTESIAN_POINT ( 'NONE',  ( 0.7554284705563453217, -78.83333333333332860, 1.310679582531389276 ) ) ;
#56866=CARTESIAN_POINT ( 'NONE',  ( -1.261445002938999860, -79.23443596263800259, -0.1968185027220000216 ) ) ;
#56877=CARTESIAN_POINT ( 'NONE',  ( -0.2977330905706521147, -79.35624198045864830, -1.239186237762031739 ) ) ;
#56878=B_SPLINE_SURFACE_WITH_KNOTS ( 'NONE', 3, 3, ( 
 ( #48959, #12357, #30346, #52804, #16796, #39791, #17364, #30921, #35350, #48388, #2651, #7639, #7926, #20928, #43093, #43950, #8502, #3501, #43664, #12075, #20645, #38929, #25926, #21503, #57515, #56946, #35057, #52235, #29766, #34488, #52518, #47823, #17075, #25639, #7353 ),
 ( #30056, #31810, #9687, #54845, #22074, #855, #27386, #35649, #27674, #45128, #18259, #26793, #49852, #4680, #22678, #572, #17662, #13516, #40981, #31510, #58398, #14106, #13217, #9397, #22379, #32103, #31211, #18839, #13808, #36253, #45422, #18551, #22971, #36832, #40689 ),
 ( #5255, #49555, #44822, #54567, #50144, #35951, #27090, #40083, #26497, #58099, #44521, #36545, #45720, #53677, #23262, #41271, #4376, #14391, #53977, #32389, #54274, #4072, #50433, #49250, #8801, #40389, #17960, #9100, #44227, #43943, #12917, #21780, #26786, #17952, #58093 ),
 ( #53085, #30631, #16789, #17653, #3776, #49243, #17068, #34772, #35944, #9093, #57507, #8793, #39784, #57798, #44815, #45122, #30915, #48381, #30339, #35344, #21497, #22370, #35641, #53971, #52796, #12351, #48951, #21204, #44514, #13509, #40382, #57224, #53669, #35050, #17356 ) ),
 .UNSPECIFIED., .F., .F., .F.,
 ( 4, 4 ),
 ( 4, 1, 1, 1, 1, 1, 1, 1, 1, 1, 1, 1, 1, 1, 1, 1, 1, 1, 1, 1, 1, 1, 1, 1, 1, 1, 1, 1, 1, 1, 1, 1, 4 ),
 ( -0.05371687727926999917, 1.053716877278999986 ),
 ( -0.02000000000000000042, 0.01250000000000000069, 0.04499999999999999833, 0.07749999999999999944, 0.1100000000000000006, 0.1424999999999999878, 0.1749999999999999889, 0.2074999999999999900, 0.2399999999999999911, 0.2725000000000000200, 0.3049999999999999933, 0.3375000000000000222, 0.3699999999999999956, 0.4025000000000000244, 0.4349999999999999978, 0.4675000000000000266, 0.5000000000000000000, 0.5324999999999999734, 0.5649999999999999467, 0.5975000000000000311, 0.6300000000000000044, 0.6624999999999999778, 0.6949999999999999512, 0.7275000000000000355, 0.7600000000000000089, 0.7924999999999999822, 0.8249999999999999556, 0.8575000000000000400, 0.8900000000000000133, 0.9224999999999999867, 0.9549999999999999600, 0.9875000000000000444, 1.020000000000000018 ),
 .UNSPECIFIED. ) ;
#56882=CARTESIAN_POINT ( 'NONE',  ( -0.7554284705563480973, -77.58333333333332860, -1.310679582531387277 ) ) ;
#56883=CARTESIAN_POINT ( 'NONE',  ( -1.500000000000000000, -80.40000000000000568, 0.000000000000000000 ) ) ;
#56898=CARTESIAN_POINT ( 'NONE',  ( 0.6263439973055000554, -79.33524224479700138, 1.488256452092999949 ) ) ;
#56924=CARTESIAN_POINT ( 'NONE',  ( -0.7554284705563540925, -78.31666666666669130, 1.310679582531384391 ) ) ;
#56946=CARTESIAN_POINT ( 'NONE',  ( 0.5643133282633999714, -78.90211458439600278, -1.192525073705999805 ) ) ;
#56958=CARTESIAN_POINT ( 'NONE',  ( -1.338466228091430121, -79.37677412509060559, -0.4637437491872735129 ) ) ;
#56969=CARTESIAN_POINT ( 'NONE',  ( -1.262741469898344793, -79.16064077602601401, -0.1731769364601504491 ) ) ;
#56971=DIRECTION ( 'NONE',  ( 2.250403632142151042E-08, -0.7071067811865473507, 0.7071067811865473507 ) ) ;
#56974=ORIENTED_EDGE ( 'NONE', *, *, #49486, .T. ) ;
#56984=DIRECTION ( 'NONE',  ( 0.000000000000000000, 1.000000000000000000, 0.000000000000000000 ) ) ;
#56991=ORIENTED_EDGE ( 'NONE', *, *, #9555, .T. ) ;
#56994=CARTESIAN_POINT ( 'NONE',  ( 0.6743760579952999823, -80.63286640014699458, 1.247107161604999792 ) ) ;
#56997=CARTESIAN_POINT ( 'NONE',  ( -0.9215294167384999735, -77.67138024546849806, -1.077461862040000051 ) ) ;
#57014=CARTESIAN_POINT ( 'NONE',  ( 0.1162945074421486008, -79.11773129756168998, 1.269215488990788954 ) ) ;
#57021=CARTESIAN_POINT ( 'NONE',  ( -1.274109108748103569, -82.15011936437316820, 0.001084848989539045992 ) ) ;
#57022=VERTEX_POINT ( 'NONE', #46828 ) ;
#57060=CARTESIAN_POINT ( 'NONE',  ( 0.9218200799623694763, -81.82291666667074992, 1.199500263597272465 ) ) ;
#57090=CARTESIAN_POINT ( 'NONE',  ( -1.250000000000000000, -76.29999999999999716, 0.000000000000000000 ) ) ;
#57094=B_SPLINE_CURVE_WITH_KNOTS ( 'NONE', 3,
 ( #23995, #19874, #55292, #14841, #33432, #15138, #32254, #51175, #24297, #10429, #5409, #5987, #51469, #42012, #42311, #18995, #5128, #14257 ),
 .UNSPECIFIED., .F., .F.,
 ( 4, 2, 2, 2, 2, 2, 2, 2, 4 ),
 ( 0.000000000000000000, 0.1250000000000000000, 0.2500000000000000000, 0.3750000000000000000, 0.5000000000000000000, 0.6250000000000000000, 0.7500000000000000000, 0.8750000000000000000, 1.000000000000000000 ),
 .UNSPECIFIED. ) ;
#57102=FACE_OUTER_BOUND ( 'NONE', #20976, .T. ) ;
#57131=EDGE_LOOP ( 'NONE', ( #33078, #45274, #12137, #15940 ) ) ;
#57149=CARTESIAN_POINT ( 'NONE',  ( -0.6211595220380999871, -80.71795433454799706, -1.084739991049000096 ) ) ;
#57159=CARTESIAN_POINT ( 'NONE',  ( -0.05395919428434999693, -80.84366592615199920, -1.332567581519000122 ) ) ;
#57191=ORIENTED_EDGE ( 'NONE', *, *, #29906, .T. ) ;
#57203=CARTESIAN_POINT ( 'NONE',  ( 1.460959015002472494, -81.17083333333333428, 0.3926218265389232465 ) ) ;
#57215=CARTESIAN_POINT ( 'NONE',  ( 0.000000000000000000, -82.50000000000000000, 0.000000000000000000 ) ) ;
#57216=CARTESIAN_POINT ( 'NONE',  ( -0.5875803945788578009, -81.33860554734724246, -1.187789484363859893 ) ) ;
#57224=CARTESIAN_POINT ( 'NONE',  ( -1.393431170853000056, -79.36590538786700222, 0.8158852592188999830 ) ) ;
#57249=CARTESIAN_POINT ( 'NONE',  ( -1.310679582531386389, -78.44166666666667709, -0.7554284705563492075 ) ) ;
#57282=CARTESIAN_POINT ( 'NONE',  ( -1.294028136707999987, -80.72633258256199440, 0.2571518259264999884 ) ) ;
#57283=CARTESIAN_POINT ( 'NONE',  ( 0.000000000000000000, -75.67500000000001137, 0.000000000000000000 ) ) ;
#57284=CARTESIAN_POINT ( 'NONE',  ( -0.6983046762106999150, -78.01866860913609969, 1.233867887851000100 ) ) ;
#57289=DIRECTION ( 'NONE',  ( -1.000000000000000000, 0.000000000000000000, 0.000000000000000000 ) ) ;
#57310=CARTESIAN_POINT ( 'NONE',  ( 1.144405438199589842, -81.86389269102102162, -0.5616028373579852184 ) ) ;
#57340=CARTESIAN_POINT ( 'NONE',  ( 0.000000000000000000, -75.67500000000001137, 0.000000000000000000 ) ) ;
#57357=CARTESIAN_POINT ( 'NONE',  ( 0.000000000000000000, -82.29687500001199396, 0.000000000000000000 ) ) ;
#57366=CARTESIAN_POINT ( 'NONE',  ( -0.6081994495308999937, -82.21302711298000077, -1.142242026498999863 ) ) ;
#57448=CARTESIAN_POINT ( 'NONE',  ( 1.268713167172250245, -80.00820858014098746, 0.1245986402332493470 ) ) ;
#57451=CARTESIAN_POINT ( 'NONE',  ( -1.179157772963000061, -82.09565872228399996, 0.6230118014947999550 ) ) ;
#57454=CARTESIAN_POINT ( 'NONE',  ( -0.09713983013762958474, -79.51964965042942879, -1.537455523586754857 ) ) ;
#57465=CARTESIAN_POINT ( 'NONE',  ( -1.390602365772999782, -80.58707595801800494, 0.2763432473779000587 ) ) ;
#57470=ORIENTED_EDGE ( 'NONE', *, *, #25665, .T. ) ;
#57485=CARTESIAN_POINT ( 'NONE',  ( -0.01872868506982610856, -79.52637485864291023, 1.273763531464531695 ) ) ;
#57507=CARTESIAN_POINT ( 'NONE',  ( -0.7952960770845000082, -78.32404029686399838, 1.405246626978000180 ) ) ;
#57512=CARTESIAN_POINT ( 'NONE',  ( 1.500000000000000000, -80.76041666666668561, 0.1963495408493652339 ) ) ;
#57515=CARTESIAN_POINT ( 'NONE',  ( -0.2380956042587999977, -78.85250196101499398, -1.297642515519999984 ) ) ;
#57531=DIRECTION ( 'NONE',  ( 0.000000000000000000, 1.000000000000000000, 0.000000000000000000 ) ) ;
#57534=CARTESIAN_POINT ( 'NONE',  ( 0.1963495408493637351, -78.53541666666669130, -1.499999999999999778 ) ) ;
#57543=( NAMED_UNIT ( * ) PLANE_ANGLE_UNIT ( ) SI_UNIT ( $, .RADIAN. ) );
#57553=CARTESIAN_POINT ( 'NONE',  ( -1.750000000000000000, -76.50000000000000000, 0.000000000000000000 ) ) ;
#57564=CARTESIAN_POINT ( 'NONE',  ( -0.6144861720749000833, -80.82555782932399779, -1.073086222052999972 ) ) ;
#57576=CARTESIAN_POINT ( 'NONE',  ( 1.500000000000000000, -80.15000000000000568, 0.000000000000000000 ) ) ;
#57585=CARTESIAN_POINT ( 'NONE',  ( -1.000564195253814015, -79.19723941947405876, 0.7893538131252750834 ) ) ;
#57608=EDGE_CURVE ( 'NONE', #52412, #7313, #54520, .T. ) ;
#57610=DIRECTION ( 'NONE',  ( 0.000000000000000000, 1.000000000000000000, 1.232687704540000236E-14 ) ) ;
#57622=AXIS2_PLACEMENT_3D ( 'NONE', #25819, #3393, #21389 ) ;
#57639=CARTESIAN_POINT ( 'NONE',  ( -0.7554284705563544255, -77.91666666666668561, 1.310679582531384169 ) ) ;
#57712=CARTESIAN_POINT ( 'NONE',  ( 1.170174673132000187, -80.01170039560800262, 0.6397400908730001001 ) ) ;
#57722=CIRCLE ( 'NONE', #22882, 2.799999999999999822 ) ;
#57730=CARTESIAN_POINT ( 'NONE',  ( -1.193790227340263632, -79.72197934125595964, 0.4455434364240217215 ) ) ;
#57734=CARTESIAN_POINT ( 'NONE',  ( -0.8719406389885000497, -81.29017953658200213, -1.009106372638000071 ) ) ;
#57752=CARTESIAN_POINT ( 'NONE',  ( -1.402375016663000018, -80.09094972420699321, 0.2083355298385999865 ) ) ;
#57773=CARTESIAN_POINT ( 'NONE',  ( -0.1961711567845059734, -81.78556630387674886, 1.499955683888876123 ) ) ;
#57775=CARTESIAN_POINT ( 'NONE',  ( 1.164640101142631723, -79.93981338681913940, 0.6367143138937826352 ) ) ;
#57780=CARTESIAN_POINT ( 'NONE',  ( 1.500000000000000000, -81.75000000000000000, 0.000000000000000000 ) ) ;
#57786=CARTESIAN_POINT ( 'NONE',  ( -1.199500263597270244, -79.95208333333334849, -0.9218200799623728070 ) ) ;
#57798=CARTESIAN_POINT ( 'NONE',  ( -1.107979503908000041, -78.47287816700719532, -1.174561767264999945 ) ) ;
#57802=CARTESIAN_POINT ( 'NONE',  ( -0.9218200799623775810, -80.92708333333335702, 1.199500263597266247 ) ) ;
#57807=VERTEX_POINT ( 'NONE', #51551 ) ;
#57858=CARTESIAN_POINT ( 'NONE',  ( 1.413837046361000160, -79.54138868576299615, -0.1054710693050000120 ) ) ;
#57859=CARTESIAN_POINT ( 'NONE',  ( 0.1427930653877000078, -78.02442767348290431, 1.311554697429999861 ) ) ;
#57901=B_SPLINE_CURVE_WITH_KNOTS ( 'NONE', 3,
 ( #41941, #6797, #20378, #15945, #24222, #33933 ),
 .UNSPECIFIED., .F., .F.,
 ( 4, 2, 4 ),
 ( 0.000000000000000000, 0.1428612160184655755, 0.2857224320369311510 ),
 .UNSPECIFIED. ) ;
#57929=EDGE_LOOP ( 'NONE', ( #29729, #47337, #12832, #40933 ) ) ;
#57995=EDGE_CURVE ( 'NONE', #27498, #35000, #33800, .T. ) ;
#58007=CARTESIAN_POINT ( 'NONE',  ( 1.170174673132000187, -80.05547441318699953, 0.6397400908730001001 ) ) ;
#58026=CARTESIAN_POINT ( 'NONE',  ( 0.08741542428476450910, -80.11951995081831512, 1.271648086810047706 ) ) ;
#58031=CARTESIAN_POINT ( 'NONE',  ( 0.2153359604882000011, -82.04020749310099347, 1.316133176457000120 ) ) ;
#58039=CARTESIAN_POINT ( 'NONE',  ( 0.4811021089508000226, -81.95005443991800576, -1.323757477563000107 ) ) ;
#58045=CARTESIAN_POINT ( 'NONE',  ( -0.5815971981373999622, -79.69404873715900806, -1.292982629223000002 ) ) ;
#58052=ORIENTED_EDGE ( 'NONE', *, *, #21984, .F. ) ;
#58069=CARTESIAN_POINT ( 'NONE',  ( 1.273811252452706766, -80.40095636055373518, 0.01856756060433174121 ) ) ;
#58080=CARTESIAN_POINT ( 'NONE',  ( 1.199500263597271577, -80.09791666666669130, -0.9218200799623702535 ) ) ;
#58093=CARTESIAN_POINT ( 'NONE',  ( -1.071041487988000140, -79.40975894690099324, -0.9340865940840999970 ) ) ;
#58097=CARTESIAN_POINT ( 'NONE',  ( -0.1963495408493673433, -80.88541666666669983, 1.499999999999999334 ) ) ;
#58099=CARTESIAN_POINT ( 'NONE',  ( 0.1641065589886999965, -78.21905598575500562, 1.507319194642999793 ) ) ;
#58117=LINE ( 'NONE', #26233, #40048 ) ;
#58129=DIRECTION ( 'NONE',  ( 0.000000000000000000, 1.000000000000000000, 0.000000000000000000 ) ) ;
#58153=CARTESIAN_POINT ( 'NONE',  ( 1.185193155257999953, -80.09864567164899540, -1.096599795159000079 ) ) ;
#58202=EDGE_CURVE ( 'NONE', #27498, #33741, #10530, .T. ) ;
#58208=EDGE_LOOP ( 'NONE', ( #16079, #51844, #41738 ) ) ;
#58244=CARTESIAN_POINT ( 'NONE',  ( -1.250000000000000000, -76.40000000064199526, 0.000000000000000000 ) ) ;
#58251=CARTESIAN_POINT ( 'NONE',  ( -0.6878299077642000547, -82.23020250931300268, -1.043738481606000024 ) ) ;
#58287=CARTESIAN_POINT ( 'NONE',  ( -0.1437691919948000108, -81.10984761958199840, -1.608273716018000066 ) ) ;
#58307=CARTESIAN_POINT ( 'NONE',  ( -0.9102058945833000347, -80.65666449956201234, 0.9747214924314999696 ) ) ;
#58324=CARTESIAN_POINT ( 'NONE',  ( 0.4533703023547435151, -79.40394685360605820, -1.191177121937188721 ) ) ;
#58328=CARTESIAN_POINT ( 'NONE',  ( -0.8218343019581000330, -80.75027928519300247, -1.050237832603999832 ) ) ;
#58338=CARTESIAN_POINT ( 'NONE',  ( 0.8482627942206000249, -81.62088116725298903, 1.124385767671000069 ) ) ;
#58344=CARTESIAN_POINT ( 'NONE',  ( -1.410851365044999861, -79.59482349039599569, 0.1398492253880000147 ) ) ;
#58347=CARTESIAN_POINT ( 'NONE',  ( -1.500000000000000000, -79.40884741929301072, -0.1667699247263852436 ) ) ;
#58390=DIRECTION ( 'NONE',  ( 1.000000000000000000, 0.000000000000000000, 0.000000000000000000 ) ) ;
#58395=CIRCLE ( 'NONE', #34777, 0.6999999999999999556 ) ;
#58398=CARTESIAN_POINT ( 'NONE',  ( -0.6374375075192000306, -78.70942315521899957, 1.266385724874999896 ) ) ;
ENDSEC;
END-ISO-10303-21;
